ISO-10303-21;
HEADER;
/* Generated by software containing ST-Developer
 * from STEP Tools, Inc. (www.steptools.com) 
 */

FILE_DESCRIPTION(
/* description */ (''),
/* implementation_level */ '2;1');

FILE_NAME(
/* name */ 'Screw_01.step',
/* time_stamp */ '2026-10-05T21:25:27-07:00',
/* author */ (''),
/* organization */ (''),
/* preprocessor_version */ 'ST-DEVELOPER v20.2',
/* originating_system */ 'Autodesk Translation Framework v15.15.0.0',
/* authorisation */ '');

FILE_SCHEMA (('AUTOMOTIVE_DESIGN { 1 0 10303 214 3 1 1 }'));
ENDSEC;

DATA;
#10=MECHANICAL_DESIGN_GEOMETRIC_PRESENTATION_REPRESENTATION('',(#34),#12118);
#23=B_SPLINE_SURFACE_WITH_KNOTS('',3,3,((#7351,#7352,#7353,#7354,#7355,
#7356,#7357,#7358,#7359,#7360,#7361,#7362,#7363,#7364,#7365,#7366,#7367,
#7368,#7369,#7370,#7371,#7372,#7373,#7374,#7375,#7376,#7377,#7378,#7379,
#7380,#7381,#7382,#7383,#7384,#7385,#7386,#7387,#7388,#7389,#7390,#7391,
#7392),(#7393,#7394,#7395,#7396,#7397,#7398,#7399,#7400,#7401,#7402,#7403,
#7404,#7405,#7406,#7407,#7408,#7409,#7410,#7411,#7412,#7413,#7414,#7415,
#7416,#7417,#7418,#7419,#7420,#7421,#7422,#7423,#7424,#7425,#7426,#7427,
#7428,#7429,#7430,#7431,#7432,#7433,#7434),(#7435,#7436,#7437,#7438,#7439,
#7440,#7441,#7442,#7443,#7444,#7445,#7446,#7447,#7448,#7449,#7450,#7451,
#7452,#7453,#7454,#7455,#7456,#7457,#7458,#7459,#7460,#7461,#7462,#7463,
#7464,#7465,#7466,#7467,#7468,#7469,#7470,#7471,#7472,#7473,#7474,#7475,
#7476),(#7477,#7478,#7479,#7480,#7481,#7482,#7483,#7484,#7485,#7486,#7487,
#7488,#7489,#7490,#7491,#7492,#7493,#7494,#7495,#7496,#7497,#7498,#7499,
#7500,#7501,#7502,#7503,#7504,#7505,#7506,#7507,#7508,#7509,#7510,#7511,
#7512,#7513,#7514,#7515,#7516,#7517,#7518)),.UNSPECIFIED.,.F.,.F.,.F.,(4,
4),(4,1,1,1,1,1,1,1,1,1,1,1,1,1,1,1,1,1,1,1,1,1,1,1,1,1,1,1,1,1,1,1,1,1,
1,1,1,1,1,4),(-0.000255169100126038,0.0463066876673496),(8.31044341387851,
9.3071677964662,10.3037486701926,11.300329543919,12.2969104176454,13.2934912913718,
14.2900721650982,15.2866530388247,16.2832339125511,17.2798147862775,18.2763956600039,
19.2729765337303,20.2695574074567,21.2661382811831,22.2627191549095,23.2593000286359,
24.2558809023623,25.2524617760888,26.2490426498152,27.2456235235416,28.242204397268,
29.2387852709944,30.2353661447208,31.2319470184472,32.2285278921736,33.2251087659,
34.2216896396264,35.2182705133528,36.2148513870793,37.2114322608057,38.2080131345321,
39.2045940082585,40.2011748819849,41.1977557557113,42.1943366294377,43.1909175031641,
44.1874983768905,45.1840792506169,46.1806601243433,47.1772409980698),
 .UNSPECIFIED.);
#24=B_SPLINE_SURFACE_WITH_KNOTS('',3,3,((#7695,#7696,#7697,#7698,#7699,
#7700,#7701,#7702,#7703,#7704,#7705,#7706,#7707,#7708,#7709,#7710,#7711,
#7712,#7713,#7714,#7715,#7716,#7717,#7718,#7719,#7720,#7721,#7722,#7723,
#7724,#7725,#7726,#7727,#7728,#7729,#7730,#7731,#7732,#7733,#7734,#7735,
#7736),(#7737,#7738,#7739,#7740,#7741,#7742,#7743,#7744,#7745,#7746,#7747,
#7748,#7749,#7750,#7751,#7752,#7753,#7754,#7755,#7756,#7757,#7758,#7759,
#7760,#7761,#7762,#7763,#7764,#7765,#7766,#7767,#7768,#7769,#7770,#7771,
#7772,#7773,#7774,#7775,#7776,#7777,#7778),(#7779,#7780,#7781,#7782,#7783,
#7784,#7785,#7786,#7787,#7788,#7789,#7790,#7791,#7792,#7793,#7794,#7795,
#7796,#7797,#7798,#7799,#7800,#7801,#7802,#7803,#7804,#7805,#7806,#7807,
#7808,#7809,#7810,#7811,#7812,#7813,#7814,#7815,#7816,#7817,#7818,#7819,
#7820),(#7821,#7822,#7823,#7824,#7825,#7826,#7827,#7828,#7829,#7830,#7831,
#7832,#7833,#7834,#7835,#7836,#7837,#7838,#7839,#7840,#7841,#7842,#7843,
#7844,#7845,#7846,#7847,#7848,#7849,#7850,#7851,#7852,#7853,#7854,#7855,
#7856,#7857,#7858,#7859,#7860,#7861,#7862)),.UNSPECIFIED.,.F.,.F.,.F.,(4,
4),(4,1,1,1,1,1,1,1,1,1,1,1,1,1,1,1,1,1,1,1,1,1,1,1,1,1,1,1,1,1,1,1,1,1,
1,1,1,1,1,4),(-0.000278939256451679,0.0463345324070479),(11.6151018031581,
12.6120023928371,13.6085832665635,14.6051641402899,15.6017450140163,16.5983258877427,
17.5949067614691,18.5914876351955,19.5880685089219,20.5846493826483,21.5812302563748,
22.5778111301012,23.5743920038276,24.570972877554,25.5675537512804,26.5641346250068,
27.5607154987332,28.5572963724596,29.553877246186,30.5504581199124,31.5470389936388,
32.5436198673653,33.5402007410917,34.5367816148181,35.5333624885445,36.5299433622709,
37.5265242359973,38.5231051097237,39.5196859834501,40.5162668571765,41.5128477309029,
42.5094286046293,43.5060094783558,44.5025903520822,45.4991712258086,46.495752099535,
47.4923329732614,48.4889138469878,49.4854947207142,50.4820755944406),
 .UNSPECIFIED.);
#28=SHAPE_REPRESENTATION_RELATIONSHIP('SRR','None',#12136,#31);
#31=ADVANCED_BREP_SHAPE_REPRESENTATION('',(#37),#12116);
#34=STYLED_ITEM('',(#12159),#37);
#37=MANIFOLD_SOLID_BREP('Body1',#2407);
#56=FACE_BOUND('',#483,.T.);
#79=PLANE('',#2686);
#80=PLANE('',#2687);
#81=PLANE('',#2688);
#82=PLANE('',#2689);
#83=PLANE('',#2690);
#84=PLANE('',#2691);
#85=PLANE('',#2692);
#86=PLANE('',#2693);
#87=PLANE('',#2694);
#237=CIRCLE('',#2669,1.5555);
#238=CIRCLE('',#2676,1.954);
#239=CIRCLE('',#2683,1.954);
#240=CIRCLE('',#2685,1.5555);
#327=FACE_OUTER_BOUND('',#466,.T.);
#328=FACE_OUTER_BOUND('',#467,.T.);
#329=FACE_OUTER_BOUND('',#468,.T.);
#330=FACE_OUTER_BOUND('',#469,.T.);
#331=FACE_OUTER_BOUND('',#470,.T.);
#332=FACE_OUTER_BOUND('',#471,.T.);
#333=FACE_OUTER_BOUND('',#472,.T.);
#334=FACE_OUTER_BOUND('',#473,.T.);
#335=FACE_OUTER_BOUND('',#474,.T.);
#336=FACE_OUTER_BOUND('',#475,.T.);
#337=FACE_OUTER_BOUND('',#476,.T.);
#338=FACE_OUTER_BOUND('',#477,.T.);
#339=FACE_OUTER_BOUND('',#478,.T.);
#340=FACE_OUTER_BOUND('',#479,.T.);
#341=FACE_OUTER_BOUND('',#480,.T.);
#342=FACE_OUTER_BOUND('',#481,.T.);
#343=FACE_OUTER_BOUND('',#482,.T.);
#344=FACE_OUTER_BOUND('',#484,.T.);
#345=FACE_OUTER_BOUND('',#485,.T.);
#346=FACE_OUTER_BOUND('',#486,.T.);
#347=FACE_OUTER_BOUND('',#487,.T.);
#348=FACE_OUTER_BOUND('',#488,.T.);
#349=FACE_OUTER_BOUND('',#489,.T.);
#350=FACE_OUTER_BOUND('',#490,.T.);
#351=FACE_OUTER_BOUND('',#491,.T.);
#466=EDGE_LOOP('',(#1931,#1932,#1933,#1934));
#467=EDGE_LOOP('',(#1935,#1936,#1937,#1938));
#468=EDGE_LOOP('',(#1939,#1940,#1941,#1942));
#469=EDGE_LOOP('',(#1943,#1944,#1945,#1946));
#470=EDGE_LOOP('',(#1947,#1948,#1949,#1950));
#471=EDGE_LOOP('',(#1951,#1952,#1953,#1954));
#472=EDGE_LOOP('',(#1955,#1956,#1957,#1958));
#473=EDGE_LOOP('',(#1959,#1960,#1961,#1962));
#474=EDGE_LOOP('',(#1963,#1964,#1965,#1966));
#475=EDGE_LOOP('',(#1967,#1968,#1969,#1970));
#476=EDGE_LOOP('',(#1971,#1972,#1973,#1974));
#477=EDGE_LOOP('',(#1975,#1976,#1977,#1978));
#478=EDGE_LOOP('',(#1979,#1980,#1981,#1982));
#479=EDGE_LOOP('',(#1983,#1984,#1985,#1986));
#480=EDGE_LOOP('',(#1987,#1988,#1989,#1990,#1991,#1992,#1993,#1994,#1995,
#1996,#1997,#1998,#1999,#2000,#2001,#2002));
#481=EDGE_LOOP('',(#2003,#2004,#2005,#2006,#2007,#2008,#2009,#2010,#2011,
#2012,#2013,#2014,#2015,#2016,#2017,#2018));
#482=EDGE_LOOP('',(#2019,#2020,#2021,#2022));
#483=EDGE_LOOP('',(#2023,#2024,#2025,#2026,#2027,#2028));
#484=EDGE_LOOP('',(#2029,#2030,#2031,#2032));
#485=EDGE_LOOP('',(#2033,#2034,#2035,#2036));
#486=EDGE_LOOP('',(#2037,#2038,#2039,#2040));
#487=EDGE_LOOP('',(#2041,#2042,#2043,#2044));
#488=EDGE_LOOP('',(#2045,#2046,#2047,#2048));
#489=EDGE_LOOP('',(#2049,#2050,#2051,#2052));
#490=EDGE_LOOP('',(#2053,#2054,#2055,#2056,#2057,#2058));
#491=EDGE_LOOP('',(#2059,#2060,#2061,#2062));
#596=LINE('',#4051,#734);
#597=LINE('',#4318,#735);
#598=LINE('',#4342,#736);
#599=LINE('',#4654,#737);
#600=LINE('',#4972,#738);
#601=LINE('',#5320,#739);
#602=LINE('',#5506,#740);
#603=LINE('',#5608,#741);
#604=LINE('',#5992,#742);
#605=LINE('',#6376,#743);
#606=LINE('',#6581,#744);
#607=LINE('',#6785,#745);
#608=LINE('',#8039,#746);
#609=LINE('',#8041,#747);
#610=LINE('',#8043,#748);
#611=LINE('',#8045,#749);
#612=LINE('',#8047,#750);
#613=LINE('',#8048,#751);
#614=LINE('',#8051,#752);
#615=LINE('',#8053,#753);
#616=LINE('',#8054,#754);
#617=LINE('',#8057,#755);
#618=LINE('',#8058,#756);
#619=LINE('',#8061,#757);
#620=LINE('',#8062,#758);
#621=LINE('',#8065,#759);
#622=LINE('',#8066,#760);
#623=LINE('',#8069,#761);
#624=LINE('',#8070,#762);
#625=LINE('',#8072,#763);
#734=VECTOR('',#3256,1.5555);
#735=VECTOR('',#3261,1.5555);
#736=VECTOR('',#3264,1.5555);
#737=VECTOR('',#3267,1.5555);
#738=VECTOR('',#3270,1.5555);
#739=VECTOR('',#3273,1.5555);
#740=VECTOR('',#3276,1.954);
#741=VECTOR('',#3281,1.954);
#742=VECTOR('',#3284,1.954);
#743=VECTOR('',#3287,1.954);
#744=VECTOR('',#3290,1.954);
#745=VECTOR('',#3293,1.954);
#746=VECTOR('',#3304,10.);
#747=VECTOR('',#3305,10.);
#748=VECTOR('',#3306,10.);
#749=VECTOR('',#3307,9.99999999999999);
#750=VECTOR('',#3308,10.);
#751=VECTOR('',#3309,10.);
#752=VECTOR('',#3312,10.);
#753=VECTOR('',#3313,10.);
#754=VECTOR('',#3314,10.);
#755=VECTOR('',#3317,10.);
#756=VECTOR('',#3318,10.);
#757=VECTOR('',#3321,10.);
#758=VECTOR('',#3322,10.);
#759=VECTOR('',#3325,10.);
#760=VECTOR('',#3326,9.99999999999999);
#761=VECTOR('',#3329,10.);
#762=VECTOR('',#3330,10.);
#763=VECTOR('',#3333,10.);
#806=B_SPLINE_CURVE_WITH_KNOTS('',3,(#4053,#4054,#4055,#4056,#4057,#4058,
#4059,#4060,#4061,#4062,#4063,#4064,#4065,#4066,#4067,#4068,#4069,#4070,
#4071,#4072,#4073,#4074,#4075,#4076,#4077,#4078,#4079,#4080,#4081,#4082,
#4083,#4084,#4085,#4086,#4087,#4088,#4089,#4090,#4091,#4092,#4093,#4094,
#4095,#4096,#4097,#4098,#4099,#4100,#4101,#4102,#4103,#4104,#4105,#4106,
#4107,#4108,#4109,#4110,#4111,#4112,#4113,#4114,#4115,#4116,#4117,#4118,
#4119,#4120,#4121,#4122,#4123,#4124,#4125,#4126,#4127,#4128,#4129,#4130,
#4131,#4132,#4133,#4134,#4135,#4136,#4137,#4138,#4139,#4140,#4141,#4142,
#4143,#4144,#4145,#4146,#4147,#4148,#4149,#4150,#4151,#4152,#4153,#4154,
#4155,#4156,#4157,#4158,#4159,#4160,#4161,#4162,#4163,#4164,#4165,#4166,
#4167,#4168,#4169,#4170,#4171,#4172,#4173,#4174,#4175,#4176,#4177,#4178,
#4179,#4180,#4181,#4182,#4183,#4184,#4185,#4186,#4187,#4188,#4189,#4190,
#4191,#4192,#4193,#4194,#4195,#4196,#4197,#4198,#4199,#4200),
 .UNSPECIFIED.,.F.,.F.,(4,3,3,3,3,3,3,3,3,3,3,3,3,3,3,3,3,3,3,3,3,3,3,3,
3,3,3,3,3,3,3,3,3,3,3,3,3,3,3,3,3,3,3,3,3,3,3,3,3,4),(10.3761213044057,
10.4916473343449,10.6020836926387,10.7124212898676,10.8227045964878,10.9329779958561,
11.0433574182079,11.153799603579,11.2644299007573,11.300329543919,11.412228455198,
11.5239351693938,11.6355347254554,11.7470696766159,11.8585824834667,11.9701986021098,
12.0818627300226,12.1937439049619,12.2969104176454,12.4084748637133,12.5198380200048,
12.6310887295725,12.7422701582708,12.8534253726942,12.9646803676604,13.0759808484134,
13.1874988487555,13.2934912913718,13.4052296275761,13.5167698094669,13.6281993328827,
13.7395610570682,13.8508977444198,13.9623346136355,14.07381749289,14.185516391903,
14.2900721650982,14.4018025327098,14.5133353791798,14.6247579576194,14.7361131396909,
14.8474437006735,14.9588751530413,15.0703529943082,15.182047571227,15.2866530388247,
15.4088138904719,15.5306080160377,15.6518307149662,15.7079632679489),
 .UNSPECIFIED.);
#807=B_SPLINE_CURVE_WITH_KNOTS('',3,(#4203,#4204,#4205,#4206,#4207,#4208,
#4209,#4210,#4211,#4212,#4213,#4214,#4215,#4216,#4217,#4218,#4219,#4220,
#4221,#4222,#4223,#4224,#4225,#4226,#4227,#4228,#4229,#4230,#4231,#4232,
#4233,#4234,#4235,#4236,#4237,#4238,#4239,#4240,#4241,#4242,#4243,#4244,
#4245,#4246,#4247,#4248,#4249,#4250,#4251,#4252,#4253,#4254,#4255,#4256,
#4257,#4258,#4259,#4260,#4261,#4262,#4263,#4264,#4265,#4266,#4267,#4268,
#4269,#4270,#4271,#4272,#4273,#4274,#4275,#4276,#4277,#4278,#4279,#4280,
#4281,#4282,#4283,#4284,#4285,#4286,#4287,#4288,#4289,#4290,#4291,#4292,
#4293,#4294,#4295,#4296,#4297,#4298,#4299,#4300,#4301,#4302,#4303,#4304,
#4305,#4306,#4307,#4308,#4309,#4310,#4311,#4312,#4313,#4314),
 .UNSPECIFIED.,.F.,.F.,(4,3,3,3,3,3,3,3,3,3,3,3,3,3,3,3,3,3,3,3,3,3,3,3,
3,3,3,3,3,3,3,3,3,3,3,3,3,4),(11.6154215191107,11.7297194433804,11.8439615074736,
11.9581751212632,12.0723949424661,12.1866556269815,12.3010886611519,12.4156103002373,
12.5303749287406,12.6120023928371,12.722600396268,12.8333482550549,12.9435980012706,
13.0537674854308,13.1639012473881,13.275071752182,13.3853379846654,13.4969606256144,
13.6085832665635,13.7204465169992,13.8321110831577,13.9436645730414,14.0551496181406,
14.16660875264,14.2781656624489,14.3897674585362,14.5015817699047,14.6051641402899,
14.7170632550792,14.8287701821625,14.9403699566644,15.051905131442,15.1634181667176,
15.2750345195736,15.386698885236,15.4985803008963,15.6017450140163,15.7079632679489),
 .UNSPECIFIED.);
#808=B_SPLINE_CURVE_WITH_KNOTS('',3,(#4319,#4320,#4321,#4322,#4323,#4324,
#4325,#4326,#4327,#4328),.UNSPECIFIED.,.F.,.F.,(4,1,1,1,1,1,1,4),(15.7079632679489,
16.2832339125511,17.2798147862775,18.2763956600039,19.2729765337303,20.2695574074567,
21.2661382811831,21.9911485751285),.UNSPECIFIED.);
#809=B_SPLINE_CURVE_WITH_KNOTS('',3,(#4329,#4330,#4331,#4332,#4333,#4334,
#4335,#4336,#4337,#4338),.UNSPECIFIED.,.F.,.F.,(4,1,1,1,1,1,1,4),(15.7079720007471,
16.5983258877427,17.5949067614691,18.5914876351955,19.5880685089219,20.5846493826483,
21.5812302563748,21.9911424371547),.UNSPECIFIED.);
#810=B_SPLINE_CURVE_WITH_KNOTS('',3,(#4343,#4344,#4345,#4346,#4347,#4348,
#4349,#4350,#4351,#4352,#4353,#4354,#4355,#4356,#4357,#4358,#4359,#4360,
#4361,#4362,#4363,#4364,#4365,#4366,#4367,#4368,#4369,#4370,#4371,#4372,
#4373,#4374,#4375,#4376,#4377,#4378,#4379,#4380,#4381,#4382,#4383,#4384,
#4385,#4386,#4387,#4388,#4389,#4390,#4391,#4392,#4393,#4394,#4395,#4396,
#4397,#4398,#4399,#4400,#4401,#4402,#4403,#4404,#4405,#4406,#4407,#4408,
#4409,#4410,#4411,#4412,#4413,#4414,#4415,#4416,#4417,#4418,#4419,#4420,
#4421,#4422,#4423,#4424,#4425,#4426,#4427,#4428,#4429,#4430,#4431,#4432,
#4433,#4434,#4435,#4436,#4437,#4438,#4439,#4440,#4441,#4442,#4443,#4444,
#4445,#4446,#4447,#4448,#4449,#4450,#4451,#4452,#4453,#4454,#4455,#4456,
#4457,#4458,#4459,#4460,#4461,#4462,#4463,#4464,#4465,#4466,#4467,#4468,
#4469,#4470,#4471,#4472,#4473,#4474,#4475,#4476,#4477,#4478,#4479,#4480,
#4481,#4482,#4483,#4484,#4485,#4486,#4487,#4488,#4489,#4490,#4491,#4492,
#4493,#4494,#4495,#4496,#4497,#4498,#4499,#4500,#4501,#4502,#4503,#4504,
#4505,#4506,#4507,#4508,#4509,#4510,#4511,#4512,#4513,#4514),
 .UNSPECIFIED.,.F.,.F.,(4,3,3,3,3,3,3,3,3,3,3,3,3,3,3,3,3,3,3,3,3,3,3,3,
3,3,3,3,3,3,3,3,3,3,3,3,3,3,3,3,3,3,3,3,3,3,3,3,3,3,3,3,3,3,3,3,3,4),(21.9911485751285,
22.1309179503363,22.2627191549095,22.374427659155,22.4859378873353,22.5973374041086,
22.708669121392,22.8199758541663,22.9313830961259,23.0428364782557,23.1545064918532,
23.2593000286359,23.3710083890299,23.4825184720439,23.5939178429524,23.7052494139272,
23.8165560002028,23.9279630965552,24.0394163333242,24.1510862038985,24.2558809023623,
24.3675891950941,24.479099207913,24.5904985071345,24.7018300050549,24.8131365170311,
24.9245435377139,25.0359966979394,25.1476664914795,25.2524617760888,25.3641701458249,
25.4756802374145,25.5870796164264,25.698411195018,25.8097177884088,25.9211248910232,
26.0325781335982,26.1442480091205,26.2490426498152,26.3607509985506,26.4722610688441,
26.5836604263951,26.6949919833986,26.8062985551115,26.9177056360823,27.0291588569968,
27.1408287111152,27.2456235235416,27.3573318547298,27.4688419071979,27.5802412467662,
27.6915727856601,27.8028793391664,27.9142864019218,28.0257396045861,28.1374094406315,
28.242204397268,28.2743338823081),.UNSPECIFIED.);
#811=B_SPLINE_CURVE_WITH_KNOTS('',3,(#4515,#4516,#4517,#4518,#4519,#4520,
#4521,#4522,#4523,#4524,#4525,#4526,#4527,#4528,#4529,#4530,#4531,#4532,
#4533,#4534,#4535,#4536,#4537,#4538,#4539,#4540,#4541,#4542,#4543,#4544,
#4545,#4546,#4547,#4548,#4549,#4550,#4551,#4552,#4553,#4554,#4555,#4556,
#4557,#4558,#4559,#4560,#4561,#4562,#4563,#4564,#4565,#4566,#4567,#4568,
#4569,#4570,#4571,#4572,#4573,#4574,#4575,#4576,#4577,#4578,#4579,#4580,
#4581,#4582,#4583,#4584,#4585,#4586,#4587,#4588,#4589,#4590,#4591,#4592,
#4593,#4594,#4595,#4596,#4597,#4598,#4599,#4600,#4601,#4602,#4603,#4604,
#4605,#4606,#4607,#4608,#4609,#4610,#4611,#4612,#4613,#4614,#4615,#4616,
#4617,#4618,#4619,#4620,#4621,#4622,#4623,#4624,#4625,#4626,#4627,#4628,
#4629,#4630,#4631,#4632,#4633,#4634,#4635,#4636,#4637,#4638,#4639,#4640,
#4641,#4642,#4643,#4644,#4645,#4646,#4647,#4648,#4649,#4650),
 .UNSPECIFIED.,.F.,.F.,(4,2,2,2,2,2,2,2,2,2,2,2,2,2,2,2,2,2,2,2,2,2,2,2,
2,2,2,2,2,2,2,2,2,2,2,2,2,2,2,2,2,2,2,2,2,2,2,2,2,2,2,2,2,2,2,2,2,2,2,2,
2,2,2,2,2,2,2,4),(-1.96082459543352,-1.95572351555056,-1.95066052951545,
-1.94362170361263,-1.93425075381217,-1.89502168228356,-1.87686387526354,
-1.87099759837285,-1.86650686710055,-1.85991368343642,-1.83588912387465,
-1.80491110925764,-1.79532103382858,-1.78754943506346,-1.77785045005196,
-1.7395832934319,-1.72145183028369,-1.71558876144544,-1.71109950362509,
-1.70450637904612,-1.67320765345622,-1.65092649870745,-1.64080239574451,
-1.63301540424833,-1.62377482636635,-1.58389582607512,-1.56598209910372,
-1.56013204953622,-1.55564145708863,-1.54903042008476,-1.52394393778717,
-1.50382039511072,-1.48957010087417,-1.481248627308,-1.47318169192042,-1.46067683095659,
-1.42781445661822,-1.41047349388771,-1.40466023251355,-1.40016532168693,
-1.39350050808931,-1.37077895797284,-1.34927674386887,-1.3385618526334,
-1.32899645945264,-1.32122258433739,-1.31149266274323,-1.27340973791122,
-1.25516680284208,-1.24929583368251,-1.24480601384231,-1.2382202508283,
-1.20684840126156,-1.18455492795627,-1.17444672041409,-1.16665843787414,
-1.15740148906793,-1.11777668409297,-1.09966402284823,-1.09380036224297,
-1.08930943635981,-1.08379516053843,-1.05304373469511,-1.02891096525692,
-1.01886083081681,-1.01107500165632,-1.00177403653395,-0.980700216948197),
 .UNSPECIFIED.);
#812=B_SPLINE_CURVE_WITH_KNOTS('',3,(#4655,#4656,#4657,#4658,#4659,#4660,
#4661,#4662,#4663,#4664,#4665,#4666,#4667,#4668,#4669,#4670,#4671,#4672,
#4673,#4674,#4675,#4676,#4677,#4678,#4679,#4680,#4681,#4682,#4683,#4684,
#4685,#4686,#4687,#4688,#4689,#4690,#4691,#4692,#4693,#4694,#4695,#4696,
#4697,#4698,#4699,#4700,#4701,#4702,#4703,#4704,#4705,#4706,#4707,#4708,
#4709,#4710,#4711,#4712,#4713,#4714,#4715,#4716,#4717,#4718,#4719,#4720,
#4721,#4722,#4723,#4724,#4725,#4726,#4727,#4728,#4729,#4730,#4731,#4732,
#4733,#4734,#4735,#4736,#4737,#4738,#4739,#4740,#4741,#4742,#4743,#4744,
#4745,#4746,#4747,#4748,#4749,#4750,#4751,#4752,#4753,#4754,#4755,#4756,
#4757,#4758,#4759,#4760,#4761,#4762,#4763,#4764,#4765,#4766,#4767,#4768,
#4769,#4770,#4771,#4772,#4773,#4774,#4775,#4776,#4777,#4778,#4779,#4780,
#4781,#4782,#4783,#4784,#4785,#4786,#4787,#4788,#4789,#4790,#4791,#4792,
#4793,#4794,#4795,#4796,#4797,#4798,#4799,#4800,#4801,#4802,#4803,#4804,
#4805,#4806,#4807,#4808,#4809,#4810,#4811,#4812,#4813,#4814,#4815,#4816,
#4817,#4818,#4819,#4820,#4821,#4822,#4823,#4824,#4825,#4826),
 .UNSPECIFIED.,.F.,.F.,(4,3,3,3,3,3,3,3,3,3,3,3,3,3,3,3,3,3,3,3,3,3,3,3,
3,3,3,3,3,3,3,3,3,3,3,3,3,3,3,3,3,3,3,3,3,3,3,3,3,3,3,3,3,3,3,3,3,4),(28.2743338828609,
28.3854499463251,28.4963720118463,28.6071867805496,28.717938100074,28.8286697232355,
28.9395040413308,29.0503910293876,29.1614837232969,29.2387852709944,29.3504936415299,
29.4620037336246,29.5734031129626,29.6847346917021,29.7960412850626,29.9074483873678,
30.0189016294807,30.1305715042882,30.2353661447208,30.3470744333654,30.4585844436019,
30.5699837411555,30.6813152383202,30.7926217504514,30.9040287727148,31.0154819353027,
31.1271517324973,31.2319470184472,31.3436553843173,31.4551654707913,31.5665648439343,
31.6778964159217,31.7892030019896,31.9006100962241,32.012063329828,32.123733195506,
32.2285278921736,32.340236400346,32.4517466310075,32.5631461493832,32.6744778673927,
32.785784600018,32.8971918404589,33.008645220319,33.1203152304053,33.2251087659,
33.3368166944273,33.448326345267,33.5597252840979,33.6710564238064,33.782362580341,
33.8937692527465,34.0052220680337,34.1168915267859,34.2216896396264,34.3523579101837,
34.481718471603,34.5575191891205),.UNSPECIFIED.);
#813=B_SPLINE_CURVE_WITH_KNOTS('',3,(#4827,#4828,#4829,#4830,#4831,#4832,
#4833,#4834,#4835,#4836,#4837,#4838,#4839,#4840,#4841,#4842,#4843,#4844,
#4845,#4846,#4847,#4848,#4849,#4850,#4851,#4852,#4853,#4854,#4855,#4856,
#4857,#4858,#4859,#4860,#4861,#4862,#4863,#4864,#4865,#4866,#4867,#4868,
#4869,#4870,#4871,#4872,#4873,#4874,#4875,#4876,#4877,#4878,#4879,#4880,
#4881,#4882,#4883,#4884,#4885,#4886,#4887,#4888,#4889,#4890,#4891,#4892,
#4893,#4894,#4895,#4896,#4897,#4898,#4899,#4900,#4901,#4902,#4903,#4904,
#4905,#4906,#4907,#4908,#4909,#4910,#4911,#4912,#4913,#4914,#4915,#4916,
#4917,#4918,#4919,#4920,#4921,#4922,#4923,#4924,#4925,#4926,#4927,#4928,
#4929,#4930,#4931,#4932,#4933,#4934,#4935,#4936,#4937,#4938,#4939,#4940,
#4941,#4942,#4943,#4944,#4945,#4946,#4947,#4948,#4949,#4950,#4951,#4952,
#4953,#4954,#4955,#4956,#4957,#4958,#4959,#4960,#4961,#4962,#4963,#4964,
#4965,#4966,#4967,#4968),.UNSPECIFIED.,.F.,.F.,(4,2,2,2,2,2,2,2,2,2,2,2,
2,2,2,2,2,2,2,2,2,2,2,2,2,2,2,2,2,2,2,2,2,2,2,2,2,2,2,2,2,2,2,2,2,2,2,2,
2,2,2,2,2,2,2,2,2,2,2,2,2,2,2,2,2,2,2,2,2,2,4),(-0.980700216948197,-0.980559999268628,
-0.955579621572852,-0.943370892251875,-0.937835489269082,-0.933291897005555,
-0.926150713138604,-0.916953615712503,-0.891349546080903,-0.871223254441055,
-0.861966129363549,-0.854176350201917,-0.844064404906459,-0.821753526458986,
-0.790354057030155,-0.783765544398651,-0.779274810972388,-0.77340375146535,
-0.755163698290188,-0.717100806565004,-0.707370007481461,-0.699594528982264,
-0.690026074686523,-0.661308930911707,-0.634689541588939,-0.628178275122494,
-0.623692439346925,-0.617763729956392,-0.598443836723945,-0.562381120374292,
-0.552467797355895,-0.544680065830786,-0.535405586845253,-0.512220539516689,
-0.478626029675242,-0.472375693210019,-0.467898681844763,-0.461744853680482,
-0.437725670751447,-0.407116607316036,-0.397117959937511,-0.389324669566922,
-0.380112242331538,-0.357849119206682,-0.324943098177345,-0.317823703984556,
-0.313282767370483,-0.307736107332356,-0.293540257053314,-0.262376920178938,
-0.246674845683532,-0.238147767728558,-0.230193327463652,-0.218508298981253,
-0.20401103902391,-0.179203341412983,-0.165928827760339,-0.160404579058862,
-0.155858235240732,-0.14869449556963,-0.139455516781709,-0.113568526872797,
-0.093603434538257,-0.0844122465129277,-0.0766165286016932,-0.0664092592360509,
-0.041010860894887,-0.0117519087702631,-0.00581551109514165,-0.00289996074689045,
-0.000457478146548932),.UNSPECIFIED.);
#814=B_SPLINE_CURVE_WITH_KNOTS('',3,(#4973,#4974,#4975,#4976,#4977,#4978,
#4979,#4980,#4981,#4982,#4983,#4984,#4985,#4986,#4987,#4988,#4989,#4990,
#4991,#4992,#4993,#4994,#4995,#4996,#4997,#4998,#4999,#5000,#5001,#5002,
#5003,#5004,#5005,#5006,#5007,#5008,#5009,#5010,#5011,#5012,#5013,#5014,
#5015,#5016,#5017,#5018,#5019,#5020,#5021,#5022,#5023,#5024,#5025,#5026,
#5027,#5028,#5029,#5030,#5031,#5032,#5033,#5034,#5035,#5036,#5037,#5038,
#5039,#5040,#5041,#5042,#5043,#5044,#5045,#5046,#5047,#5048,#5049,#5050,
#5051,#5052,#5053,#5054,#5055,#5056,#5057,#5058,#5059,#5060,#5061,#5062,
#5063,#5064,#5065,#5066,#5067,#5068,#5069,#5070,#5071,#5072,#5073,#5074,
#5075,#5076,#5077,#5078,#5079,#5080,#5081,#5082,#5083,#5084,#5085,#5086,
#5087,#5088,#5089,#5090,#5091,#5092,#5093,#5094,#5095,#5096,#5097,#5098,
#5099,#5100,#5101,#5102,#5103,#5104,#5105,#5106,#5107,#5108,#5109,#5110,
#5111,#5112,#5113,#5114,#5115,#5116,#5117,#5118,#5119,#5120,#5121,#5122,
#5123,#5124,#5125,#5126,#5127,#5128,#5129,#5130,#5131,#5132,#5133,#5134,
#5135,#5136,#5137,#5138,#5139,#5140,#5141,#5142,#5143,#5144),
 .UNSPECIFIED.,.F.,.F.,(4,3,3,3,3,3,3,3,3,3,3,3,3,3,3,3,3,3,3,3,3,3,3,3,
3,3,3,3,3,3,3,3,3,3,3,3,3,3,3,3,3,3,3,3,3,3,3,3,3,3,3,3,3,3,3,3,3,4),(34.5575191894877,
34.6688302723381,34.7801258851519,34.8915360000218,35.0030001705124,35.1146924423317,
35.2182705133528,35.329979844159,35.4414909051851,35.5528912580536,35.6642238132373,
35.7755313842774,35.8869394583063,35.9983936704943,36.1100644998149,36.2148513870793,
36.3265566868323,36.4380637110229,36.5494600262282,36.660788549687,36.7720921017016,
36.8834962086944,36.9949464756926,37.1066134484121,37.2114322608057,37.3231433221254,
37.4346560660442,37.5460580718723,37.6573922476747,37.7687014045501,37.8801109978222,
37.9915666953808,38.1032389338652,38.2080131345321,38.3197270786043,38.4312428141906,
38.5426478756073,38.6539851650299,38.7652974877472,38.8767103021911,38.9881692564663,
39.0998447680598,39.2045940082585,39.3162806032607,39.4277689172748,39.5391465312969,
39.6504563936481,39.7617413557063,39.8731271322649,39.9845591801971,40.0962083605028,
40.2011748819849,40.31341306353,40.4254718990605,40.5373841223233,40.6492090027682,
40.7610153241073,40.8407044966673),.UNSPECIFIED.);
#815=B_SPLINE_CURVE_WITH_KNOTS('',3,(#5145,#5146,#5147,#5148,#5149,#5150,
#5151,#5152,#5153,#5154,#5155,#5156,#5157,#5158,#5159,#5160,#5161,#5162,
#5163,#5164,#5165,#5166,#5167,#5168,#5169,#5170,#5171,#5172,#5173,#5174,
#5175,#5176,#5177,#5178,#5179,#5180,#5181,#5182,#5183,#5184,#5185,#5186,
#5187,#5188,#5189,#5190,#5191,#5192,#5193,#5194,#5195,#5196,#5197,#5198,
#5199,#5200,#5201,#5202,#5203,#5204,#5205,#5206,#5207,#5208,#5209,#5210,
#5211,#5212,#5213,#5214,#5215,#5216,#5217,#5218,#5219,#5220,#5221,#5222,
#5223,#5224,#5225,#5226,#5227,#5228,#5229,#5230,#5231,#5232,#5233,#5234,
#5235,#5236,#5237,#5238,#5239,#5240,#5241,#5242,#5243,#5244,#5245,#5246,
#5247,#5248,#5249,#5250,#5251,#5252,#5253,#5254,#5255,#5256,#5257,#5258,
#5259,#5260,#5261,#5262,#5263,#5264,#5265,#5266,#5267,#5268,#5269,#5270,
#5271,#5272,#5273,#5274,#5275,#5276,#5277,#5278,#5279,#5280,#5281,#5282,
#5283,#5284,#5285,#5286,#5287,#5288,#5289,#5290,#5291,#5292,#5293,#5294,
#5295,#5296,#5297,#5298,#5299,#5300,#5301,#5302,#5303,#5304,#5305,#5306,
#5307,#5308,#5309,#5310,#5311,#5312,#5313,#5314,#5315,#5316),
 .UNSPECIFIED.,.F.,.F.,(4,3,3,3,3,3,3,3,3,3,3,3,3,3,3,3,3,3,3,3,3,3,3,3,
3,3,3,3,3,3,3,3,3,3,3,3,3,3,3,3,3,3,3,3,3,3,3,3,3,3,3,3,3,3,3,3,3,4),(34.557519189864,
34.6688316922454,34.7799480549331,34.8909555466977,35.0018977265955,35.1128180578457,
35.2238400790168,35.3349122896089,35.4461940347628,35.5333624885445,35.6450709986201,
35.7565812311951,35.8679807514893,35.979312471419,36.0906192059629,36.2020264483048,
36.3134798300592,36.4251498420041,36.5299433622709,36.6416512870095,36.7531609340693,
36.8645598691282,36.9758910050783,37.0871971578744,37.1986038266027,37.3100566382398,
37.4217260934355,37.5265242359973,37.6382328481534,37.7497431759177,37.861142787168,
37.9724745937193,38.083781410444,38.1951887274328,38.3066421798416,38.4183122548368,
38.5231051097237,38.634814450544,38.7463255216521,38.8577258846372,38.9690584499546,
39.0803660311284,39.19177411521,39.3032283374232,39.4148991765908,39.5196859834501,
39.6313912609589,39.742898262931,39.8542945559478,39.9656230572846,40.0769265872801,
40.1883306725883,40.2997809180488,40.4114478697594,40.5162668571765,40.6484523927198,
40.7791766765676,40.8407044966673),.UNSPECIFIED.);
#816=B_SPLINE_CURVE_WITH_KNOTS('',3,(#5321,#5322,#5323,#5324,#5325,#5326,
#5327,#5328,#5329,#5330,#5331,#5332,#5333,#5334,#5335,#5336,#5337,#5338,
#5339,#5340,#5341,#5342,#5343,#5344,#5345,#5346,#5347,#5348,#5349,#5350,
#5351,#5352,#5353,#5354,#5355,#5356,#5357,#5358,#5359,#5360,#5361,#5362,
#5363,#5364,#5365,#5366,#5367,#5368,#5369,#5370,#5371,#5372,#5373,#5374,
#5375,#5376,#5377,#5378,#5379,#5380,#5381,#5382,#5383,#5384,#5385,#5386,
#5387,#5388,#5389,#5390,#5391,#5392,#5393,#5394,#5395,#5396,#5397,#5398,
#5399,#5400,#5401,#5402,#5403,#5404,#5405,#5406,#5407,#5408,#5409,#5410,
#5411,#5412,#5413,#5414,#5415,#5416,#5417,#5418,#5419,#5420,#5421,#5422,
#5423,#5424,#5425,#5426,#5427,#5428,#5429,#5430,#5431,#5432,#5433,#5434,
#5435,#5436,#5437,#5438,#5439,#5440,#5441,#5442,#5443,#5444,#5445,#5446,
#5447,#5448,#5449,#5450,#5451,#5452,#5453,#5454,#5455,#5456,#5457,#5458,
#5459,#5460,#5461,#5462,#5463,#5464,#5465,#5466,#5467,#5468,#5469,#5470,
#5471,#5472,#5473,#5474,#5475,#5476,#5477,#5478,#5479,#5480,#5481,#5482,
#5483,#5484,#5485,#5486,#5487,#5488,#5489,#5490,#5491,#5492),
 .UNSPECIFIED.,.F.,.F.,(4,3,3,3,3,3,3,3,3,3,3,3,3,3,3,3,3,3,3,3,3,3,3,3,
3,3,3,3,3,3,3,3,3,3,3,3,3,3,3,3,3,3,3,3,3,3,3,3,3,3,3,3,3,3,3,3,3,4),(40.840704497049,
40.9675412582681,41.0954926672067,41.1977557557113,41.3094929575612,41.4210324227689,
41.5324614834252,41.643822998072,41.755159728709,41.8665970369414,41.9780805721874,
42.0897804857432,42.1943366294377,42.3058933565765,42.4172516335833,42.5284991889106,
42.6396791835826,42.750834681469,42.8620926517494,42.9733975818198,43.0849224744629,
43.1909175031641,43.3028373726712,43.4145573215696,43.5261654134577,43.6377042144518,
43.7492161924285,43.8608241682442,43.972476138112,44.0843385386926,44.1874983768905,
44.2993486307196,44.4110045193044,44.5225519596468,44.6340335782541,44.7454919074657,
44.8570521214737,44.9686594749185,45.0804830762105,45.1840792506169,45.2946069224391,
45.4053635726771,45.5155858115154,45.6257438851438,45.7358823024636,45.8470767579335,
45.9573868777162,46.0690235010298,46.1806601243433,46.2985638342812,46.4122814276395,
46.5258600264502,46.6393375177505,46.7527516466315,46.8661750751564,46.9796037930556,
47.09312121241,47.1238898038469),.UNSPECIFIED.);
#817=B_SPLINE_CURVE_WITH_KNOTS('',3,(#5493,#5494,#5495,#5496,#5497,#5498,
#5499,#5500,#5501,#5502),.UNSPECIFIED.,.F.,.F.,(4,1,1,1,1,1,1,4),(40.8407044966673,
41.5128477309029,42.5094286046293,43.5060094783558,44.5025903520822,45.4991712258086,
46.495752099535,47.1238898038469),.UNSPECIFIED.);
#818=B_SPLINE_CURVE_WITH_KNOTS('',3,(#5508,#5509,#5510,#5511,#5512,#5513,
#5514,#5515,#5516,#5517,#5518,#5519,#5520,#5521,#5522,#5523,#5524,#5525,
#5526,#5527,#5528,#5529,#5530,#5531,#5532,#5533,#5534,#5535,#5536,#5537,
#5538,#5539,#5540,#5541,#5542,#5543,#5544,#5545,#5546,#5547,#5548,#5549,
#5550,#5551,#5552,#5553,#5554,#5555,#5556,#5557,#5558,#5559,#5560,#5561,
#5562,#5563,#5564,#5565,#5566,#5567,#5568),.UNSPECIFIED.,.F.,.F.,(4,3,3,
3,3,3,3,3,3,3,3,3,3,3,3,3,3,3,3,3,4),(-4.09254174883831,-3.98632349490564,
-3.88060657601914,-3.77504892759548,-3.66961679425284,-3.56425173722798,
-3.45891795737595,-3.35357970118941,-3.24813369183697,-3.14262668426919,
-3.03694351958987,-2.98974262117923,-2.88522737486619,-2.78088717581068,
-2.67664451339598,-2.5724618858615,-2.46830187348436,-2.36405791614848,
-2.25977409419917,-2.15530886452126,-2.0655090872996),.UNSPECIFIED.);
#819=B_SPLINE_CURVE_WITH_KNOTS('',3,(#5571,#5572,#5573,#5574,#5575,#5576,
#5577,#5578,#5579,#5580,#5581,#5582,#5583,#5584,#5585,#5586,#5587,#5588,
#5589,#5590,#5591,#5592,#5593,#5594,#5595,#5596,#5597,#5598,#5599,#5600,
#5601,#5602,#5603,#5604),.UNSPECIFIED.,.F.,.F.,(4,3,3,3,3,3,3,3,3,3,3,4),
(0.,0.107961337641777,0.219038779652356,0.32692137897961,0.434806064728328,
0.542722047025844,0.656186753700985,0.764334836393942,0.872582285248764,
0.981026153163086,0.996580873726409,1.11419103802958),.UNSPECIFIED.);
#820=B_SPLINE_CURVE_WITH_KNOTS('',3,(#5609,#5610,#5611,#5612,#5613,#5614,
#5615,#5616,#5617,#5618,#5619,#5620,#5621,#5622,#5623,#5624,#5625,#5626,
#5627,#5628,#5629,#5630,#5631,#5632,#5633,#5634,#5635,#5636,#5637,#5638,
#5639,#5640,#5641,#5642,#5643,#5644,#5645,#5646,#5647,#5648,#5649,#5650,
#5651,#5652,#5653,#5654,#5655,#5656,#5657,#5658,#5659,#5660,#5661,#5662,
#5663,#5664,#5665,#5666,#5667,#5668,#5669,#5670,#5671,#5672,#5673,#5674,
#5675,#5676,#5677,#5678,#5679,#5680,#5681,#5682,#5683,#5684,#5685,#5686,
#5687,#5688,#5689,#5690,#5691,#5692,#5693,#5694,#5695,#5696,#5697,#5698,
#5699,#5700,#5701,#5702,#5703,#5704,#5705,#5706,#5707,#5708,#5709,#5710,
#5711,#5712,#5713,#5714,#5715,#5716,#5717,#5718,#5719,#5720,#5721,#5722,
#5723,#5724,#5725,#5726,#5727,#5728,#5729,#5730,#5731,#5732,#5733,#5734,
#5735,#5736,#5737,#5738,#5739,#5740,#5741,#5742,#5743,#5744,#5745,#5746,
#5747,#5748,#5749,#5750,#5751,#5752,#5753,#5754,#5755,#5756,#5757,#5758,
#5759,#5760,#5761,#5762,#5763,#5764,#5765,#5766,#5767,#5768,#5769,#5770,
#5771,#5772,#5773,#5774,#5775,#5776,#5777,#5778,#5779,#5780,#5781,#5782,
#5783,#5784,#5785,#5786,#5787,#5788,#5789,#5790,#5791,#5792,#5793,#5794,
#5795,#5796,#5797,#5798),.UNSPECIFIED.,.F.,.F.,(4,3,3,3,3,3,3,3,3,3,3,3,
3,3,3,3,3,3,3,3,3,3,3,3,3,3,3,3,3,3,3,3,3,3,3,3,3,3,3,3,3,3,3,3,3,3,3,3,
3,3,3,3,3,3,3,3,3,3,3,3,3,3,3,4),(-10.3757270556279,-10.2603201973078,-10.1445336437559,
-10.0282150027604,-9.96580873726409,-9.86028927215325,-9.75492847331706,
-9.6496913482242,-9.54452003581519,-9.43937844760697,-9.33423053922643,
-9.22897081685296,-9.12364803666887,-9.01814404094803,-8.96922786353768,
-8.863705637873,-8.75834200872326,-8.65310196527414,-8.5479276817438,-8.44278307461428,
-8.33763210442475,-8.23236927738943,-8.12704336360682,-8.02153622334531,
-7.97264698981127,-7.86715075765799,-7.76181321062034,-7.65659925346559,
-7.55145104369271,-7.44633245870662,-7.34120741993231,-7.23597021141748,
-7.13066977480087,-7.02518762842017,-6.97606611608487,-6.87052576919234,
-6.76514418013919,-6.65988649813286,-6.55469478529851,-6.44953298257141,
-6.34436507518076,-6.23908581202832,-6.13374372441398,-6.02822097903253,
-5.97948524235845,-5.87394087033655,-5.7685547754276,-5.66329190907336,
-5.55809459516585,-5.45292678697878,-5.34775248164716,-5.24246628022611,
-5.13711693603417,-5.0315865271823,-4.98290436863205,-4.87887809662517,
-4.77503069661954,-4.67128271432362,-4.56759611534957,-4.46393295588717,
-4.36019408038188,-4.25641481532166,-4.15247510001585,-4.09254174928665),
 .UNSPECIFIED.);
#821=B_SPLINE_CURVE_WITH_KNOTS('',3,(#5799,#5800,#5801,#5802,#5803,#5804,
#5805,#5806,#5807,#5808,#5809,#5810,#5811,#5812,#5813,#5814,#5815,#5816,
#5817,#5818,#5819,#5820,#5821,#5822,#5823,#5824,#5825,#5826,#5827,#5828,
#5829,#5830,#5831,#5832,#5833,#5834,#5835,#5836,#5837,#5838,#5839,#5840,
#5841,#5842,#5843,#5844,#5845,#5846,#5847,#5848,#5849,#5850,#5851,#5852,
#5853,#5854,#5855,#5856,#5857,#5858,#5859,#5860,#5861,#5862,#5863,#5864,
#5865,#5866,#5867,#5868,#5869,#5870,#5871,#5872,#5873,#5874,#5875,#5876,
#5877,#5878,#5879,#5880,#5881,#5882,#5883,#5884,#5885,#5886,#5887,#5888,
#5889,#5890,#5891,#5892,#5893,#5894,#5895,#5896,#5897,#5898,#5899,#5900,
#5901,#5902,#5903,#5904,#5905,#5906,#5907,#5908,#5909,#5910,#5911,#5912,
#5913,#5914,#5915,#5916,#5917,#5918,#5919,#5920,#5921,#5922,#5923,#5924,
#5925,#5926,#5927,#5928,#5929,#5930,#5931,#5932,#5933,#5934,#5935,#5936,
#5937,#5938,#5939,#5940,#5941,#5942,#5943,#5944,#5945,#5946,#5947,#5948,
#5949,#5950,#5951,#5952,#5953,#5954,#5955,#5956,#5957,#5958,#5959,#5960,
#5961,#5962,#5963,#5964,#5965,#5966,#5967,#5968,#5969,#5970,#5971,#5972,
#5973,#5974,#5975,#5976,#5977,#5978,#5979,#5980,#5981,#5982,#5983,#5984,
#5985,#5986,#5987,#5988),.UNSPECIFIED.,.F.,.F.,(4,3,3,3,3,3,3,3,3,3,3,3,
3,3,3,3,3,3,3,3,3,3,3,3,3,3,3,3,3,3,3,3,3,3,3,3,3,3,3,3,3,3,3,3,3,3,3,3,
3,3,3,3,3,3,3,3,3,3,3,3,3,3,3,4),(1.1141910384302,1.2172423853623,1.32013451940761,
1.42293952840393,1.52569615018631,1.62844303717393,1.73128762649985,1.83418552892848,
1.93726302853859,1.99316174745282,2.09882380530123,2.20432723759872,2.30970630945708,
2.41501904637488,2.52030130546144,2.62558889901074,2.73098582593685,2.83644458423473,
2.94208122698995,2.98974262117923,3.09543951511609,3.20098166055251,3.30640502061644,
3.41176548868153,3.51709885740485,3.62244087819006,3.72789690172125,3.83341751347036,
3.93911962813814,3.98632349490564,4.09170446142591,4.19692477051415,4.30201914206343,
4.40704637515926,4.51204277383519,4.61704459671689,4.72215786837964,4.82733377202005,
4.93269176979819,4.98290436863205,5.08844958739663,5.19383628319028,5.29909938551086,
5.40429670879892,5.50946430050002,5.61463816395977,5.71992358734206,5.82527196030871,
5.93080111180717,5.97948524235846,6.08502293419111,6.19040246033158,6.29565896133585,
6.40085004111375,6.50601175791141,6.61118012626036,6.71646067026059,6.82180450898163,
6.92732970844788,6.97606611608486,7.09145618049362,7.20651961582521,7.32105406185248,
7.39737634485402),.UNSPECIFIED.);
#822=B_SPLINE_CURVE_WITH_KNOTS('',3,(#5993,#5994,#5995,#5996,#5997,#5998,
#5999,#6000,#6001,#6002,#6003,#6004,#6005,#6006,#6007,#6008,#6009,#6010,
#6011,#6012,#6013,#6014,#6015,#6016,#6017,#6018,#6019,#6020,#6021,#6022,
#6023,#6024,#6025,#6026,#6027,#6028,#6029,#6030,#6031,#6032,#6033,#6034,
#6035,#6036,#6037,#6038,#6039,#6040,#6041,#6042,#6043,#6044,#6045,#6046,
#6047,#6048,#6049,#6050,#6051,#6052,#6053,#6054,#6055,#6056,#6057,#6058,
#6059,#6060,#6061,#6062,#6063,#6064,#6065,#6066,#6067,#6068,#6069,#6070,
#6071,#6072,#6073,#6074,#6075,#6076,#6077,#6078,#6079,#6080,#6081,#6082,
#6083,#6084,#6085,#6086,#6087,#6088,#6089,#6090,#6091,#6092,#6093,#6094,
#6095,#6096,#6097,#6098,#6099,#6100,#6101,#6102,#6103,#6104,#6105,#6106,
#6107,#6108,#6109,#6110,#6111,#6112,#6113,#6114,#6115,#6116,#6117,#6118,
#6119,#6120,#6121,#6122,#6123,#6124,#6125,#6126,#6127,#6128,#6129,#6130,
#6131,#6132,#6133,#6134,#6135,#6136,#6137,#6138,#6139,#6140,#6141,#6142,
#6143,#6144,#6145,#6146,#6147,#6148,#6149,#6150,#6151,#6152,#6153,#6154,
#6155,#6156,#6157,#6158,#6159,#6160,#6161,#6162,#6163,#6164,#6165,#6166,
#6167,#6168,#6169,#6170,#6171,#6172,#6173,#6174,#6175,#6176,#6177,#6178,
#6179,#6180,#6181,#6182),.UNSPECIFIED.,.F.,.F.,(4,3,3,3,3,3,3,3,3,3,3,3,
3,3,3,3,3,3,3,3,3,3,3,3,3,3,3,3,3,3,3,3,3,3,3,3,3,3,3,3,3,3,3,3,3,3,3,3,
3,3,3,3,3,3,3,3,3,3,3,3,3,3,3,4),(-16.6589123631975,-16.5545511958811,-16.4502386019146,
-16.3459373792314,-16.2415362416229,-16.1370858710382,-16.0324418402438,
-15.9452939796226,-15.8397770700369,-15.7344188085271,-15.6291841820782,
-15.5240153429196,-15.4188761990733,-15.3137307026422,-15.2084733274024,
-15.1031528607634,-14.9976511031841,-14.9487131058961,-14.8431960601416,
-14.7378376610967,-14.6326028957817,-14.5274339170146,-14.4222946330345,
-14.3171489961609,-14.2118914809823,-14.1065708744895,-14.0010689786591,
-13.9521322321697,-13.8466157393099,-13.7412578942319,-13.6360236817895,
-13.5308552548953,-13.4257165209662,-13.3205714314978,-13.2153144560295,
-13.1099943856373,-13.0044930147745,-12.9555513584433,-12.8500342162662,
-12.7446757247134,-12.6394408730378,-12.5342718117637,-12.4291324492194,
-12.3239867378176,-12.2187291546321,-12.1134084837551,-12.0079065297222,
-11.9589704847169,-11.853452654262,-11.7480934645292,-11.642857903596,-11.5376881266249,
-11.432548043081,-11.3274016065084,-11.2221432969163,-11.1168218978765,
-11.0113192206858,-10.9623896109905,-10.8549891203279,-10.7477671220514,
-10.6407197315394,-10.533774763467,-10.4269036873042,-10.3757270560179),
 .UNSPECIFIED.);
#823=B_SPLINE_CURVE_WITH_KNOTS('',3,(#6183,#6184,#6185,#6186,#6187,#6188,
#6189,#6190,#6191,#6192,#6193,#6194,#6195,#6196,#6197,#6198,#6199,#6200,
#6201,#6202,#6203,#6204,#6205,#6206,#6207,#6208,#6209,#6210,#6211,#6212,
#6213,#6214,#6215,#6216,#6217,#6218,#6219,#6220,#6221,#6222,#6223,#6224,
#6225,#6226,#6227,#6228,#6229,#6230,#6231,#6232,#6233,#6234,#6235,#6236,
#6237,#6238,#6239,#6240,#6241,#6242,#6243,#6244,#6245,#6246,#6247,#6248,
#6249,#6250,#6251,#6252,#6253,#6254,#6255,#6256,#6257,#6258,#6259,#6260,
#6261,#6262,#6263,#6264,#6265,#6266,#6267,#6268,#6269,#6270,#6271,#6272,
#6273,#6274,#6275,#6276,#6277,#6278,#6279,#6280,#6281,#6282,#6283,#6284,
#6285,#6286,#6287,#6288,#6289,#6290,#6291,#6292,#6293,#6294,#6295,#6296,
#6297,#6298,#6299,#6300,#6301,#6302,#6303,#6304,#6305,#6306,#6307,#6308,
#6309,#6310,#6311,#6312,#6313,#6314,#6315,#6316,#6317,#6318,#6319,#6320,
#6321,#6322,#6323,#6324,#6325,#6326,#6327,#6328,#6329,#6330,#6331,#6332,
#6333,#6334,#6335,#6336,#6337,#6338,#6339,#6340,#6341,#6342,#6343,#6344,
#6345,#6346,#6347,#6348,#6349,#6350,#6351,#6352,#6353,#6354,#6355,#6356,
#6357,#6358,#6359,#6360,#6361,#6362,#6363,#6364,#6365,#6366,#6367,#6368,
#6369,#6370,#6371,#6372),.UNSPECIFIED.,.F.,.F.,(4,3,3,3,3,3,3,3,3,3,3,3,
3,3,3,3,3,3,3,3,3,3,3,3,3,3,3,3,3,3,3,3,3,3,3,3,3,3,3,3,3,3,3,3,3,3,3,3,
3,3,3,3,3,3,3,3,3,3,3,3,3,3,3,4),(7.39737634520917,7.5045643963064,7.61181522811714,
7.71924509232123,7.82677710957549,7.9345284980795,7.97264698981127,8.07816920580476,
8.18353281643407,8.28877282842226,8.39394707248085,8.49909163221331,8.60424254715742,
8.70950530751085,8.81483114798201,8.92033820552694,8.96922786353769,9.07474698125427,
9.18010750983919,9.28534447958757,9.39051570803975,9.49565728357388,9.60080525053349,
9.70606513833567,9.81138814522103,9.91689245928974,9.96580873726409,10.0713229311904,
10.1766784331034,10.2819102485201,10.3870762463538,10.4922125229135,10.5973551303977,
10.7026096036373,10.8079271565929,10.9134260129313,10.9623896109905,11.0679074212527,
11.1732665931826,11.278502139918,11.3836719049369,11.4888119787845,11.5939584079301,
11.6992167135617,11.8045381106151,11.9100407888698,11.9589704847169,12.0644875831435,
12.1698460407089,12.2750808729382,12.3802499237997,12.4853892849515,12.5905350039773,
12.6957926083051,12.8011133080767,12.9066153025981,12.9555513584433,13.0600577982311,
13.1644187171344,13.2686717663157,13.372878279919,13.4770515526011,13.5812931985024,
13.6805616523888),.UNSPECIFIED.);
#824=B_SPLINE_CURVE_WITH_KNOTS('',3,(#6377,#6378,#6379,#6380,#6381,#6382,
#6383,#6384,#6385,#6386,#6387),.UNSPECIFIED.,.F.,.F.,(4,1,1,1,1,1,1,1,4),
(-22.9420976703771,-22.9213600957074,-21.924779221981,-20.9281983482546,
-19.9316174745282,-18.9350366008018,-17.9384557270754,-16.941874853349,
-16.6589168227746),.UNSPECIFIED.);
#825=B_SPLINE_CURVE_WITH_KNOTS('',3,(#6388,#6389,#6390,#6391,#6392,#6393,
#6394,#6395,#6396,#6397,#6398,#6399,#6400,#6401,#6402,#6403,#6404,#6405,
#6406,#6407,#6408,#6409,#6410,#6411,#6412,#6413,#6414,#6415,#6416,#6417,
#6418,#6419,#6420,#6421,#6422,#6423,#6424,#6425,#6426,#6427,#6428,#6429,
#6430,#6431,#6432,#6433,#6434,#6435,#6436,#6437,#6438,#6439,#6440,#6441,
#6442,#6443,#6444,#6445,#6446,#6447,#6448,#6449,#6450,#6451,#6452,#6453,
#6454,#6455,#6456,#6457,#6458,#6459,#6460,#6461,#6462,#6463,#6464,#6465,
#6466,#6467,#6468,#6469,#6470,#6471,#6472,#6473,#6474,#6475,#6476,#6477,
#6478,#6479,#6480,#6481,#6482,#6483,#6484,#6485,#6486,#6487,#6488,#6489,
#6490,#6491,#6492,#6493,#6494,#6495,#6496,#6497,#6498,#6499,#6500,#6501,
#6502,#6503,#6504,#6505,#6506,#6507,#6508,#6509,#6510,#6511,#6512,#6513,
#6514,#6515,#6516,#6517,#6518,#6519,#6520,#6521,#6522,#6523,#6524,#6525,
#6526,#6527,#6528,#6529,#6530,#6531,#6532,#6533,#6534,#6535,#6536,#6537,
#6538,#6539,#6540,#6541,#6542,#6543,#6544,#6545,#6546,#6547,#6548,#6549,
#6550,#6551,#6552,#6553,#6554,#6555,#6556,#6557,#6558,#6559,#6560,#6561,
#6562,#6563,#6564,#6565,#6566,#6567,#6568,#6569,#6570,#6571,#6572,#6573,
#6574,#6575,#6576,#6577),.UNSPECIFIED.,.F.,.F.,(4,3,3,3,3,3,3,3,3,3,3,3,
3,3,3,3,3,3,3,3,3,3,3,3,3,3,3,3,3,3,3,3,3,3,3,3,3,3,3,3,3,3,3,3,3,3,3,3,
3,3,3,3,3,3,3,3,3,3,3,3,3,3,3,4),(13.6805616528234,13.8163469424965,13.9521322321697,
14.0576492724172,14.1630076667914,14.2682424286896,14.37341140482,14.4785506869449,
14.5836963227472,14.6889538380414,14.7942744453278,14.8997763429845,14.9487131058961,
15.0542300102651,15.1595882677422,15.2648228919211,15.369991729905,15.4751308736699,
15.5802763711125,15.6855337490015,15.790854219229,15.8963559818009,15.9452939796226,
16.0508108200795,16.1561690120437,16.2614035686587,16.3665723378434,16.4717114116778,
16.5768568381605,16.6821141440126,16.7874345414829,16.8929362309439,16.941874853349,
17.0473917665423,17.1527500324105,17.2579846642936,17.3631535095492,17.4682926601413,
17.5734381639533,17.6786955474717,17.7840160229135,17.889517790002,17.9384557270754,
18.043972620432,18.149330866254,18.2545654778811,18.3597343027627,18.4648734328942,
18.5700189161904,18.6752762792507,18.7805967342379,18.8860984810917,18.9350366008018,
19.0405534775837,19.1459117066389,19.251146301295,19.3563151090886,19.4614542220405,
19.5665996880905,19.6718570339203,19.7771774716607,19.8826792014214,19.9316174745282,
19.9637469595683),.UNSPECIFIED.);
#826=B_SPLINE_CURVE_WITH_KNOTS('',3,(#6582,#6583,#6584,#6585,#6586,#6587,
#6588,#6589,#6590,#6591,#6592,#6593,#6594,#6595,#6596,#6597,#6598,#6599,
#6600,#6601,#6602,#6603,#6604,#6605,#6606,#6607,#6608,#6609,#6610,#6611,
#6612,#6613,#6614,#6615,#6616,#6617,#6618,#6619,#6620,#6621,#6622,#6623,
#6624,#6625,#6626,#6627,#6628,#6629,#6630,#6631,#6632,#6633,#6634,#6635,
#6636,#6637,#6638,#6639,#6640,#6641,#6642,#6643,#6644,#6645,#6646,#6647,
#6648,#6649,#6650,#6651,#6652,#6653,#6654,#6655,#6656,#6657,#6658,#6659,
#6660,#6661,#6662,#6663,#6664,#6665,#6666,#6667,#6668,#6669,#6670,#6671,
#6672,#6673,#6674,#6675,#6676,#6677,#6678,#6679,#6680,#6681,#6682,#6683,
#6684,#6685,#6686,#6687,#6688,#6689,#6690,#6691,#6692,#6693,#6694,#6695,
#6696,#6697,#6698,#6699,#6700,#6701,#6702,#6703,#6704,#6705,#6706,#6707,
#6708,#6709,#6710,#6711,#6712,#6713,#6714,#6715,#6716,#6717,#6718,#6719,
#6720,#6721,#6722,#6723,#6724,#6725,#6726,#6727,#6728,#6729,#6730,#6731,
#6732,#6733,#6734,#6735,#6736,#6737,#6738,#6739,#6740,#6741,#6742,#6743,
#6744,#6745,#6746,#6747,#6748,#6749,#6750,#6751,#6752,#6753,#6754,#6755,
#6756,#6757,#6758,#6759,#6760,#6761,#6762,#6763,#6764,#6765,#6766,#6767,
#6768,#6769,#6770,#6771),.UNSPECIFIED.,.F.,.F.,(4,3,3,3,3,3,3,3,3,3,3,3,
3,3,3,3,3,3,3,3,3,3,3,3,3,3,3,3,3,3,3,3,3,3,3,3,3,3,3,3,3,3,3,3,3,3,3,3,
3,3,3,3,3,3,3,3,3,3,3,3,3,3,3,4),(-29.2252829771425,-29.1019668884045,-28.9772671757159,
-28.9008453380659,-28.7953311638247,-28.6899756819199,-28.5847438868928,
-28.4795779096734,-28.3744416539219,-28.269299067409,-28.1640446152449,
-28.0587270834549,-27.953228248201,-27.9042644643395,-27.7987466448287,
-27.6933874635456,-27.5881519073482,-27.4829821328055,-27.3778420493867,
-27.2726956106372,-27.1674372954176,-27.0621158887715,-26.956613201017,
-26.9076835906131,-26.8021664914534,-26.696808033114,-26.5915732000532,
-26.486404148325,-26.3812647862725,-26.2761190663134,-26.1708614610086,
-26.0655407602334,-25.9600387646784,-25.9111027168866,-25.8055861967743,
-25.7002283306547,-25.5949941064194,-25.4898256734777,-25.3846869392369,
-25.2795418551893,-25.1742848937338,-25.0689648422825,-24.9634634977247,
-24.9145218431602,-24.8090048011679,-24.7036464050276,-24.5984116413407,
-24.4932426634085,-24.3881033794714,-24.2829577418493,-24.1777002247363,
-24.0723796156288,-23.966877716167,-23.9179409694338,-23.8127945908852,
-23.7039574758217,-23.5990948008806,-23.494295154551,-23.3895219001087,
-23.2847384419461,-23.1798422596678,-23.074878461885,-22.9697413145948,
-22.9420976703771),.UNSPECIFIED.);
#827=B_SPLINE_CURVE_WITH_KNOTS('',3,(#6772,#6773,#6774,#6775,#6776,#6777,
#6778,#6779,#6780,#6781),.UNSPECIFIED.,.F.,.F.,(4,1,1,1,1,1,1,4),(19.9637512898265,
20.9281983482546,21.924779221981,22.9213600957074,23.9179409694338,24.9145218431602,
25.9111027168866,26.2469251046285),.UNSPECIFIED.);
#828=B_SPLINE_CURVE_WITH_KNOTS('',3,(#6786,#6787,#6788,#6789,#6790,#6791,
#6792,#6793,#6794,#6795,#6796,#6797,#6798,#6799,#6800,#6801,#6802,#6803,
#6804,#6805,#6806,#6807,#6808,#6809,#6810,#6811,#6812,#6813,#6814,#6815,
#6816,#6817,#6818,#6819,#6820,#6821,#6822,#6823,#6824,#6825,#6826,#6827,
#6828,#6829,#6830,#6831,#6832,#6833,#6834,#6835,#6836,#6837,#6838,#6839,
#6840,#6841,#6842,#6843,#6844,#6845,#6846,#6847,#6848,#6849,#6850,#6851,
#6852,#6853,#6854,#6855,#6856,#6857,#6858,#6859,#6860,#6861,#6862,#6863,
#6864,#6865,#6866,#6867,#6868,#6869,#6870,#6871,#6872,#6873,#6874,#6875,
#6876,#6877,#6878,#6879,#6880,#6881,#6882,#6883,#6884,#6885,#6886,#6887,
#6888,#6889,#6890,#6891,#6892,#6893,#6894,#6895,#6896,#6897,#6898,#6899,
#6900,#6901,#6902,#6903,#6904,#6905,#6906,#6907,#6908,#6909,#6910,#6911,
#6912,#6913,#6914,#6915,#6916,#6917,#6918,#6919,#6920,#6921,#6922,#6923,
#6924,#6925,#6926,#6927,#6928,#6929,#6930,#6931,#6932,#6933,#6934,#6935,
#6936,#6937,#6938,#6939,#6940,#6941,#6942,#6943,#6944,#6945,#6946,#6947,
#6948,#6949,#6950,#6951,#6952,#6953,#6954,#6955,#6956,#6957,#6958,#6959,
#6960,#6961,#6962,#6963,#6964,#6965,#6966,#6967,#6968,#6969,#6970,#6971,
#6972,#6973,#6974,#6975),.UNSPECIFIED.,.F.,.F.,(4,3,3,3,3,3,3,3,3,3,3,3,
3,3,3,3,3,3,3,3,3,3,3,3,3,3,3,3,3,3,3,3,3,3,3,3,3,3,3,3,3,3,3,3,3,3,3,3,
3,3,3,3,3,3,3,3,3,3,3,3,3,3,3,4),(-35.5084682847362,-35.4023595064501,-35.2962353664595,
-35.1899767723763,-35.0836517048971,-34.9771072128198,-34.8803305804243,
-34.774950120342,-34.6697303251661,-34.5646364761803,-34.4596097707505,
-34.3546139040873,-34.2496126168141,-34.1444998826447,-34.0393245183892,
-33.9339670573159,-33.8837497066979,-33.7782042662091,-33.6728173464079,
-33.5675540178141,-33.4623564669828,-33.357188646819,-33.2520145543265,
-33.1467289026187,-33.0413803014023,-32.935850924157,-32.8871688329715,
-32.7816310902558,-32.6762515117445,-32.570994956414,-32.4658038211252,
-32.3606420477127,-32.2554736217244,-32.1501930189174,-32.0448491206367,
-31.9393238610627,-31.8905879592451,-31.7850905501634,-31.6797520943826,
-31.5745376278472,-31.4693891567627,-31.3642705581269,-31.2591457532205,
-31.1539091496212,-31.0486095307009,-30.9431285201142,-30.8940070855187,
-30.7884848231671,-30.6831211656924,-30.5778811063686,-30.4727068146982,
-30.367562207151,-30.2624112442611,-30.1571484360919,-30.0518225478098,
-29.9463154429618,-29.8974262117923,-29.7921249664941,-29.6869771514366,
-29.5819461862507,-29.476987732131,-29.3720711679722,-29.2671322858929,
-29.2252829775566),.UNSPECIFIED.);
#829=B_SPLINE_CURVE_WITH_KNOTS('',3,(#6976,#6977,#6978,#6979,#6980,#6981,
#6982,#6983,#6984,#6985,#6986,#6987,#6988,#6989,#6990,#6991,#6992,#6993,
#6994,#6995,#6996,#6997,#6998,#6999,#7000,#7001,#7002,#7003,#7004,#7005,
#7006,#7007,#7008,#7009,#7010,#7011,#7012,#7013,#7014,#7015,#7016,#7017,
#7018,#7019,#7020,#7021,#7022,#7023,#7024,#7025,#7026,#7027,#7028,#7029,
#7030,#7031,#7032,#7033,#7034,#7035,#7036,#7037,#7038,#7039,#7040,#7041,
#7042,#7043,#7044,#7045,#7046,#7047,#7048,#7049,#7050,#7051,#7052,#7053,
#7054,#7055,#7056,#7057,#7058,#7059,#7060,#7061,#7062,#7063,#7064,#7065,
#7066,#7067,#7068,#7069,#7070,#7071,#7072,#7073,#7074,#7075,#7076,#7077,
#7078,#7079,#7080,#7081,#7082,#7083,#7084,#7085,#7086,#7087,#7088,#7089,
#7090,#7091,#7092,#7093,#7094,#7095,#7096,#7097,#7098,#7099,#7100,#7101,
#7102,#7103,#7104,#7105,#7106,#7107,#7108,#7109,#7110,#7111,#7112,#7113,
#7114,#7115,#7116,#7117,#7118,#7119,#7120,#7121,#7122,#7123,#7124,#7125,
#7126,#7127,#7128,#7129,#7130,#7131,#7132,#7133,#7134,#7135,#7136,#7137,
#7138,#7139,#7140,#7141,#7142,#7143,#7144,#7145,#7146,#7147,#7148,#7149,
#7150,#7151,#7152,#7153,#7154,#7155,#7156,#7157,#7158,#7159,#7160,#7161,
#7162,#7163,#7164,#7165),.UNSPECIFIED.,.F.,.F.,(4,3,3,3,3,3,3,3,3,3,3,3,
3,3,3,3,3,3,3,3,3,3,3,3,3,3,3,3,3,3,3,3,3,3,3,3,3,3,3,3,3,3,3,3,3,3,3,3,
3,3,3,3,3,3,3,3,3,3,3,3,3,3,3,4),(26.2469322667479,26.3520739127527,26.457200702523,
26.5623485411171,26.6676237508216,26.7729747238681,26.8785103872483,26.9076835906131,
27.0132014116089,27.118560591826,27.2237961432062,27.328965910607,27.4341059845773,
27.5392524115879,27.6445107117001,27.749832101293,27.855334769187,27.9042644643395,
28.009778477704,28.115133840206,28.2203655774866,28.325531535249,28.4306678097399,
28.5358104531352,28.6410650192125,28.7463826976559,28.8518817282747,28.9008453380659,
29.0063647936613,29.1117255831179,29.2169626990727,29.3221340024984,29.4272755818899,
29.532423481632,29.6376831956915,29.7430059677345,29.8485099556621,29.8974262117923,
30.0029483903628,30.1083119720987,30.2135519678938,30.318726203649,30.4238707629551,
30.5290216853453,30.6342844649434,30.7396103314267,30.8451174250954,30.8940070855187,
30.9995034308467,31.1048410912434,31.2100551614917,31.31520348413,31.4203221815892,
31.5254473322799,31.6306846511216,31.7359851973197,31.8414674509995,31.8905879592451,
31.9966053193322,32.1024616306616,32.2093756164781,32.315013108761,32.4225653413443,
32.5301175739275),.UNSPECIFIED.);
#830=B_SPLINE_CURVE_WITH_KNOTS('',3,(#7168,#7169,#7170,#7171,#7172,#7173,
#7174,#7175,#7176,#7177,#7178,#7179,#7180,#7181,#7182,#7183,#7184,#7185,
#7186,#7187,#7188,#7189,#7190,#7191,#7192,#7193,#7194,#7195,#7196,#7197,
#7198,#7199,#7200,#7201,#7202,#7203,#7204,#7205,#7206,#7207,#7208,#7209,
#7210,#7211,#7212,#7213,#7214,#7215,#7216,#7217,#7218,#7219,#7220,#7221,
#7222,#7223,#7224,#7225,#7226,#7227,#7228,#7229,#7230,#7231,#7232,#7233,
#7234,#7235,#7236,#7237,#7238,#7239,#7240,#7241,#7242,#7243,#7244,#7245,
#7246,#7247,#7248,#7249,#7250,#7251,#7252,#7253,#7254,#7255,#7256,#7257,
#7258,#7259,#7260,#7261,#7262,#7263,#7264,#7265,#7266,#7267,#7268,#7269,
#7270,#7271,#7272,#7273,#7274,#7275,#7276,#7277,#7278,#7279,#7280,#7281,
#7282,#7283,#7284,#7285,#7286,#7287,#7288,#7289,#7290,#7291,#7292,#7293,
#7294),.UNSPECIFIED.,.F.,.F.,(4,3,3,3,3,3,3,3,3,3,3,3,3,3,3,3,3,3,3,3,3,
3,3,3,3,3,3,3,3,3,3,3,3,3,3,3,3,3,3,3,3,3,4),(32.5301175743904,32.6499243852403,
32.7707627025496,32.8871688329715,32.9927129802535,33.0980988488266,33.2033614876022,
33.3085585732964,33.4137261529851,33.5189002298821,33.6241862045267,33.7295353225629,
33.8350655085771,33.8837497066979,33.9891233821121,34.0943380597535,34.1994292723219,
34.3044548813996,34.4094511884809,34.5144544512916,34.6195714611784,34.7247524196896,
34.8301174455497,34.8803305804243,34.9860472709756,35.0916046934767,35.1970366054674,
35.3024014441107,35.4077350088511,35.5130730534988,35.6185188580414,35.7240256643669,
35.8297086352625,35.8769114541507,35.9814256971422,36.085764885428,36.1900065327749,
36.2941881420584,36.3983471341029,36.5025900738691,36.6068728780943,36.7113371001607,
36.8011443739907),.UNSPECIFIED.);
#831=B_SPLINE_CURVE_WITH_KNOTS('',3,(#7297,#7298,#7299,#7300,#7301,#7302,
#7303),.UNSPECIFIED.,.F.,.F.,(4,1,1,1,4),(-38.86665407533,-37.8700732016036,
-36.8734923278771,-35.8769114541507,-35.5084758780373),.UNSPECIFIED.);
#832=B_SPLINE_CURVE_WITH_KNOTS('',3,(#7306,#7307,#7308,#7309,#7310,#7311,
#7312,#7313,#7314,#7315,#7316,#7317,#7318,#7319,#7320,#7321,#7322,#7323,
#7324,#7325,#7326,#7327,#7328,#7329,#7330,#7331,#7332,#7333,#7334,#7335,
#7336,#7337,#7338,#7339,#7340,#7341,#7342),.UNSPECIFIED.,.F.,.F.,(4,3,3,
3,3,3,3,3,3,3,3,3,4),(47.1238898038469,47.2495729833432,47.3762357179408,
47.4923329732614,47.6078590787388,47.7183089200037,47.8286551120703,47.9389421371105,
48.0492143835049,48.1595854549815,48.2700151013785,48.3806268044217,48.4165418170808),
 .UNSPECIFIED.);
#833=B_SPLINE_CURVE_WITH_KNOTS('',3,(#7345,#7346,#7347,#7348,#7349,#7350),
 .UNSPECIFIED.,.F.,.F.,(4,2,4),(9.70317678897598E-6,0.00416850045810854,
0.00832730327464804),.UNSPECIFIED.);
#834=B_SPLINE_CURVE_WITH_KNOTS('',3,(#7519,#7520,#7521,#7522,#7523,#7524,
#7525,#7526,#7527,#7528,#7529,#7530,#7531,#7532,#7533,#7534,#7535,#7536,
#7537,#7538,#7539,#7540,#7541,#7542,#7543,#7544,#7545,#7546,#7547,#7548,
#7549,#7550,#7551,#7552,#7553,#7554,#7555,#7556,#7557,#7558,#7559,#7560,
#7561,#7562,#7563,#7564,#7565,#7566,#7567,#7568,#7569,#7570,#7571,#7572,
#7573,#7574,#7575,#7576,#7577,#7578,#7579,#7580,#7581,#7582,#7583,#7584,
#7585,#7586,#7587,#7588,#7589,#7590,#7591,#7592,#7593,#7594,#7595,#7596,
#7597,#7598,#7599,#7600,#7601,#7602,#7603,#7604,#7605,#7606),
 .UNSPECIFIED.,.F.,.F.,(4,3,3,3,3,3,3,3,3,3,3,3,3,3,3,3,3,3,3,3,3,3,3,3,
3,3,3,3,3,4),(0.,0.0141071418350746,0.0355442788990485,0.0572656760919848,
0.0669720866841882,0.0731473068623763,0.0768712322010848,0.097962135648359,
0.118760026435029,0.139128689171555,0.144047130563164,0.148652874159979,
0.168817015633453,0.188376963157815,0.19974270647635,0.210158636009444,
0.214504663218229,0.217541294053797,0.237154834658274,0.256934379130968,
0.270710750322308,0.279046676847462,0.284344207394495,0.303389528646404,
0.31873922745522,0.324227329017253,0.328196248006345,0.346653672870525,
0.365111097734705,0.366397579005847),.UNSPECIFIED.);
#835=B_SPLINE_CURVE_WITH_KNOTS('',3,(#7607,#7608,#7609,#7610,#7611,#7612,
#7613,#7614,#7615,#7616,#7617,#7618,#7619,#7620,#7621,#7622,#7623,#7624,
#7625,#7626,#7627,#7628,#7629,#7630,#7631,#7632,#7633,#7634,#7635,#7636,
#7637,#7638,#7639,#7640,#7641,#7642,#7643,#7644,#7645,#7646,#7647,#7648,
#7649,#7650,#7651,#7652,#7653,#7654,#7655,#7656,#7657,#7658,#7659,#7660,
#7661,#7662,#7663,#7664,#7665,#7666,#7667,#7668,#7669,#7670,#7671,#7672,
#7673,#7674,#7675,#7676,#7677,#7678,#7679,#7680,#7681,#7682,#7683,#7684,
#7685,#7686,#7687,#7688,#7689,#7690,#7691,#7692,#7693,#7694),
 .UNSPECIFIED.,.F.,.F.,(4,3,3,3,3,3,3,3,3,3,3,3,3,3,3,3,3,3,3,3,3,3,3,3,
3,3,3,3,3,4),(0.,0.0113475426890351,0.0295973948769154,0.0478472470647956,
0.056029692194114,0.0601609064742412,0.0640260637796794,0.0829599659548612,
0.102409502743582,0.12142565969715,0.125492936129605,0.128447152844756,
0.148489790019264,0.168489720575875,0.178766369133891,0.190382802806189,
0.193958991934283,0.213737709639448,0.233952453150079,0.254598727957293,
0.259921705844119,0.263839735837504,0.267527540816782,0.288775631129183,
0.3076511551242,0.313183531178787,0.317664298570661,0.339328410842523,0.360810180213187,
0.364629307890663),.UNSPECIFIED.);
#836=B_SPLINE_CURVE_WITH_KNOTS('',3,(#7863,#7864,#7865,#7866,#7867,#7868,
#7869,#7870,#7871,#7872,#7873,#7874,#7875,#7876,#7877,#7878,#7879,#7880,
#7881,#7882,#7883,#7884,#7885,#7886,#7887,#7888,#7889,#7890,#7891,#7892,
#7893,#7894,#7895,#7896,#7897,#7898,#7899,#7900,#7901,#7902,#7903,#7904,
#7905,#7906,#7907,#7908,#7909,#7910,#7911,#7912,#7913,#7914,#7915,#7916,
#7917,#7918,#7919,#7920,#7921,#7922,#7923,#7924,#7925,#7926,#7927,#7928,
#7929,#7930,#7931,#7932,#7933,#7934,#7935,#7936,#7937,#7938,#7939,#7940,
#7941,#7942,#7943,#7944,#7945,#7946,#7947,#7948,#7949,#7950),
 .UNSPECIFIED.,.F.,.F.,(4,3,3,3,3,3,3,3,3,3,3,3,3,3,3,3,3,3,3,3,3,3,3,3,
3,3,3,3,3,4),(0.,0.0113475426890348,0.0291670043826812,0.0475729265912865,
0.0560296567510774,0.0601608189470318,0.0640260370135678,0.0829599116450913,
0.1024094459103,0.121425612309687,0.125492777420358,0.128446963999971,0.148489595673194,
0.168489527887108,0.178766369133891,0.19038280280619,0.196167693616744,
0.215997966192077,0.236257447265082,0.256915792055175,0.259921709458412,
0.263839753802059,0.267527548188019,0.288775627558559,0.307651148858093,
0.313183536190041,0.317664301193788,0.339328429311912,0.360810221499639,
0.364629307890676),.UNSPECIFIED.);
#837=B_SPLINE_CURVE_WITH_KNOTS('',3,(#7951,#7952,#7953,#7954,#7955,#7956,
#7957,#7958,#7959,#7960,#7961,#7962,#7963,#7964,#7965,#7966,#7967,#7968,
#7969,#7970,#7971,#7972,#7973,#7974,#7975,#7976,#7977,#7978,#7979,#7980,
#7981,#7982,#7983,#7984,#7985,#7986,#7987,#7988,#7989,#7990,#7991,#7992,
#7993,#7994,#7995,#7996,#7997,#7998,#7999,#8000,#8001,#8002,#8003,#8004,
#8005,#8006,#8007,#8008,#8009,#8010,#8011,#8012,#8013,#8014,#8015,#8016,
#8017,#8018,#8019,#8020,#8021,#8022,#8023,#8024,#8025,#8026,#8027,#8028,
#8029,#8030,#8031,#8032,#8033,#8034,#8035),.UNSPECIFIED.,.F.,.F.,(4,3,3,
3,3,3,3,3,3,3,3,3,3,3,3,3,3,3,3,3,3,3,3,3,3,3,3,3,4),(0.,0.0141071418350769,
0.0355831078562044,0.0572869708038222,0.0731472545817825,0.07687123101439,
0.0979621340421377,0.118760002281852,0.139128677516317,0.144047115677256,
0.148652871053239,0.168816990654727,0.1883768924813,0.199742706476349,0.210158636009442,
0.214504668205586,0.217541304162528,0.237140058799154,0.257539855958027,
0.272839703827182,0.279653079547202,0.284485042082695,0.303528865961174,
0.318739247434647,0.32422724443456,0.328196234497253,0.34665369295304,0.365111151408828,
0.366397579005838),.UNSPECIFIED.);
#1021=VERTEX_POINT('',#4049);
#1022=VERTEX_POINT('',#4050);
#1023=VERTEX_POINT('',#4052);
#1024=VERTEX_POINT('',#4201);
#1025=VERTEX_POINT('',#4316);
#1026=VERTEX_POINT('',#4317);
#1027=VERTEX_POINT('',#4340);
#1028=VERTEX_POINT('',#4341);
#1029=VERTEX_POINT('',#4652);
#1030=VERTEX_POINT('',#4653);
#1031=VERTEX_POINT('',#4970);
#1032=VERTEX_POINT('',#4971);
#1033=VERTEX_POINT('',#5318);
#1034=VERTEX_POINT('',#5319);
#1035=VERTEX_POINT('',#5504);
#1036=VERTEX_POINT('',#5505);
#1037=VERTEX_POINT('',#5507);
#1038=VERTEX_POINT('',#5569);
#1039=VERTEX_POINT('',#5606);
#1040=VERTEX_POINT('',#5607);
#1041=VERTEX_POINT('',#5990);
#1042=VERTEX_POINT('',#5991);
#1043=VERTEX_POINT('',#6374);
#1044=VERTEX_POINT('',#6375);
#1045=VERTEX_POINT('',#6579);
#1046=VERTEX_POINT('',#6580);
#1047=VERTEX_POINT('',#6783);
#1048=VERTEX_POINT('',#6784);
#1049=VERTEX_POINT('',#7167);
#1050=VERTEX_POINT('',#7295);
#1051=VERTEX_POINT('',#7305);
#1052=VERTEX_POINT('',#7343);
#1053=VERTEX_POINT('',#8037);
#1054=VERTEX_POINT('',#8038);
#1055=VERTEX_POINT('',#8040);
#1056=VERTEX_POINT('',#8042);
#1057=VERTEX_POINT('',#8044);
#1058=VERTEX_POINT('',#8046);
#1059=VERTEX_POINT('',#8050);
#1060=VERTEX_POINT('',#8052);
#1061=VERTEX_POINT('',#8056);
#1062=VERTEX_POINT('',#8060);
#1063=VERTEX_POINT('',#8064);
#1064=VERTEX_POINT('',#8068);
#1339=EDGE_CURVE('',#1021,#1022,#596,.T.);
#1340=EDGE_CURVE('',#1023,#1021,#806,.T.);
#1341=EDGE_CURVE('',#1024,#1023,#237,.T.);
#1342=EDGE_CURVE('',#1024,#1022,#807,.T.);
#1343=EDGE_CURVE('',#1025,#1026,#597,.T.);
#1344=EDGE_CURVE('',#1021,#1025,#808,.T.);
#1345=EDGE_CURVE('',#1022,#1026,#809,.T.);
#1346=EDGE_CURVE('',#1027,#1028,#598,.T.);
#1347=EDGE_CURVE('',#1025,#1027,#810,.T.);
#1348=EDGE_CURVE('',#1026,#1028,#811,.T.);
#1349=EDGE_CURVE('',#1029,#1030,#599,.T.);
#1350=EDGE_CURVE('',#1027,#1029,#812,.T.);
#1351=EDGE_CURVE('',#1028,#1030,#813,.T.);
#1352=EDGE_CURVE('',#1031,#1032,#600,.T.);
#1353=EDGE_CURVE('',#1029,#1031,#814,.T.);
#1354=EDGE_CURVE('',#1030,#1032,#815,.T.);
#1355=EDGE_CURVE('',#1033,#1034,#601,.T.);
#1356=EDGE_CURVE('',#1031,#1033,#816,.T.);
#1357=EDGE_CURVE('',#1032,#1034,#817,.T.);
#1358=EDGE_CURVE('',#1035,#1036,#602,.T.);
#1359=EDGE_CURVE('',#1035,#1037,#818,.T.);
#1360=EDGE_CURVE('',#1037,#1038,#238,.F.);
#1361=EDGE_CURVE('',#1038,#1036,#819,.T.);
#1362=EDGE_CURVE('',#1039,#1040,#603,.T.);
#1363=EDGE_CURVE('',#1039,#1035,#820,.T.);
#1364=EDGE_CURVE('',#1036,#1040,#821,.T.);
#1365=EDGE_CURVE('',#1041,#1042,#604,.T.);
#1366=EDGE_CURVE('',#1041,#1039,#822,.T.);
#1367=EDGE_CURVE('',#1040,#1042,#823,.T.);
#1368=EDGE_CURVE('',#1043,#1044,#605,.T.);
#1369=EDGE_CURVE('',#1043,#1041,#824,.T.);
#1370=EDGE_CURVE('',#1042,#1044,#825,.T.);
#1371=EDGE_CURVE('',#1045,#1046,#606,.T.);
#1372=EDGE_CURVE('',#1045,#1043,#826,.T.);
#1373=EDGE_CURVE('',#1044,#1046,#827,.T.);
#1374=EDGE_CURVE('',#1047,#1048,#607,.T.);
#1375=EDGE_CURVE('',#1047,#1045,#828,.T.);
#1376=EDGE_CURVE('',#1046,#1048,#829,.T.);
#1377=EDGE_CURVE('',#1048,#1049,#830,.T.);
#1378=EDGE_CURVE('',#1050,#1049,#239,.F.);
#1379=EDGE_CURVE('',#1050,#1047,#831,.T.);
#1380=EDGE_CURVE('',#1034,#1051,#832,.T.);
#1381=EDGE_CURVE('',#1052,#1051,#240,.T.);
#1382=EDGE_CURVE('',#1033,#1052,#833,.T.);
#1383=EDGE_CURVE('',#1049,#1052,#834,.T.);
#1384=EDGE_CURVE('',#1023,#1038,#835,.T.);
#1385=EDGE_CURVE('',#1051,#1050,#836,.T.);
#1386=EDGE_CURVE('',#1037,#1024,#837,.T.);
#1387=EDGE_CURVE('',#1053,#1054,#608,.T.);
#1388=EDGE_CURVE('',#1054,#1055,#609,.T.);
#1389=EDGE_CURVE('',#1055,#1056,#610,.T.);
#1390=EDGE_CURVE('',#1056,#1057,#611,.T.);
#1391=EDGE_CURVE('',#1057,#1058,#612,.T.);
#1392=EDGE_CURVE('',#1058,#1053,#613,.T.);
#1393=EDGE_CURVE('',#1053,#1059,#614,.T.);
#1394=EDGE_CURVE('',#1059,#1060,#615,.T.);
#1395=EDGE_CURVE('',#1054,#1060,#616,.T.);
#1396=EDGE_CURVE('',#1058,#1061,#617,.T.);
#1397=EDGE_CURVE('',#1061,#1059,#618,.T.);
#1398=EDGE_CURVE('',#1057,#1062,#619,.T.);
#1399=EDGE_CURVE('',#1062,#1061,#620,.T.);
#1400=EDGE_CURVE('',#1056,#1063,#621,.T.);
#1401=EDGE_CURVE('',#1063,#1062,#622,.T.);
#1402=EDGE_CURVE('',#1055,#1064,#623,.T.);
#1403=EDGE_CURVE('',#1064,#1063,#624,.T.);
#1404=EDGE_CURVE('',#1060,#1064,#625,.T.);
#1931=ORIENTED_EDGE('',*,*,#1339,.F.);
#1932=ORIENTED_EDGE('',*,*,#1340,.F.);
#1933=ORIENTED_EDGE('',*,*,#1341,.F.);
#1934=ORIENTED_EDGE('',*,*,#1342,.T.);
#1935=ORIENTED_EDGE('',*,*,#1343,.F.);
#1936=ORIENTED_EDGE('',*,*,#1344,.F.);
#1937=ORIENTED_EDGE('',*,*,#1339,.T.);
#1938=ORIENTED_EDGE('',*,*,#1345,.T.);
#1939=ORIENTED_EDGE('',*,*,#1346,.F.);
#1940=ORIENTED_EDGE('',*,*,#1347,.F.);
#1941=ORIENTED_EDGE('',*,*,#1343,.T.);
#1942=ORIENTED_EDGE('',*,*,#1348,.T.);
#1943=ORIENTED_EDGE('',*,*,#1349,.F.);
#1944=ORIENTED_EDGE('',*,*,#1350,.F.);
#1945=ORIENTED_EDGE('',*,*,#1346,.T.);
#1946=ORIENTED_EDGE('',*,*,#1351,.T.);
#1947=ORIENTED_EDGE('',*,*,#1352,.F.);
#1948=ORIENTED_EDGE('',*,*,#1353,.F.);
#1949=ORIENTED_EDGE('',*,*,#1349,.T.);
#1950=ORIENTED_EDGE('',*,*,#1354,.T.);
#1951=ORIENTED_EDGE('',*,*,#1355,.F.);
#1952=ORIENTED_EDGE('',*,*,#1356,.F.);
#1953=ORIENTED_EDGE('',*,*,#1352,.T.);
#1954=ORIENTED_EDGE('',*,*,#1357,.T.);
#1955=ORIENTED_EDGE('',*,*,#1358,.F.);
#1956=ORIENTED_EDGE('',*,*,#1359,.T.);
#1957=ORIENTED_EDGE('',*,*,#1360,.T.);
#1958=ORIENTED_EDGE('',*,*,#1361,.T.);
#1959=ORIENTED_EDGE('',*,*,#1362,.F.);
#1960=ORIENTED_EDGE('',*,*,#1363,.T.);
#1961=ORIENTED_EDGE('',*,*,#1358,.T.);
#1962=ORIENTED_EDGE('',*,*,#1364,.T.);
#1963=ORIENTED_EDGE('',*,*,#1365,.F.);
#1964=ORIENTED_EDGE('',*,*,#1366,.T.);
#1965=ORIENTED_EDGE('',*,*,#1362,.T.);
#1966=ORIENTED_EDGE('',*,*,#1367,.T.);
#1967=ORIENTED_EDGE('',*,*,#1368,.F.);
#1968=ORIENTED_EDGE('',*,*,#1369,.T.);
#1969=ORIENTED_EDGE('',*,*,#1365,.T.);
#1970=ORIENTED_EDGE('',*,*,#1370,.T.);
#1971=ORIENTED_EDGE('',*,*,#1371,.F.);
#1972=ORIENTED_EDGE('',*,*,#1372,.T.);
#1973=ORIENTED_EDGE('',*,*,#1368,.T.);
#1974=ORIENTED_EDGE('',*,*,#1373,.T.);
#1975=ORIENTED_EDGE('',*,*,#1374,.F.);
#1976=ORIENTED_EDGE('',*,*,#1375,.T.);
#1977=ORIENTED_EDGE('',*,*,#1371,.T.);
#1978=ORIENTED_EDGE('',*,*,#1376,.T.);
#1979=ORIENTED_EDGE('',*,*,#1374,.T.);
#1980=ORIENTED_EDGE('',*,*,#1377,.T.);
#1981=ORIENTED_EDGE('',*,*,#1378,.F.);
#1982=ORIENTED_EDGE('',*,*,#1379,.T.);
#1983=ORIENTED_EDGE('',*,*,#1355,.T.);
#1984=ORIENTED_EDGE('',*,*,#1380,.T.);
#1985=ORIENTED_EDGE('',*,*,#1381,.F.);
#1986=ORIENTED_EDGE('',*,*,#1382,.F.);
#1987=ORIENTED_EDGE('',*,*,#1383,.F.);
#1988=ORIENTED_EDGE('',*,*,#1377,.F.);
#1989=ORIENTED_EDGE('',*,*,#1376,.F.);
#1990=ORIENTED_EDGE('',*,*,#1373,.F.);
#1991=ORIENTED_EDGE('',*,*,#1370,.F.);
#1992=ORIENTED_EDGE('',*,*,#1367,.F.);
#1993=ORIENTED_EDGE('',*,*,#1364,.F.);
#1994=ORIENTED_EDGE('',*,*,#1361,.F.);
#1995=ORIENTED_EDGE('',*,*,#1384,.F.);
#1996=ORIENTED_EDGE('',*,*,#1340,.T.);
#1997=ORIENTED_EDGE('',*,*,#1344,.T.);
#1998=ORIENTED_EDGE('',*,*,#1347,.T.);
#1999=ORIENTED_EDGE('',*,*,#1350,.T.);
#2000=ORIENTED_EDGE('',*,*,#1353,.T.);
#2001=ORIENTED_EDGE('',*,*,#1356,.T.);
#2002=ORIENTED_EDGE('',*,*,#1382,.T.);
#2003=ORIENTED_EDGE('',*,*,#1385,.F.);
#2004=ORIENTED_EDGE('',*,*,#1380,.F.);
#2005=ORIENTED_EDGE('',*,*,#1357,.F.);
#2006=ORIENTED_EDGE('',*,*,#1354,.F.);
#2007=ORIENTED_EDGE('',*,*,#1351,.F.);
#2008=ORIENTED_EDGE('',*,*,#1348,.F.);
#2009=ORIENTED_EDGE('',*,*,#1345,.F.);
#2010=ORIENTED_EDGE('',*,*,#1342,.F.);
#2011=ORIENTED_EDGE('',*,*,#1386,.F.);
#2012=ORIENTED_EDGE('',*,*,#1359,.F.);
#2013=ORIENTED_EDGE('',*,*,#1363,.F.);
#2014=ORIENTED_EDGE('',*,*,#1366,.F.);
#2015=ORIENTED_EDGE('',*,*,#1369,.F.);
#2016=ORIENTED_EDGE('',*,*,#1372,.F.);
#2017=ORIENTED_EDGE('',*,*,#1375,.F.);
#2018=ORIENTED_EDGE('',*,*,#1379,.F.);
#2019=ORIENTED_EDGE('',*,*,#1383,.T.);
#2020=ORIENTED_EDGE('',*,*,#1381,.T.);
#2021=ORIENTED_EDGE('',*,*,#1385,.T.);
#2022=ORIENTED_EDGE('',*,*,#1378,.T.);
#2023=ORIENTED_EDGE('',*,*,#1387,.T.);
#2024=ORIENTED_EDGE('',*,*,#1388,.T.);
#2025=ORIENTED_EDGE('',*,*,#1389,.T.);
#2026=ORIENTED_EDGE('',*,*,#1390,.T.);
#2027=ORIENTED_EDGE('',*,*,#1391,.T.);
#2028=ORIENTED_EDGE('',*,*,#1392,.T.);
#2029=ORIENTED_EDGE('',*,*,#1387,.F.);
#2030=ORIENTED_EDGE('',*,*,#1393,.T.);
#2031=ORIENTED_EDGE('',*,*,#1394,.T.);
#2032=ORIENTED_EDGE('',*,*,#1395,.F.);
#2033=ORIENTED_EDGE('',*,*,#1392,.F.);
#2034=ORIENTED_EDGE('',*,*,#1396,.T.);
#2035=ORIENTED_EDGE('',*,*,#1397,.T.);
#2036=ORIENTED_EDGE('',*,*,#1393,.F.);
#2037=ORIENTED_EDGE('',*,*,#1391,.F.);
#2038=ORIENTED_EDGE('',*,*,#1398,.T.);
#2039=ORIENTED_EDGE('',*,*,#1399,.T.);
#2040=ORIENTED_EDGE('',*,*,#1396,.F.);
#2041=ORIENTED_EDGE('',*,*,#1390,.F.);
#2042=ORIENTED_EDGE('',*,*,#1400,.T.);
#2043=ORIENTED_EDGE('',*,*,#1401,.T.);
#2044=ORIENTED_EDGE('',*,*,#1398,.F.);
#2045=ORIENTED_EDGE('',*,*,#1389,.F.);
#2046=ORIENTED_EDGE('',*,*,#1402,.T.);
#2047=ORIENTED_EDGE('',*,*,#1403,.T.);
#2048=ORIENTED_EDGE('',*,*,#1400,.F.);
#2049=ORIENTED_EDGE('',*,*,#1388,.F.);
#2050=ORIENTED_EDGE('',*,*,#1395,.T.);
#2051=ORIENTED_EDGE('',*,*,#1404,.T.);
#2052=ORIENTED_EDGE('',*,*,#1402,.F.);
#2053=ORIENTED_EDGE('',*,*,#1404,.F.);
#2054=ORIENTED_EDGE('',*,*,#1394,.F.);
#2055=ORIENTED_EDGE('',*,*,#1397,.F.);
#2056=ORIENTED_EDGE('',*,*,#1399,.F.);
#2057=ORIENTED_EDGE('',*,*,#1401,.F.);
#2058=ORIENTED_EDGE('',*,*,#1403,.F.);
#2059=ORIENTED_EDGE('',*,*,#1384,.T.);
#2060=ORIENTED_EDGE('',*,*,#1360,.F.);
#2061=ORIENTED_EDGE('',*,*,#1386,.T.);
#2062=ORIENTED_EDGE('',*,*,#1341,.T.);
#2246=CYLINDRICAL_SURFACE('',#2668,1.5555);
#2247=CYLINDRICAL_SURFACE('',#2670,1.5555);
#2248=CYLINDRICAL_SURFACE('',#2671,1.5555);
#2249=CYLINDRICAL_SURFACE('',#2672,1.5555);
#2250=CYLINDRICAL_SURFACE('',#2673,1.5555);
#2251=CYLINDRICAL_SURFACE('',#2674,1.5555);
#2252=CYLINDRICAL_SURFACE('',#2675,1.954);
#2253=CYLINDRICAL_SURFACE('',#2677,1.954);
#2254=CYLINDRICAL_SURFACE('',#2678,1.954);
#2255=CYLINDRICAL_SURFACE('',#2679,1.954);
#2256=CYLINDRICAL_SURFACE('',#2680,1.954);
#2257=CYLINDRICAL_SURFACE('',#2681,1.954);
#2258=CYLINDRICAL_SURFACE('',#2682,1.954);
#2259=CYLINDRICAL_SURFACE('',#2684,1.5555);
#2356=ADVANCED_FACE('',(#327),#2246,.T.);
#2357=ADVANCED_FACE('',(#328),#2247,.T.);
#2358=ADVANCED_FACE('',(#329),#2248,.T.);
#2359=ADVANCED_FACE('',(#330),#2249,.T.);
#2360=ADVANCED_FACE('',(#331),#2250,.T.);
#2361=ADVANCED_FACE('',(#332),#2251,.T.);
#2362=ADVANCED_FACE('',(#333),#2252,.T.);
#2363=ADVANCED_FACE('',(#334),#2253,.T.);
#2364=ADVANCED_FACE('',(#335),#2254,.T.);
#2365=ADVANCED_FACE('',(#336),#2255,.T.);
#2366=ADVANCED_FACE('',(#337),#2256,.T.);
#2367=ADVANCED_FACE('',(#338),#2257,.T.);
#2368=ADVANCED_FACE('',(#339),#2258,.T.);
#2369=ADVANCED_FACE('',(#340),#2259,.T.);
#2370=ADVANCED_FACE('',(#341),#23,.F.);
#2371=ADVANCED_FACE('',(#342),#24,.F.);
#2372=ADVANCED_FACE('',(#343,#56),#79,.T.);
#2373=ADVANCED_FACE('',(#344),#80,.F.);
#2374=ADVANCED_FACE('',(#345),#81,.F.);
#2375=ADVANCED_FACE('',(#346),#82,.F.);
#2376=ADVANCED_FACE('',(#347),#83,.F.);
#2377=ADVANCED_FACE('',(#348),#84,.F.);
#2378=ADVANCED_FACE('',(#349),#85,.F.);
#2379=ADVANCED_FACE('',(#350),#86,.F.);
#2380=ADVANCED_FACE('',(#351),#87,.F.);
#2407=CLOSED_SHELL('',(#2356,#2357,#2358,#2359,#2360,#2361,#2362,#2363,
#2364,#2365,#2366,#2367,#2368,#2369,#2370,#2371,#2372,#2373,#2374,#2375,
#2376,#2377,#2378,#2379,#2380));
#2667=AXIS2_PLACEMENT_3D('',#4047,#3252,#3253);
#2668=AXIS2_PLACEMENT_3D('',#4048,#3254,#3255);
#2669=AXIS2_PLACEMENT_3D('',#4202,#3257,#3258);
#2670=AXIS2_PLACEMENT_3D('',#4315,#3259,#3260);
#2671=AXIS2_PLACEMENT_3D('',#4339,#3262,#3263);
#2672=AXIS2_PLACEMENT_3D('',#4651,#3265,#3266);
#2673=AXIS2_PLACEMENT_3D('',#4969,#3268,#3269);
#2674=AXIS2_PLACEMENT_3D('',#5317,#3271,#3272);
#2675=AXIS2_PLACEMENT_3D('',#5503,#3274,#3275);
#2676=AXIS2_PLACEMENT_3D('',#5570,#3277,#3278);
#2677=AXIS2_PLACEMENT_3D('',#5605,#3279,#3280);
#2678=AXIS2_PLACEMENT_3D('',#5989,#3282,#3283);
#2679=AXIS2_PLACEMENT_3D('',#6373,#3285,#3286);
#2680=AXIS2_PLACEMENT_3D('',#6578,#3288,#3289);
#2681=AXIS2_PLACEMENT_3D('',#6782,#3291,#3292);
#2682=AXIS2_PLACEMENT_3D('',#7166,#3294,#3295);
#2683=AXIS2_PLACEMENT_3D('',#7296,#3296,#3297);
#2684=AXIS2_PLACEMENT_3D('',#7304,#3298,#3299);
#2685=AXIS2_PLACEMENT_3D('',#7344,#3300,#3301);
#2686=AXIS2_PLACEMENT_3D('',#8036,#3302,#3303);
#2687=AXIS2_PLACEMENT_3D('',#8049,#3310,#3311);
#2688=AXIS2_PLACEMENT_3D('',#8055,#3315,#3316);
#2689=AXIS2_PLACEMENT_3D('',#8059,#3319,#3320);
#2690=AXIS2_PLACEMENT_3D('',#8063,#3323,#3324);
#2691=AXIS2_PLACEMENT_3D('',#8067,#3327,#3328);
#2692=AXIS2_PLACEMENT_3D('',#8071,#3331,#3332);
#2693=AXIS2_PLACEMENT_3D('',#8073,#3334,#3335);
#2694=AXIS2_PLACEMENT_3D('',#8074,#3336,#3337);
#3252=DIRECTION('axis',(0.,0.,1.));
#3253=DIRECTION('refdir',(1.,0.,0.));
#3254=DIRECTION('center_axis',(1.,0.,0.));
#3255=DIRECTION('ref_axis',(0.,1.,4.63931189975154E-15));
#3256=DIRECTION('',(-1.,0.,0.));
#3257=DIRECTION('center_axis',(-1.,0.,0.));
#3258=DIRECTION('ref_axis',(0.,1.,4.63931189975154E-15));
#3259=DIRECTION('center_axis',(1.,0.,0.));
#3260=DIRECTION('ref_axis',(0.,1.,4.63931189975154E-15));
#3261=DIRECTION('',(-1.,0.,0.));
#3262=DIRECTION('center_axis',(1.,0.,0.));
#3263=DIRECTION('ref_axis',(0.,1.,4.63931189975154E-15));
#3264=DIRECTION('',(-1.,0.,0.));
#3265=DIRECTION('center_axis',(1.,0.,0.));
#3266=DIRECTION('ref_axis',(0.,1.,4.63931189975154E-15));
#3267=DIRECTION('',(-1.,0.,0.));
#3268=DIRECTION('center_axis',(1.,0.,0.));
#3269=DIRECTION('ref_axis',(0.,1.,4.63931189975154E-15));
#3270=DIRECTION('',(-1.,0.,0.));
#3271=DIRECTION('center_axis',(1.,0.,0.));
#3272=DIRECTION('ref_axis',(0.,1.,4.63931189975154E-15));
#3273=DIRECTION('',(-1.,0.,0.));
#3274=DIRECTION('center_axis',(1.,0.,0.));
#3275=DIRECTION('ref_axis',(0.,1.,0.));
#3276=DIRECTION('',(-1.,0.,0.));
#3277=DIRECTION('center_axis',(-1.,0.,0.));
#3278=DIRECTION('ref_axis',(0.,1.,0.));
#3279=DIRECTION('center_axis',(1.,0.,0.));
#3280=DIRECTION('ref_axis',(0.,1.,0.));
#3281=DIRECTION('',(-1.,0.,0.));
#3282=DIRECTION('center_axis',(1.,0.,0.));
#3283=DIRECTION('ref_axis',(0.,1.,0.));
#3284=DIRECTION('',(-1.,0.,0.));
#3285=DIRECTION('center_axis',(1.,0.,0.));
#3286=DIRECTION('ref_axis',(0.,1.,0.));
#3287=DIRECTION('',(-1.,0.,0.));
#3288=DIRECTION('center_axis',(1.,0.,0.));
#3289=DIRECTION('ref_axis',(0.,1.,0.));
#3290=DIRECTION('',(-1.,0.,0.));
#3291=DIRECTION('center_axis',(1.,0.,0.));
#3292=DIRECTION('ref_axis',(0.,1.,0.));
#3293=DIRECTION('',(-1.,0.,0.));
#3294=DIRECTION('center_axis',(1.,0.,0.));
#3295=DIRECTION('ref_axis',(0.,1.,0.));
#3296=DIRECTION('center_axis',(-1.,0.,0.));
#3297=DIRECTION('ref_axis',(0.,1.,0.));
#3298=DIRECTION('center_axis',(1.,0.,0.));
#3299=DIRECTION('ref_axis',(0.,1.,4.63931189975154E-15));
#3300=DIRECTION('center_axis',(1.,0.,0.));
#3301=DIRECTION('ref_axis',(0.,1.,4.63931189975154E-15));
#3302=DIRECTION('center_axis',(1.,0.,0.));
#3303=DIRECTION('ref_axis',(0.,1.,0.));
#3304=DIRECTION('',(0.,0.5,0.866025403784439));
#3305=DIRECTION('',(0.,1.,0.));
#3306=DIRECTION('',(0.,0.499999999999999,-0.866025403784439));
#3307=DIRECTION('',(0.,-0.5,-0.866025403784438));
#3308=DIRECTION('',(0.,-1.,4.80740671595891E-16));
#3309=DIRECTION('',(0.,-0.499999999999999,0.866025403784439));
#3310=DIRECTION('center_axis',(0.,-0.866025403784439,0.5));
#3311=DIRECTION('ref_axis',(0.,0.5,0.866025403784439));
#3312=DIRECTION('',(-1.,0.,0.));
#3313=DIRECTION('',(0.,0.5,0.866025403784439));
#3314=DIRECTION('',(-1.,0.,0.));
#3315=DIRECTION('center_axis',(0.,-0.866025403784439,-0.499999999999999));
#3316=DIRECTION('ref_axis',(0.,-0.499999999999999,0.866025403784439));
#3317=DIRECTION('',(-1.,0.,0.));
#3318=DIRECTION('',(0.,-0.499999999999999,0.866025403784439));
#3319=DIRECTION('center_axis',(0.,-4.80740671595891E-16,-1.));
#3320=DIRECTION('ref_axis',(0.,-1.,4.80740671595891E-16));
#3321=DIRECTION('',(-1.,0.,0.));
#3322=DIRECTION('',(0.,-1.,4.80740671595891E-16));
#3323=DIRECTION('center_axis',(0.,0.866025403784438,-0.5));
#3324=DIRECTION('ref_axis',(0.,-0.5,-0.866025403784438));
#3325=DIRECTION('',(-1.,0.,0.));
#3326=DIRECTION('',(0.,-0.5,-0.866025403784438));
#3327=DIRECTION('center_axis',(0.,0.866025403784439,0.499999999999999));
#3328=DIRECTION('ref_axis',(0.,0.499999999999999,-0.866025403784439));
#3329=DIRECTION('',(-1.,0.,0.));
#3330=DIRECTION('',(0.,0.499999999999999,-0.866025403784439));
#3331=DIRECTION('center_axis',(0.,0.,1.));
#3332=DIRECTION('ref_axis',(0.,1.,0.));
#3333=DIRECTION('',(0.,1.,0.));
#3334=DIRECTION('center_axis',(-1.,0.,0.));
#3335=DIRECTION('ref_axis',(0.,0.,1.));
#3336=DIRECTION('center_axis',(1.,0.,0.));
#3337=DIRECTION('ref_axis',(0.,1.,0.));
#4047=CARTESIAN_POINT('',(0.,0.,0.));
#4048=CARTESIAN_POINT('Origin',(1.2059437743963,0.,3.64739446828387));
#4049=CARTESIAN_POINT('',(3.0940562256037,-1.55537930835193,3.64803845831604));
#4050=CARTESIAN_POINT('',(2.95594377439629,-1.55549966270667,3.64841883122548));
#4051=CARTESIAN_POINT('',(1.2059437743963,-1.5555,3.64739446828386));
#4052=CARTESIAN_POINT('',(2.50004392260581,-0.903577229903434,2.38124738377906));
#4053=CARTESIAN_POINT('Ctrl Pts',(2.50004392260581,-0.903577229903434,2.38124738377906));
#4054=CARTESIAN_POINT('Ctrl Pts',(2.50433411497395,-0.855085523975061,2.34664160862681));
#4055=CARTESIAN_POINT('Ctrl Pts',(2.50862430734209,-0.804491254712249,2.31474615079293));
#4056=CARTESIAN_POINT('Ctrl Pts',(2.51291449971023,-0.752136324784237,2.28582508006303));
#4057=CARTESIAN_POINT('Ctrl Pts',(2.51701568125145,-0.702087969422061,2.25817817026229));
#4058=CARTESIAN_POINT('Ctrl Pts',(2.52111686279267,-0.650431357336844,2.2332493669833));
#4059=CARTESIAN_POINT('Ctrl Pts',(2.5252180443339,-0.59749677222433,2.21122670051386));
#4060=CARTESIAN_POINT('Ctrl Pts',(2.52931555826907,-0.544609525470972,2.18922372848223));
#4061=CARTESIAN_POINT('Ctrl Pts',(2.53341307220424,-0.490447057473864,2.17012195018667));
#4062=CARTESIAN_POINT('Ctrl Pts',(2.53751058613941,-0.435362908197946,2.15406282790206));
#4063=CARTESIAN_POINT('Ctrl Pts',(2.5416060839302,-0.380305862575501,2.13801160736216));
#4064=CARTESIAN_POINT('Ctrl Pts',(2.54570158172099,-0.324328543987199,2.12500022449484));
#4065=CARTESIAN_POINT('Ctrl Pts',(2.54979707951179,-0.267800829156953,2.11512067881188));
#4066=CARTESIAN_POINT('Ctrl Pts',(2.55389220938536,-0.211278192468817,2.10524202065351));
#4067=CARTESIAN_POINT('Ctrl Pts',(2.55798733925893,-0.15420578155813,2.09849473034022));
#4068=CARTESIAN_POINT('Ctrl Pts',(2.5620824691325,-0.0969625372344377,2.09491950347025));
#4069=CARTESIAN_POINT('Ctrl Pts',(2.56618153629185,-0.0396642560697558,
2.09134083917818));
#4070=CARTESIAN_POINT('Ctrl Pts',(2.5702806034512,0.0178046547621242,2.09094035559528));
#4071=CARTESIAN_POINT('Ctrl Pts',(2.57437967061055,0.0750629135762425,2.09370665890727));
#4072=CARTESIAN_POINT('Ctrl Pts',(2.578481068547,0.132353730100148,2.09647453517141));
#4073=CARTESIAN_POINT('Ctrl Pts',(2.58258246648346,0.189433127822244,2.10241272382605));
#4074=CARTESIAN_POINT('Ctrl Pts',(2.58668386441992,0.245925895792555,2.11145804258825));
#4075=CARTESIAN_POINT('Ctrl Pts',(2.59079224810531,0.302514885660727,2.12051876788424));
#4076=CARTESIAN_POINT('Ctrl Pts',(2.59490063179069,0.358514735044393,2.13269706306549));
#4077=CARTESIAN_POINT('Ctrl Pts',(2.59900901547608,0.413562868294999,2.14787921195347));
#4078=CARTESIAN_POINT('Ctrl Pts',(2.60034219013111,0.431426043128821,2.15280583460032));
#4079=CARTESIAN_POINT('Ctrl Pts',(2.60167536478614,0.449189147593446,2.15804838267406));
#4080=CARTESIAN_POINT('Ctrl Pts',(2.60300853944117,0.466840256073619,2.16360188665087));
#4081=CARTESIAN_POINT('Ctrl Pts',(2.60716403457439,0.521858625278663,2.18091211578018));
#4082=CARTESIAN_POINT('Ctrl Pts',(2.61131952970761,0.576023644694694,2.20132138484262));
#4083=CARTESIAN_POINT('Ctrl Pts',(2.61547502484083,0.628963033455763,2.22472593607191));
#4084=CARTESIAN_POINT('Ctrl Pts',(2.61962338251369,0.681811493752981,2.24809028774582));
#4085=CARTESIAN_POINT('Ctrl Pts',(2.62377174018654,0.733438031573039,2.27443950101456));
#4086=CARTESIAN_POINT('Ctrl Pts',(2.6279200978594,0.7834870450404,2.30362056607641));
#4087=CARTESIAN_POINT('Ctrl Pts',(2.63206447609135,0.833488047437554,2.33277363829552));
#4088=CARTESIAN_POINT('Ctrl Pts',(2.6362088543233,0.881914078343766,2.36475291915531));
#4089=CARTESIAN_POINT('Ctrl Pts',(2.64035323255525,0.928432591928899,2.39935874273584));
#4090=CARTESIAN_POINT('Ctrl Pts',(2.64449521160968,0.974924175980639,2.4339445330305));
#4091=CARTESIAN_POINT('Ctrl Pts',(2.64863719066411,1.01951001672808,2.47115354250065));
#4092=CARTESIAN_POINT('Ctrl Pts',(2.65277916971854,1.06188696852165,2.5107431074507));
#4093=CARTESIAN_POINT('Ctrl Pts',(2.65692032641849,1.10425550673423,2.55032481223155));
#4094=CARTESIAN_POINT('Ctrl Pts',(2.66106148311844,1.14441564814524,2.59228577999221));
#4095=CARTESIAN_POINT('Ctrl Pts',(2.66520263981839,1.18209939933818,2.63634488488832));
#4096=CARTESIAN_POINT('Ctrl Pts',(2.66934763312091,1.21981806289667,2.68044480863942));
#4097=CARTESIAN_POINT('Ctrl Pts',(2.67349262642342,1.25505541323187,2.72664635923879));
#4098=CARTESIAN_POINT('Ctrl Pts',(2.67763761972594,1.28758315415597,2.77463455219367));
#4099=CARTESIAN_POINT('Ctrl Pts',(2.68178439590806,1.32012488618732,2.82264338623629));
#4100=CARTESIAN_POINT('Ctrl Pts',(2.68593117209018,1.34995441737378,2.87243994937993));
#4101=CARTESIAN_POINT('Ctrl Pts',(2.69007794827229,1.37688806469823,2.92368215852843));
#4102=CARTESIAN_POINT('Ctrl Pts',(2.69423278474608,1.4038740642702,2.97502396966489));
#4103=CARTESIAN_POINT('Ctrl Pts',(2.69838762121987,1.42795271460861,3.02781656903579));
#4104=CARTESIAN_POINT('Ctrl Pts',(2.70254245769365,1.4489877876146,3.08169610224084));
#4105=CARTESIAN_POINT('Ctrl Pts',(2.70637366513319,1.46838439412368,3.1313788442106));
#4106=CARTESIAN_POINT('Ctrl Pts',(2.71020487257272,1.48519355951164,3.1819852701583));
#4107=CARTESIAN_POINT('Ctrl Pts',(2.71403608001225,1.49934664266485,3.23322071835562));
#4108=CARTESIAN_POINT('Ctrl Pts',(2.71817915439409,1.51465181137774,3.28862682105782));
#4109=CARTESIAN_POINT('Ctrl Pts',(2.72232222877592,1.52691450781882,3.34500138694104));
#4110=CARTESIAN_POINT('Ctrl Pts',(2.72646530315776,1.5360179517072,3.40197828700556));
#4111=CARTESIAN_POINT('Ctrl Pts',(2.73060090241158,1.54510497073757,3.45885238668985));
#4112=CARTESIAN_POINT('Ctrl Pts',(2.73473650166541,1.55104396849635,3.51632615235848));
#4113=CARTESIAN_POINT('Ctrl Pts',(2.73887210091923,1.55376848069945,3.57402036941437));
#4114=CARTESIAN_POINT('Ctrl Pts',(2.74300352433428,1.55649024188075,3.63165633088643));
#4115=CARTESIAN_POINT('Ctrl Pts',(2.74713494774932,1.55600392310557,3.68951178383782));
#4116=CARTESIAN_POINT('Ctrl Pts',(2.75126637116436,1.55229470988028,3.74720119990902));
#4117=CARTESIAN_POINT('Ctrl Pts',(2.75539522175441,1.54858780655053,3.80485469016076));
#4118=CARTESIAN_POINT('Ctrl Pts',(2.75952407234446,1.54166202030053,3.86234182841597));
#4119=CARTESIAN_POINT('Ctrl Pts',(2.76365292293451,1.53155460991275,3.91927813247688));
#4120=CARTESIAN_POINT('Ctrl Pts',(2.76778080002723,1.52144958264269,3.97620101213823));
#4121=CARTESIAN_POINT('Ctrl Pts',(2.77190867711994,1.50816451151997,4.032572801459));
#4122=CARTESIAN_POINT('Ctrl Pts',(2.77603655421266,1.49178807918711,4.08801741003251));
#4123=CARTESIAN_POINT('Ctrl Pts',(2.78016813677092,1.47539694624562,4.14351178948868));
#4124=CARTESIAN_POINT('Ctrl Pts',(2.78429971932918,1.45590905346099,4.19807682245723));
#4125=CARTESIAN_POINT('Ctrl Pts',(2.78843130188743,1.4334631269432,4.25135118336718));
#4126=CARTESIAN_POINT('Ctrl Pts',(2.79256457361284,1.41100802357336,4.30464732510794));
#4127=CARTESIAN_POINT('Ctrl Pts',(2.79669784533826,1.38559270429132,4.35665127207839));
#4128=CARTESIAN_POINT('Ctrl Pts',(2.80083111706367,1.35740294273005,4.40702431305553));
#4129=CARTESIAN_POINT('Ctrl Pts',(2.80497246662991,1.32915808863627,4.45749580035655));
#4130=CARTESIAN_POINT('Ctrl Pts',(2.80911381619615,1.29812823699445,4.50632956924818));
#4131=CARTESIAN_POINT('Ctrl Pts',(2.81325516576239,1.26454328228959,4.55321483525311));
#4132=CARTESIAN_POINT('Ctrl Pts',(2.81719131736937,1.23262241414807,4.59777700325587));
#4133=CARTESIAN_POINT('Ctrl Pts',(2.82112746897635,1.19839396464653,4.64057893014162));
#4134=CARTESIAN_POINT('Ctrl Pts',(2.82506362058333,1.16208710892346,4.68138373383449));
#4135=CARTESIAN_POINT('Ctrl Pts',(2.82921315257594,1.12381204372855,4.72440058259503));
#4136=CARTESIAN_POINT('Ctrl Pts',(2.83336268456856,1.08306535950521,4.7653790955833));
#4137=CARTESIAN_POINT('Ctrl Pts',(2.83751221656118,1.04009256905409,4.80402219482273));
#4138=CARTESIAN_POINT('Ctrl Pts',(2.84165438986481,0.997195985606616,4.84259676523792));
#4139=CARTESIAN_POINT('Ctrl Pts',(2.84579656316844,0.952081515568067,4.87884379743944));
#4140=CARTESIAN_POINT('Ctrl Pts',(2.84993873647208,0.905032885213859,4.91250147035187));
#4141=CARTESIAN_POINT('Ctrl Pts',(2.85407680034561,0.858030931578244,4.94612575164981));
#4142=CARTESIAN_POINT('Ctrl Pts',(2.85821486421914,0.809099040695546,4.97716546230242));
#4143=CARTESIAN_POINT('Ctrl Pts',(2.86235292809268,0.758554187283901,5.00539881104352));
#4144=CARTESIAN_POINT('Ctrl Pts',(2.86648847416359,0.708040087859669,5.03361498121957));
#4145=CARTESIAN_POINT('Ctrl Pts',(2.87062402023451,0.65591542477365,5.05902792115145));
#4146=CARTESIAN_POINT('Ctrl Pts',(2.87475956630543,0.602524480517781,5.08146019215317));
#4147=CARTESIAN_POINT('Ctrl Pts',(2.87889418260464,0.549145539849433,5.10388741983281));
#4148=CARTESIAN_POINT('Ctrl Pts',(2.88302879890385,0.494501362733951,5.12333510754781));
#4149=CARTESIAN_POINT('Ctrl Pts',(2.88716341520306,0.438957034282695,5.13967358830591));
#4150=CARTESIAN_POINT('Ctrl Pts',(2.89130175187135,0.383362726489476,5.15602677059231));
#4151=CARTESIAN_POINT('Ctrl Pts',(2.89544008853964,0.326867148839329,5.16926500674999));
#4152=CARTESIAN_POINT('Ctrl Pts',(2.89957842520793,0.269850104507573,5.17930868621425));
#4153=CARTESIAN_POINT('Ctrl Pts',(2.90371847051207,0.212809518986683,5.18935651251146));
#4154=CARTESIAN_POINT('Ctrl Pts',(2.90785851581621,0.155247555237423,5.19620708965532));
#4155=CARTESIAN_POINT('Ctrl Pts',(2.91199856112035,0.097550542943304,5.19983259638156));
#4156=CARTESIAN_POINT('Ctrl Pts',(2.91614662856738,0.0397417314675851,5.20346512823214));
#4157=CARTESIAN_POINT('Ctrl Pts',(2.92029469601441,-0.0182021292545922,
5.20386009675022));
#4158=CARTESIAN_POINT('Ctrl Pts',(2.92444276346143,-0.0758942242730695,
5.2010418918398));
#4159=CARTESIAN_POINT('Ctrl Pts',(2.92832556269243,-0.129896919511898,5.19840391065973));
#4160=CARTESIAN_POINT('Ctrl Pts',(2.93220836192342,-0.183678700365295,5.19295113580139));
#4161=CARTESIAN_POINT('Ctrl Pts',(2.93609116115441,-0.236929761373951,5.18474431076452));
#4162=CARTESIAN_POINT('Ctrl Pts',(2.94024039722414,-0.293834898607237,5.17597433517856));
#4163=CARTESIAN_POINT('Ctrl Pts',(2.94438963329388,-0.350371063130989,5.16402229316462));
#4164=CARTESIAN_POINT('Ctrl Pts',(2.94853886936362,-0.406155507456992,5.14893299718093));
#4165=CARTESIAN_POINT('Ctrl Pts',(2.95268077025794,-0.461841333946435,5.13387037662161));
#4166=CARTESIAN_POINT('Ctrl Pts',(2.95682267115226,-0.516777579703662,5.11568164538635));
#4167=CARTESIAN_POINT('Ctrl Pts',(2.96096457204658,-0.570590348551148,5.09446285095978));
#4168=CARTESIAN_POINT('Ctrl Pts',(2.96510237801041,-0.624349914882801,5.07326503470012));
#4169=CARTESIAN_POINT('Ctrl Pts',(2.96924018397424,-0.676987723304684,5.04904328073132));
#4170=CARTESIAN_POINT('Ctrl Pts',(2.97337798993807,-0.728145436661753,5.02194329356025));
#4171=CARTESIAN_POINT('Ctrl Pts',(2.97751329306004,-0.779272206164113,4.99485969840537));
#4172=CARTESIAN_POINT('Ctrl Pts',(2.98164859618201,-0.828920196343047,4.96490156436302));
#4173=CARTESIAN_POINT('Ctrl Pts',(2.98578389930398,-0.876753485845831,4.93226161124348));
#4174=CARTESIAN_POINT('Ctrl Pts',(2.98991828809341,-0.924576199211488,4.89962887495188));
#4175=CARTESIAN_POINT('Ctrl Pts',(2.99405267688284,-0.970584578814997,4.86431579004715));
#4176=CARTESIAN_POINT('Ctrl Pts',(2.99818706567227,-1.0144715234176,4.82655848493922));
#4177=CARTESIAN_POINT('Ctrl Pts',(3.00232520117966,-1.05839823980069,4.78876696293002));
#4178=CARTESIAN_POINT('Ctrl Pts',(3.00646333668705,-1.1001992831074,4.74852713370931));
#4179=CARTESIAN_POINT('Ctrl Pts',(3.01060147219444,-1.13960159336577,4.70611466663573));
#4180=CARTESIAN_POINT('Ctrl Pts',(3.01474133040711,-1.17902030680078,4.66368454325762));
#4181=CARTESIAN_POINT('Ctrl Pts',(3.01888118861977,-1.21603796238855,4.61908037948236));
#4182=CARTESIAN_POINT('Ctrl Pts',(3.02302104683244,-1.25042144777123,4.57261144443255));
#4183=CARTESIAN_POINT('Ctrl Pts',(3.02716895377351,-1.28487178165969,4.52605216429879));
#4184=CARTESIAN_POINT('Ctrl Pts',(3.03131686071459,-1.31667742338716,4.47762130385618));
#4185=CARTESIAN_POINT('Ctrl Pts',(3.03546476765566,-1.34564884130241,4.42765688946119));
#4186=CARTESIAN_POINT('Ctrl Pts',(3.03934941234561,-1.37278148105623,4.38086365137199));
#4187=CARTESIAN_POINT('Ctrl Pts',(3.04323405703555,-1.39742853975662,4.332725917409));
#4188=CARTESIAN_POINT('Ctrl Pts',(3.04711870172549,-1.41947265623265,4.28353724173008));
#4189=CARTESIAN_POINT('Ctrl Pts',(3.05165528585028,-1.44521632053973,4.2260934899805));
#4190=CARTESIAN_POINT('Ctrl Pts',(3.05619186997507,-1.46750340567384,4.16700868888048));
#4191=CARTESIAN_POINT('Ctrl Pts',(3.06072845409986,-1.48614312745068,4.10669704255393));
#4192=CARTESIAN_POINT('Ctrl Pts',(3.06525141942865,-1.50472689290411,4.04656645139699));
#4193=CARTESIAN_POINT('Ctrl Pts',(3.06977438475743,-1.51968497676747,3.98521668123109));
#4194=CARTESIAN_POINT('Ctrl Pts',(3.07429735008621,-1.53087461175201,3.92308119827488));
#4195=CARTESIAN_POINT('Ctrl Pts',(3.07879909482774,-1.54201174785402,3.86123723898547));
#4196=CARTESIAN_POINT('Ctrl Pts',(3.08330083956928,-1.54941557119281,3.79861525544587));
#4197=CARTESIAN_POINT('Ctrl Pts',(3.08780258431081,-1.55299366908022,3.73566062146132));
#4198=CARTESIAN_POINT('Ctrl Pts',(3.08988713140844,-1.55465051858958,3.70650927968396));
#4199=CARTESIAN_POINT('Ctrl Pts',(3.09197167850607,-1.55548775667919,3.67728683394445));
#4200=CARTESIAN_POINT('Ctrl Pts',(3.0940562256037,-1.55549986667069,3.64803850823206));
#4201=CARTESIAN_POINT('',(2.5,0.903606778650208,2.38126847156104));
#4202=CARTESIAN_POINT('Origin',(2.5,0.,3.64739446828387));
#4203=CARTESIAN_POINT('Ctrl Pts',(2.5,0.903606778650211,2.38126847156104));
#4204=CARTESIAN_POINT('Ctrl Pts',(2.50424458524762,0.951845303079998,2.41569526461296));
#4205=CARTESIAN_POINT('Ctrl Pts',(2.50848917049525,0.998152286150711,2.45290980505556));
#4206=CARTESIAN_POINT('Ctrl Pts',(2.51273375574287,1.0422040353451,2.49266896033386));
#4207=CARTESIAN_POINT('Ctrl Pts',(2.51697626655841,1.08623425537784,2.53240868434561));
#4208=CARTESIAN_POINT('Ctrl Pts',(2.52121877737395,1.12801106716945,2.57469023195135));
#4209=CARTESIAN_POINT('Ctrl Pts',(2.52546128818949,1.16724434287761,2.61923062238177));
#4210=CARTESIAN_POINT('Ctrl Pts',(2.52970274247019,1.20646784811627,2.66375992068391));
#4211=CARTESIAN_POINT('Ctrl Pts',(2.53394419675089,1.24314875403151,2.71054658023801));
#4212=CARTESIAN_POINT('Ctrl Pts',(2.53818565103159,1.27703555050152,2.759272600095));
#4213=CARTESIAN_POINT('Ctrl Pts',(2.54242733583174,1.31092418869024,2.80800126816995));
#4214=CARTESIAN_POINT('Ctrl Pts',(2.5466690206319,1.34201813870961,2.85866910663541));
#4215=CARTESIAN_POINT('Ctrl Pts',(2.55091070543205,1.37010880618714,2.91092850898334));
#4216=CARTESIAN_POINT('Ctrl Pts',(2.55515390773845,1.39820952338907,2.96320660766845));
#4217=CARTESIAN_POINT('Ctrl Pts',(2.55939711004484,1.42330459453235,3.01707697287856));
#4218=CARTESIAN_POINT('Ctrl Pts',(2.56364031235124,1.4452318670257,3.07216833837198));
#4219=CARTESIAN_POINT('Ctrl Pts',(2.56788991506085,1.46719221439397,3.12734280312106));
#4220=CARTESIAN_POINT('Ctrl Pts',(2.57213951777047,1.48597504305494,3.18374149258933));
#4221=CARTESIAN_POINT('Ctrl Pts',(2.57638912048009,1.50146706506278,3.24097485442182));
#4222=CARTESIAN_POINT('Ctrl Pts',(2.58064201363542,1.51697108246427,3.29825253175462));
#4223=CARTESIAN_POINT('Ctrl Pts',(2.58489490679076,1.52917911615244,3.35636569304));
#4224=CARTESIAN_POINT('Ctrl Pts',(2.58914779994609,1.53802901468287,3.41491436162175));
#4225=CARTESIAN_POINT('Ctrl Pts',(2.59340971679372,1.54689769072741,3.47358725744138));
#4226=CARTESIAN_POINT('Ctrl Pts',(2.59767163364135,1.55239394856735,3.5326970219068));
#4227=CARTESIAN_POINT('Ctrl Pts',(2.60193355048897,1.55450758299866,3.59183887090921));
#4228=CARTESIAN_POINT('Ctrl Pts',(2.60496488051634,1.5560109261533,3.63390408925219));
#4229=CARTESIAN_POINT('Ctrl Pts',(2.60799621054371,1.55580413569242,3.67598547779199));
#4230=CARTESIAN_POINT('Ctrl Pts',(2.61102754057108,1.55389953165917,3.71793874877079));
#4231=CARTESIAN_POINT('Ctrl Pts',(2.61513472499091,1.55131896143399,3.77478172507797));
#4232=CARTESIAN_POINT('Ctrl Pts',(2.61924190941074,1.5456085090895,3.83162701942664));
#4233=CARTESIAN_POINT('Ctrl Pts',(2.62334909383056,1.53676371753942,3.88809662127468));
#4234=CARTESIAN_POINT('Ctrl Pts',(2.62746184330188,1.52790694169175,3.94464273691165));
#4235=CARTESIAN_POINT('Ctrl Pts',(2.6315745927732,1.51590728810265,4.00081160376279));
#4236=CARTESIAN_POINT('Ctrl Pts',(2.63568734224451,1.50081279014695,4.05622355106948));
#4237=CARTESIAN_POINT('Ctrl Pts',(2.63978159373098,1.48578618297733,4.1113862710967));
#4238=CARTESIAN_POINT('Ctrl Pts',(2.64387584521744,1.46769260897502,4.16579833998209));
#4239=CARTESIAN_POINT('Ctrl Pts',(2.64797009670391,1.44663091606903,4.21909302755551));
#4240=CARTESIAN_POINT('Ctrl Pts',(2.65206136756637,1.42558455612138,4.27234891648024));
#4241=CARTESIAN_POINT('Ctrl Pts',(2.65615263842883,1.40157455173156,4.32448854122649));
#4242=CARTESIAN_POINT('Ctrl Pts',(2.66024390929129,1.3747491713709,4.37516157788351));
#4243=CARTESIAN_POINT('Ctrl Pts',(2.66433385356855,1.34793248907838,4.42581818392448));
#4244=CARTESIAN_POINT('Ctrl Pts',(2.66842379784581,1.31830248987026,4.47500867441784));
#4245=CARTESIAN_POINT('Ctrl Pts',(2.67251374212306,1.28605401101196,4.52240608578392));
#4246=CARTESIAN_POINT('Ctrl Pts',(2.67664218704132,1.25350196148786,4.57024967210879));
#4247=CARTESIAN_POINT('Ctrl Pts',(2.68077063195958,1.21828215147022,4.61626576508543));
#4248=CARTESIAN_POINT('Ctrl Pts',(2.68489907687784,1.18063904171931,4.66014898106973));
#4249=CARTESIAN_POINT('Ctrl Pts',(2.68899394060087,1.1433021248915,4.70367524646555));
#4250=CARTESIAN_POINT('Ctrl Pts',(2.6930888043239,1.10358160406715,4.74510285780619));
#4251=CARTESIAN_POINT('Ctrl Pts',(2.69718366804694,1.0617538575275,4.78417017000583));
#4252=CARTESIAN_POINT('Ctrl Pts',(2.70132890356281,1.0194115789482,4.82371805755303));
#4253=CARTESIAN_POINT('Ctrl Pts',(2.70547413907868,0.974910298315913,4.86084680903068));
#4254=CARTESIAN_POINT('Ctrl Pts',(2.70961937459455,0.928569653750268,4.89532821978437));
#4255=CARTESIAN_POINT('Ctrl Pts',(2.71376461011042,0.882229009184622,4.92980963053806));
#4256=CARTESIAN_POINT('Ctrl Pts',(2.71790984562629,0.834049506379408,4.96164345442314));
#4257=CARTESIAN_POINT('Ctrl Pts',(2.72205508114216,0.78437668455737,4.99064927163385));
#4258=CARTESIAN_POINT('Ctrl Pts',(2.72620925196883,0.734596789904449,5.01971761267242));
#4259=CARTESIAN_POINT('Ctrl Pts',(2.7303634227955,0.68309621457768,5.04607495812686));
#4260=CARTESIAN_POINT('Ctrl Pts',(2.73451759362218,0.630201320826852,5.06951490805966));
#4261=CARTESIAN_POINT('Ctrl Pts',(2.73866438607905,0.577400375568407,5.09291322546801));
#4262=CARTESIAN_POINT('Ctrl Pts',(2.74281117853593,0.523210498602565,5.11340422484302));
#4263=CARTESIAN_POINT('Ctrl Pts',(2.74695797099281,0.467983399567045,5.13082690278491));
#4264=CARTESIAN_POINT('Ctrl Pts',(2.75110063850411,0.412811236673221,5.14823224983814));
#4265=CARTESIAN_POINT('Ctrl Pts',(2.75524330601541,0.356604388684665,5.16257516809759));
#4266=CARTESIAN_POINT('Ctrl Pts',(2.75938597352671,0.299733729231273,5.17374303318021));
#4267=CARTESIAN_POINT('Ctrl Pts',(2.76352609926199,0.242897963352565,5.184904046105));
#4268=CARTESIAN_POINT('Ctrl Pts',(2.76766622499728,0.185399701714438,5.19289376819827));
#4269=CARTESIAN_POINT('Ctrl Pts',(2.77180635073256,0.127622009920947,5.19765021253504));
#4270=CARTESIAN_POINT('Ctrl Pts',(2.77594551424784,0.0698577464276025,5.20240555141119));
#4271=CARTESIAN_POINT('Ctrl Pts',(2.78008467776312,0.0118146987145777,5.20392906193616));
#4272=CARTESIAN_POINT('Ctrl Pts',(2.78422384127839,-0.0461191024158946,
5.20221062410177));
#4273=CARTESIAN_POINT('Ctrl Pts',(2.78836663579256,-0.104103724821433,5.20049067880196));
#4274=CARTESIAN_POINT('Ctrl Pts',(2.79250943030673,-0.161978389084661,5.19552311584121));
#4275=CARTESIAN_POINT('Ctrl Pts',(2.79665222482089,-0.219356586646865,5.18734996695733));
#4276=CARTESIAN_POINT('Ctrl Pts',(2.80079668623878,-0.276757871024192,5.17917352950768));
#4277=CARTESIAN_POINT('Ctrl Pts',(2.80494114765667,-0.333661780046128,5.16778903477395));
#4278=CARTESIAN_POINT('Ctrl Pts',(2.80908560907455,-0.389691619463311,5.15328978062137));
#4279=CARTESIAN_POINT('Ctrl Pts',(2.81323796249252,-0.445828152477676,5.13876291658096));
#4280=CARTESIAN_POINT('Ctrl Pts',(2.81739031591049,-0.501086793044878,5.1211095972325));
#4281=CARTESIAN_POINT('Ctrl Pts',(2.82154266932845,-0.555106538707374,5.10047291788125));
#4282=CARTESIAN_POINT('Ctrl Pts',(2.82538932012338,-0.605149267896918,5.08135554249413));
#4283=CARTESIAN_POINT('Ctrl Pts',(2.82923597091831,-0.654128713604237,5.05967858632401));
#4284=CARTESIAN_POINT('Ctrl Pts',(2.83308262171324,-0.701776811900782,5.03559098040972));
#4285=CARTESIAN_POINT('Ctrl Pts',(2.83723812440405,-0.753250629317283,5.00956935366784));
#4286=CARTESIAN_POINT('Ctrl Pts',(2.84139362709486,-0.803378780995949,4.98062856210417));
#4287=CARTESIAN_POINT('Ctrl Pts',(2.84554912978567,-0.851810797414874,4.94893148865918));
#4288=CARTESIAN_POINT('Ctrl Pts',(2.84969749536435,-0.900159631423033,4.91728885521438));
#4289=CARTESIAN_POINT('Ctrl Pts',(2.85384586094303,-0.946817682329859,4.88289961882828));
#4290=CARTESIAN_POINT('Ctrl Pts',(2.85799422652171,-0.991458942442055,4.84597254894932));
#4291=CARTESIAN_POINT('Ctrl Pts',(2.86213861286569,-1.03605738133995,4.80908090060571));
#4292=CARTESIAN_POINT('Ctrl Pts',(2.86628299920966,-1.07864246529873,4.76965657176451));
#4293=CARTESIAN_POINT('Ctrl Pts',(2.87042738555364,-1.11891851883289,4.72795062055584));
#4294=CARTESIAN_POINT('Ctrl Pts',(2.87456937291235,-1.15917125850318,4.68626881090982));
#4295=CARTESIAN_POINT('Ctrl Pts',(2.87871136027106,-1.19711725811529,4.64230836973604));
#4296=CARTESIAN_POINT('Ctrl Pts',(2.88285334762977,-1.23249683959237,4.59635800309163));
#4297=CARTESIAN_POINT('Ctrl Pts',(2.88699451281254,-1.26786939829556,4.55041675750012));
#4298=CARTESIAN_POINT('Ctrl Pts',(2.89113567799531,-1.30067623431274,4.50248678159935));
#4299=CARTESIAN_POINT('Ctrl Pts',(2.89527684317808,-1.33069860539263,4.45288901923136));
#4300=CARTESIAN_POINT('Ctrl Pts',(2.89942184517836,-1.36074879240209,4.40324530420159));
#4301=CARTESIAN_POINT('Ctrl Pts',(2.90356684717864,-1.38800908947886,4.35193115929336));
#4302=CARTESIAN_POINT('Ctrl Pts',(2.90771184917892,-1.41230542657339,4.29929448521236));
#4303=CARTESIAN_POINT('Ctrl Pts',(2.91185863419015,-1.43661221496202,4.24663516897921));
#4304=CARTESIAN_POINT('Ctrl Pts',(2.91600541920137,-1.45795230958072,4.19265267234785));
#4305=CARTESIAN_POINT('Ctrl Pts',(2.9201522042126,-1.47620006451291,4.13771438377995));
#4306=CARTESIAN_POINT('Ctrl Pts',(2.92430704962584,-1.49448328890885,4.08266930773916));
#4307=CARTESIAN_POINT('Ctrl Pts',(2.92846189503908,-1.50966202478595,4.02666522918671));
#4308=CARTESIAN_POINT('Ctrl Pts',(2.93261674045232,-1.52166098851936,3.97008330604912));
#4309=CARTESIAN_POINT('Ctrl Pts',(2.93644788106299,-1.53272511068825,3.91790969138922));
#4310=CARTESIAN_POINT('Ctrl Pts',(2.94027902167365,-1.54108617161881,3.86524520012915));
#4311=CARTESIAN_POINT('Ctrl Pts',(2.94411016228431,-1.54672433177784,3.8123917151894));
#4312=CARTESIAN_POINT('Ctrl Pts',(2.94805469965497,-1.55252937411617,3.75797383610294));
#4313=CARTESIAN_POINT('Ctrl Pts',(2.95199923702563,-1.5554635597827,3.7032412811352));
#4314=CARTESIAN_POINT('Ctrl Pts',(2.95594377439629,-1.55549966270667,3.64841883122548));
#4315=CARTESIAN_POINT('Origin',(1.2059437743963,0.,3.64739446828387));
#4316=CARTESIAN_POINT('',(3.7940562256037,-1.55549937976475,3.64600538531537));
#4317=CARTESIAN_POINT('',(3.65594309057409,-1.55328922867419,3.64812360962188));
#4318=CARTESIAN_POINT('',(1.2059437743963,-1.5555,3.64739446828386));
#4319=CARTESIAN_POINT('Ctrl Pts',(3.0940562256037,-1.55320831614475,3.64803755943733));
#4320=CARTESIAN_POINT('Ctrl Pts',(3.11541956450132,-1.55211225787393,3.34872916974666));
#4321=CARTESIAN_POINT('Ctrl Pts',(3.1737920835893,-1.32451511527677,2.5293530162389));
#4322=CARTESIAN_POINT('Ctrl Pts',(3.26917378286765,0.00194386449727044,
1.80949553386703));
#4323=CARTESIAN_POINT('Ctrl Pts',(3.38020132343871,1.54419526187211,2.6507072563878));
#4324=CARTESIAN_POINT('Ctrl Pts',(3.4912288640098,1.67560476579265,4.40256135417452));
#4325=CARTESIAN_POINT('Ctrl Pts',(3.60225640458087,0.276097817182276,5.46444788548381));
#4326=CARTESIAN_POINT('Ctrl Pts',(3.70319885844552,-1.22562677556159,4.92053574953289));
#4327=CARTESIAN_POINT('Ctrl Pts',(3.76713213211979,-1.55162911722742,4.02218696309102));
#4328=CARTESIAN_POINT('Ctrl Pts',(3.7940562256037,-1.5548981372976,3.64600592223341));
#4329=CARTESIAN_POINT('Ctrl Pts',(2.95594474730389,-1.55731930826876,3.64840649193144));
#4330=CARTESIAN_POINT('Ctrl Pts',(2.98900906582105,-1.55406984475527,3.18832795677562));
#4331=CARTESIAN_POINT('Ctrl Pts',(3.05908256452858,-1.09493216072152,2.20731900520876));
#4332=CARTESIAN_POINT('Ctrl Pts',(3.16616524342647,0.571437519320519,1.90065774706199));
#4333=CARTESIAN_POINT('Ctrl Pts',(3.27719278399755,1.77703909951801,3.17828914298809));
#4334=CARTESIAN_POINT('Ctrl Pts',(3.38822032456863,1.35908642417454,4.88467959896744));
#4335=CARTESIAN_POINT('Ctrl Pts',(3.4992478651397,-0.300609421841399,5.4605432395681));
#4336=CARTESIAN_POINT('Ctrl Pts',(3.58848878714152,-1.41386361340158,4.59192891748905));
#4337=CARTESIAN_POINT('Ctrl Pts',(3.64072052895299,-1.55417851871196,3.86136782353057));
#4338=CARTESIAN_POINT('Ctrl Pts',(3.65594309057409,-1.55328922867419,3.64812360962188));
#4339=CARTESIAN_POINT('Origin',(1.2059437743963,0.,3.64739446828387));
#4340=CARTESIAN_POINT('',(4.49405622566528,-1.55549997006787,3.64769962209175));
#4341=CARTESIAN_POINT('',(4.35539415465377,-1.5555,3.64739446822634));
#4342=CARTESIAN_POINT('',(1.2059437743963,-1.5555,3.64739446828386));
#4343=CARTESIAN_POINT('Ctrl Pts',(3.7940562256037,-1.55549937976475,3.64600538531537));
#4344=CARTESIAN_POINT('Ctrl Pts',(3.79924672256038,-1.55543459285259,3.57345680185877));
#4345=CARTESIAN_POINT('Ctrl Pts',(3.80443721951705,-1.55029041969612,3.5011332527424));
#4346=CARTESIAN_POINT('Ctrl Pts',(3.80962771647373,-1.54018379952585,3.42964664699029));
#4347=CARTESIAN_POINT('Ctrl Pts',(3.8145223062235,-1.5306533518822,3.36223545097562));
#4348=CARTESIAN_POINT('Ctrl Pts',(3.81941689597326,-1.51671067473822,3.29556811307793));
#4349=CARTESIAN_POINT('Ctrl Pts',(3.82431148572303,-1.49849211920356,3.23013960769526));
#4350=CARTESIAN_POINT('Ctrl Pts',(3.82845990987145,-1.48305092809396,3.17468548271223));
#4351=CARTESIAN_POINT('Ctrl Pts',(3.83260833401987,-1.46449498927746,3.11997351657148));
#4352=CARTESIAN_POINT('Ctrl Pts',(3.83675675816829,-1.44291390367817,3.06637836130212));
#4353=CARTESIAN_POINT('Ctrl Pts',(3.84089781910633,-1.42137112324431,3.0128783343005));
#4354=CARTESIAN_POINT('Ctrl Pts',(3.84503888004438,-1.39681404658781,2.96049166264528));
#4355=CARTESIAN_POINT('Ctrl Pts',(3.84917994098242,-1.36938210802426,2.90957816850252));
#4356=CARTESIAN_POINT('Ctrl Pts',(3.85331689052468,-1.34197740488623,2.85871522312702));
#4357=CARTESIAN_POINT('Ctrl Pts',(3.85745384006693,-1.3117037407644,2.8093230134315));
#4358=CARTESIAN_POINT('Ctrl Pts',(3.86159078960919,-1.27874802547169,2.7617400563645));
#4359=CARTESIAN_POINT('Ctrl Pts',(3.86572522133919,-1.24581236754324,2.71418605903009));
#4360=CARTESIAN_POINT('Ctrl Pts',(3.86985965306919,-1.21019819009308,2.66843955871357));
#4361=CARTESIAN_POINT('Ctrl Pts',(3.87399408479919,-1.1721364451885,2.62481126684701));
#4362=CARTESIAN_POINT('Ctrl Pts',(3.87812758870062,-1.13408324191102,2.58119276582428));
#4363=CARTESIAN_POINT('Ctrl Pts',(3.88226109260206,-1.09358390378638,2.5396919216926));
#4364=CARTESIAN_POINT('Ctrl Pts',(3.88639459650349,-1.05090908617977,2.50058570367453));
#4365=CARTESIAN_POINT('Ctrl Pts',(3.89053183292945,-1.0081957335174,2.46144417302066));
#4366=CARTESIAN_POINT('Ctrl Pts',(3.89466906935541,-0.96330335971897,2.42470194310739));
#4367=CARTESIAN_POINT('Ctrl Pts',(3.89880630578137,-0.91653786376006,2.39059751002285));
#4368=CARTESIAN_POINT('Ctrl Pts',(3.90294525567577,-0.86975299950965,2.35647895232384));
#4369=CARTESIAN_POINT('Ctrl Pts',(3.90708420557016,-0.82109390399685,2.32500065384954));
#4370=CARTESIAN_POINT('Ctrl Pts',(3.91122315546455,-0.770895120881121,2.29635747300888));
#4371=CARTESIAN_POINT('Ctrl Pts',(3.91537015021836,-0.720598766602835,2.26765861853869));
#4372=CARTESIAN_POINT('Ctrl Pts',(3.91951714497217,-0.668757211424592,2.2418061280752));
#4373=CARTESIAN_POINT('Ctrl Pts',(3.92366413972598,-0.61572840390472,2.21894818556094));
#4374=CARTESIAN_POINT('Ctrl Pts',(3.92755576858202,-0.565965033127231,2.1974978018592));
#4375=CARTESIAN_POINT('Ctrl Pts',(3.93144739743807,-0.515156658330791,2.17868417709864));
#4376=CARTESIAN_POINT('Ctrl Pts',(3.93533902629412,-0.463610415301871,2.16258955422155));
#4377=CARTESIAN_POINT('Ctrl Pts',(3.93948744510044,-0.40866288256262,2.14543292426175));
#4378=CARTESIAN_POINT('Ctrl Pts',(3.94363586390677,-0.352646623653681,2.13129460873933));
#4379=CARTESIAN_POINT('Ctrl Pts',(3.9477842827131,-0.295924871440223,2.12030287952336));
#4380=CARTESIAN_POINT('Ctrl Pts',(3.95192533826022,-0.239303797818583,2.10933066013874));
#4381=CARTESIAN_POINT('Ctrl Pts',(3.95606639380735,-0.181980223358909,2.10149403971228));
#4382=CARTESIAN_POINT('Ctrl Pts',(3.96020744935448,-0.124331997913654,2.0968713938684));
#4383=CARTESIAN_POINT('Ctrl Pts',(3.96434439347988,-0.0667410081572655,
2.09225333759024));
#4384=CARTESIAN_POINT('Ctrl Pts',(3.96848133760527,-0.00882652245795808,
2.09084297499291));
#4385=CARTESIAN_POINT('Ctrl Pts',(3.97261828173067,0.0490257099392183,2.09266724791209));
#4386=CARTESIAN_POINT('Ctrl Pts',(3.97675270802733,0.10684273228551,2.0944904105415));
#4387=CARTESIAN_POINT('Ctrl Pts',(3.98088713432399,0.164597057061208,2.09954428982219));
#4388=CARTESIAN_POINT('Ctrl Pts',(3.98502156062065,0.221902358276826,2.1078037455945));
#4389=CARTESIAN_POINT('Ctrl Pts',(3.98915505908169,0.279194799207568,2.11606134780436));
#4390=CARTESIAN_POINT('Ctrl Pts',(3.99328855754272,0.336037901517856,2.12752302405912));
#4391=CARTESIAN_POINT('Ctrl Pts',(3.99742205600376,0.392052103871693,2.14211197059456));
#4392=CARTESIAN_POINT('Ctrl Pts',(4.00155928702243,0.448116887165724,2.15671409097879));
#4393=CARTESIAN_POINT('Ctrl Pts',(4.00569651804109,0.503350769332033,2.17444899447389));
#4394=CARTESIAN_POINT('Ctrl Pts',(4.00983374905976,0.557387348271569,2.1951893884185));
#4395=CARTESIAN_POINT('Ctrl Pts',(4.01397269355601,0.611446307026598,2.21593837221463));
#4396=CARTESIAN_POINT('Ctrl Pts',(4.01811163805227,0.664306497514946,2.23969511520849));
#4397=CARTESIAN_POINT('Ctrl Pts',(4.02225058254852,0.715622597532277,2.26628457117171));
#4398=CARTESIAN_POINT('Ctrl Pts',(4.026397571991,0.76703844164267,2.29292570957317));
#4399=CARTESIAN_POINT('Ctrl Pts',(4.03054456143347,0.816903747256577,2.32241029888278));
#4400=CARTESIAN_POINT('Ctrl Pts',(4.03469155087595,0.864899667938198,2.35451828921629));
#4401=CARTESIAN_POINT('Ctrl Pts',(4.03858322287236,0.909940626698687,2.38464948886733));
#4402=CARTESIAN_POINT('Ctrl Pts',(4.04247489486878,0.953335299435898,2.41709037054296));
#4403=CARTESIAN_POINT('Ctrl Pts',(4.04636656686519,0.994847796632108,2.4516277219925));
#4404=CARTESIAN_POINT('Ctrl Pts',(4.0505149831588,1.03909898735835,2.48844359743718));
#4405=CARTESIAN_POINT('Ctrl Pts',(4.05466339945241,1.08139645579429,2.5277962696892));
#4406=CARTESIAN_POINT('Ctrl Pts',(4.05881181574603,1.12143520301905,2.56945043660615));
#4407=CARTESIAN_POINT('Ctrl Pts',(4.06295286868638,1.16140288229428,2.61103066823696));
#4408=CARTESIAN_POINT('Ctrl Pts',(4.06709392162673,1.19911944019534,2.65490391383242));
#4409=CARTESIAN_POINT('Ctrl Pts',(4.07123497456709,1.23431383195747,2.70079549604776));
#4410=CARTESIAN_POINT('Ctrl Pts',(4.0753719160303,1.26947328068963,2.74664151444305));
#4411=CARTESIAN_POINT('Ctrl Pts',(4.07950885749352,1.30211520951442,2.79450148797202));
#4412=CARTESIAN_POINT('Ctrl Pts',(4.08364579895674,1.33200746762012,2.84406616914072));
#4413=CARTESIAN_POINT('Ctrl Pts',(4.08778022254044,1.36188153230803,2.89360068360374));
#4414=CARTESIAN_POINT('Ctrl Pts',(4.09191464612414,1.38900897537653,2.94483740401325));
#4415=CARTESIAN_POINT('Ctrl Pts',(4.09604906970783,1.41320106171707,2.99743830886868));
#4416=CARTESIAN_POINT('Ctrl Pts',(4.10018256540968,1.43738771866765,3.05002740858995));
#4417=CARTESIAN_POINT('Ctrl Pts',(4.10431606111153,1.45864010930287,3.10397961210197));
#4418=CARTESIAN_POINT('Ctrl Pts',(4.10844955681337,1.4768165506152,3.15893451513619));
#4419=CARTESIAN_POINT('Ctrl Pts',(4.11258678502196,1.49500940507867,3.21393904191767));
#4420=CARTESIAN_POINT('Ctrl Pts',(4.11672401323054,1.51012059463378,3.26994758241584));
#4421=CARTESIAN_POINT('Ctrl Pts',(4.12086124143913,1.52205797546509,3.3265833566884));
#4422=CARTESIAN_POINT('Ctrl Pts',(4.12500018309285,1.53400030019751,3.38324258683218));
#4423=CARTESIAN_POINT('Ctrl Pts',(4.12913912474658,1.5427661155984,3.44052905299624));
#4424=CARTESIAN_POINT('Ctrl Pts',(4.1332780664003,1.5483148227319,3.49805773566702));
#4425=CARTESIAN_POINT('Ctrl Pts',(4.13742505298203,1.55387431497743,3.55569823777109));
#4426=CARTESIAN_POINT('Ctrl Pts',(4.14157203956375,1.55620418080109,3.6135813750954));
#4427=CARTESIAN_POINT('Ctrl Pts',(4.14571902614548,1.55531598818641,3.67131991272536));
#4428=CARTESIAN_POINT('Ctrl Pts',(4.14961071990908,1.55448247363523,3.72550400577357));
#4429=CARTESIAN_POINT('Ctrl Pts',(4.15350241367268,1.55081545093387,3.77956041061298));
#4430=CARTESIAN_POINT('Ctrl Pts',(4.15739410743628,1.5443658084111,3.83317525257204));
#4431=CARTESIAN_POINT('Ctrl Pts',(4.16154252658954,1.53749069896047,3.89032693273814));
#4432=CARTESIAN_POINT('Ctrl Pts',(4.16569094574279,1.52742442723014,3.94721615662609));
#4433=CARTESIAN_POINT('Ctrl Pts',(4.16983936489605,1.51419888969869,4.00345903045659));
#4434=CARTESIAN_POINT('Ctrl Pts',(4.17398042076164,1.50099682699795,4.05960207530557));
#4435=CARTESIAN_POINT('Ctrl Pts',(4.17812147662723,1.48464674700967,4.115100544536));
#4436=CARTESIAN_POINT('Ctrl Pts',(4.18226253249283,1.46523204945129,4.16957766531415));
#4437=CARTESIAN_POINT('Ctrl Pts',(4.18639947691915,1.44583662773766,4.22400069858879));
#4438=CARTESIAN_POINT('Ctrl Pts',(4.19053642134547,1.42338279090196,4.27740390454189));
#4439=CARTESIAN_POINT('Ctrl Pts',(4.1946733657718,1.39800409065943,4.32942438881485));
#4440=CARTESIAN_POINT('Ctrl Pts',(4.19880779235131,1.37264083652224,4.38141321213309));
#4441=CARTESIAN_POINT('Ctrl Pts',(4.20294221893083,1.34435647560062,4.43202051497412));
#4442=CARTESIAN_POINT('Ctrl Pts',(4.20707664551035,1.31333230115958,4.48090422631366));
#4443=CARTESIAN_POINT('Ctrl Pts',(4.21121014423562,1.28231508921055,4.529776967097));
#4444=CARTESIAN_POINT('Ctrl Pts',(4.21534364296089,1.24855956333046,4.57692644490256));
#4445=CARTESIAN_POINT('Ctrl Pts',(4.21947714168616,1.21229136733348,4.62203793678336));
#4446=CARTESIAN_POINT('Ctrl Pts',(4.22361437293737,1.17599042136089,4.66719016408588));
#4447=CARTESIAN_POINT('Ctrl Pts',(4.22775160418858,1.13717259725465,4.71030032036805));
#4448=CARTESIAN_POINT('Ctrl Pts',(4.23188883543979,1.09610419663964,4.75108638186709));
#4449=CARTESIAN_POINT('Ctrl Pts',(4.23602778015166,1.0550187872851,4.79188933517311));
#4450=CARTESIAN_POINT('Ctrl Pts',(4.24016672486353,1.01168133261274,4.83036592741653));
#4451=CARTESIAN_POINT('Ctrl Pts',(4.2443056695754,0.966393050279938,4.86627293735724));
#4452=CARTESIAN_POINT('Ctrl Pts',(4.24845265920163,0.92101674059282,4.90224974016541));
#4453=CARTESIAN_POINT('Ctrl Pts',(4.25259964882785,0.873682452134044,4.93564667763785));
#4454=CARTESIAN_POINT('Ctrl Pts',(4.25674663845407,0.824721598466709,4.96626312551344));
#4455=CARTESIAN_POINT('Ctrl Pts',(4.26063830830516,0.778775142055065,4.99499459529853));
#4456=CARTESIAN_POINT('Ctrl Pts',(4.26452997815626,0.731396819639839,5.02127767127384));
#4457=CARTESIAN_POINT('Ctrl Pts',(4.26842164800735,0.682877801894672,5.04498459334898));
#4458=CARTESIAN_POINT('Ctrl Pts',(4.27257006638072,0.631157796762306,5.07025555282798));
#4459=CARTESIAN_POINT('Ctrl Pts',(4.27671848475409,0.577924791530181,5.09270459408807));
#4460=CARTESIAN_POINT('Ctrl Pts',(4.28086690312746,0.523518435833337,5.11214997598562));
#4461=CARTESIAN_POINT('Ctrl Pts',(4.2850079582022,0.469208649529545,5.13156084300521));
#4462=CARTESIAN_POINT('Ctrl Pts',(4.28914901327693,0.413730132841133,5.1479784589707));
#4463=CARTESIAN_POINT('Ctrl Pts',(4.29329006835167,0.357444531875432,5.16126819374196));
#4464=CARTESIAN_POINT('Ctrl Pts',(4.29742701198102,0.30121481405313,5.17454473380371));
#4465=CARTESIAN_POINT('Ctrl Pts',(4.30156395561037,0.244180103809134,5.18469942661238));
#4466=CARTESIAN_POINT('Ctrl Pts',(4.30570089923972,0.186717636011615,5.19164728903643));
#4467=CARTESIAN_POINT('Ctrl Pts',(4.30983532501754,0.129290141367093,5.19859092281064));
#4468=CARTESIAN_POINT('Ctrl Pts',(4.31396975079536,0.0714359211261826,5.20233153280199));
#4469=CARTESIAN_POINT('Ctrl Pts',(4.31810417657318,0.0135406585836287,5.20283553131555));
#4470=CARTESIAN_POINT('Ctrl Pts',(4.32223767449341,-0.0443416109675579,
5.20333941672058));
#4471=CARTESIAN_POINT('Ctrl Pts',(4.32637117241365,-0.102264384113827,5.20060812818138));
#4472=CARTESIAN_POINT('Ctrl Pts',(4.33050467033388,-0.159840849343945,5.19466017037935));
#4473=CARTESIAN_POINT('Ctrl Pts',(4.33464190078134,-0.217469305824048,5.18870684160221));
#4474=CARTESIAN_POINT('Ctrl Pts',(4.33877913122879,-0.27475031016035,5.17953109150458));
#4475=CARTESIAN_POINT('Ctrl Pts',(4.34291636167625,-0.331302421324728,5.16720332324701));
#4476=CARTESIAN_POINT('Ctrl Pts',(4.34705530558373,-0.387877953901842,5.15487044936664));
#4477=CARTESIAN_POINT('Ctrl Pts',(4.35119424949121,-0.443723488318946,5.13938309309897));
#4478=CARTESIAN_POINT('Ctrl Pts',(4.35533319339869,-0.498471197309644,5.12086205036795));
#4479=CARTESIAN_POINT('Ctrl Pts',(4.35948018223006,-0.553325320197597,5.10230500802389));
#4480=CARTESIAN_POINT('Ctrl Pts',(4.36362717106142,-0.607076868142607,5.08070268949815));
#4481=CARTESIAN_POINT('Ctrl Pts',(4.36777415989279,-0.659377377398221,5.05622438143004));
#4482=CARTESIAN_POINT('Ctrl Pts',(4.37166583612134,-0.708457964997463,5.03325309949574));
#4483=CARTESIAN_POINT('Ctrl Pts',(4.37555751234988,-0.75626058697706,5.00774967826569));
#4484=CARTESIAN_POINT('Ctrl Pts',(4.37944918857843,-0.80251981524134,4.97988919478188));
#4485=CARTESIAN_POINT('Ctrl Pts',(4.38359760630016,-0.851830855280502,4.95019070070559));
#4486=CARTESIAN_POINT('Ctrl Pts',(4.3877460240219,-0.899594386513456,4.91768906526787));
#4487=CARTESIAN_POINT('Ctrl Pts',(4.39189444174363,-0.945473326109707,4.88257074704535));
#4488=CARTESIAN_POINT('Ctrl Pts',(4.3960354961564,-0.991270832053471,4.84751476271605));
#4489=CARTESIAN_POINT('Ctrl Pts',(4.40017655056918,-1.0351899758604,4.80985162826571));
#4490=CARTESIAN_POINT('Ctrl Pts',(4.40431760498195,-1.07692128200617,4.76981186050577));
#4491=CARTESIAN_POINT('Ctrl Pts',(4.40845454794349,-1.11861115517064,4.72981184628104));
#4492=CARTESIAN_POINT('Ctrl Pts',(4.41259149090503,-1.15811712064239,4.68744023260772));
#4493=CARTESIAN_POINT('Ctrl Pts',(4.41672843386657,-1.1951629199996,4.64296759199605));
#4494=CARTESIAN_POINT('Ctrl Pts',(4.42086285897187,-1.2321861722736,4.59852201864561));
#4495=CARTESIAN_POINT('Ctrl Pts',(4.42499728407717,-1.26675189399725,4.55197835246775));
#4496=CARTESIAN_POINT('Ctrl Pts',(4.42913170918247,-1.298622390327,4.50364217621738));
#4497=CARTESIAN_POINT('Ctrl Pts',(4.43326520642658,-1.33048573417588,4.45531684772954));
#4498=CARTESIAN_POINT('Ctrl Pts',(4.43739870367069,-1.35965476700263,4.40520024231461));
#4499=CARTESIAN_POINT('Ctrl Pts',(4.44153220091481,-1.38593491887239,4.35362718534686));
#4500=CARTESIAN_POINT('Ctrl Pts',(4.44566943068581,-1.41223880158502,4.30200755817217));
#4501=CARTESIAN_POINT('Ctrl Pts',(4.44980666045682,-1.43564835228939,4.24892931577879));
#4502=CARTESIAN_POINT('Ctrl Pts',(4.45394389022782,-1.45601549310078,4.1947509644091));
#4503=CARTESIAN_POINT('Ctrl Pts',(4.45808283345756,-1.47639106908672,4.14055017474754));
#4504=CARTESIAN_POINT('Ctrl Pts',(4.46222177668729,-1.49372156596722,4.08524886536933));
#4505=CARTESIAN_POINT('Ctrl Pts',(4.46636071991703,-1.50790861123553,4.02922148430256));
#4506=CARTESIAN_POINT('Ctrl Pts',(4.47050770807723,-1.52212323209172,3.97308520191481));
#4507=CARTESIAN_POINT('Ctrl Pts',(4.47465469623744,-1.53318209055859,3.91622054035901));
#4508=CARTESIAN_POINT('Ctrl Pts',(4.47880168439765,-1.54103804564489,3.85901202869643));
#4509=CARTESIAN_POINT('Ctrl Pts',(4.4826933659816,-1.54841035406552,3.80532552111992));
#4510=CARTESIAN_POINT('Ctrl Pts',(4.48658504756556,-1.55296246258241,3.7513366184223));
#4511=CARTESIAN_POINT('Ctrl Pts',(4.49047672914951,-1.55469719497037,3.69736327806831));
#4512=CARTESIAN_POINT('Ctrl Pts',(4.49166989463424,-1.55522905318279,3.68081538600245));
#4513=CARTESIAN_POINT('Ctrl Pts',(4.49286306011897,-1.55549672149286,3.66425895728589));
#4514=CARTESIAN_POINT('Ctrl Pts',(4.4940562256037,-1.55549997006771,3.64769962294641));
#4515=CARTESIAN_POINT('Ctrl Pts',(3.6546715967529,-1.55549987088463,3.64802824892936));
#4516=CARTESIAN_POINT('Ctrl Pts',(3.65583554611893,-1.55550678373996,3.63106189683294));
#4517=CARTESIAN_POINT('Ctrl Pts',(3.65700687296806,-1.55523611007452,3.61409701908527));
#4518=CARTESIAN_POINT('Ctrl Pts',(3.65935708872429,-1.55414398231178,3.58031035979871));
#4519=CARTESIAN_POINT('Ctrl Pts',(3.66053568689316,-1.553326734999,3.56349088548048));
#4520=CARTESIAN_POINT('Ctrl Pts',(3.66337304825961,-1.55072111876458,3.52332906623534));
#4521=CARTESIAN_POINT('Ctrl Pts',(3.66503936028455,-1.54867857683863,3.50000800802103));
#4522=CARTESIAN_POINT('Ctrl Pts',(3.66896318495946,-1.54269205754422,3.44576983796235));
#4523=CARTESIAN_POINT('Ctrl Pts',(3.67123284707807,-1.53834370033202,3.41490860768942));
#4524=CARTESIAN_POINT('Ctrl Pts',(3.68315082552336,-1.51100262491104,3.25565012963292));
#4525=CARTESIAN_POINT('Ctrl Pts',(3.69328367884008,-1.4728553502184,3.13040637075574));
#4526=CARTESIAN_POINT('Ctrl Pts',(3.70803836616504,-1.39487416093124,2.9563457391689));
#4527=CARTESIAN_POINT('Ctrl Pts',(3.71267374577518,-1.36701325213118,2.9027478965415));
#4528=CARTESIAN_POINT('Ctrl Pts',(3.7186219360081,-1.32611964739185,2.83414959584725));
#4529=CARTESIAN_POINT('Ctrl Pts',(3.72005913626803,-1.31581933905118,2.8175871968984));
#4530=CARTESIAN_POINT('Ctrl Pts',(3.72256246548942,-1.29708770617275,2.78869391088441));
#4531=CARTESIAN_POINT('Ctrl Pts',(3.72363581372294,-1.28878631801524,2.77628424176131));
#4532=CARTESIAN_POINT('Ctrl Pts',(3.72625693457796,-1.26785639942322,2.74595063821165));
#4533=CARTESIAN_POINT('Ctrl Pts',(3.72779180579342,-1.25502548111744,2.72817088166312));
#4534=CARTESIAN_POINT('Ctrl Pts',(3.73483261797166,-1.19371101295616,2.646886116256));
#4535=CARTESIAN_POINT('Ctrl Pts',(3.74009812593129,-1.14076045336598,2.58689086018623));
#4536=CARTESIAN_POINT('Ctrl Pts',(3.75216359587134,-1.00929016446441,2.45929557370979));
#4537=CARTESIAN_POINT('Ctrl Pts',(3.75893462135127,-0.928279295445408,2.39499531484981));
#4538=CARTESIAN_POINT('Ctrl Pts',(3.76820638574018,-0.814750259645629,2.32195845638415));
#4539=CARTESIAN_POINT('Ctrl Pts',(3.77042440273262,-0.787389467575519,2.30552406392182));
#4540=CARTESIAN_POINT('Ctrl Pts',(3.77449557003691,-0.736979070458635,2.27731757093337));
#4541=CARTESIAN_POINT('Ctrl Pts',(3.77633744759334,-0.714103896334543,2.26525687274259));
#4542=CARTESIAN_POINT('Ctrl Pts',(3.78052407799056,-0.66203132754091,2.23943995787143));
#4543=CARTESIAN_POINT('Ctrl Pts',(3.78287931487905,-0.632685878936419,2.22601145424461));
#4544=CARTESIAN_POINT('Ctrl Pts',(3.79467579654245,-0.48560822553442,2.16416571683606));
#4545=CARTESIAN_POINT('Ctrl Pts',(3.80456766130157,-0.362675252472706,2.12942285856925));
#4546=CARTESIAN_POINT('Ctrl Pts',(3.81907447215377,-0.177330195496224,2.1008599285124));
#4547=CARTESIAN_POINT('Ctrl Pts',(3.82370504365851,-0.117254235714453,2.09514835401263));
#4548=CARTESIAN_POINT('Ctrl Pts',(3.82964856040533,-0.0375065884422887,
2.09222446656055));
#4549=CARTESIAN_POINT('Ctrl Pts',(3.83108561643035,-0.0180072309045984,
2.09187644622304));
#4550=CARTESIAN_POINT('Ctrl Pts',(3.8335889385491,0.0164270910425676,2.09190953556467));
#4551=CARTESIAN_POINT('Ctrl Pts',(3.83466241648109,0.0313576239195768,2.09213887509024));
#4552=CARTESIAN_POINT('Ctrl Pts',(3.83728434998413,0.0682069141321993,2.0932358269107));
#4553=CARTESIAN_POINT('Ctrl Pts',(3.838819886545,0.0901145359934732,2.09435204504922));
#4554=CARTESIAN_POINT('Ctrl Pts',(3.84753727450119,0.2158521755376,2.10342844313732));
#4555=CARTESIAN_POINT('Ctrl Pts',(3.85430539505902,0.31870990806458,2.12133652219784));
#4556=CARTESIAN_POINT('Ctrl Pts',(3.86606195438739,0.490423267156688,2.16936768880612));
#4557=CARTESIAN_POINT('Ctrl Pts',(3.8709835101432,0.560303712190277,2.1944195002446));
#4558=CARTESIAN_POINT('Ctrl Pts',(3.87836259443023,0.658944774022286,2.23795954717948));
#4559=CARTESIAN_POINT('Ctrl Pts',(3.88069634274767,0.689310208044315,2.25255893699471));
#4560=CARTESIAN_POINT('Ctrl Pts',(3.88488549146297,0.742147378174409,2.28010932246872));
#4561=CARTESIAN_POINT('Ctrl Pts',(3.88672620365827,0.764814597393887,2.29265837394579));
#4562=CARTESIAN_POINT('Ctrl Pts',(3.89079627301214,0.813669412320937,2.32132236129602));
#4563=CARTESIAN_POINT('Ctrl Pts',(3.89303318337718,0.839713288787557,2.33765919423335));
#4564=CARTESIAN_POINT('Ctrl Pts',(3.90507091660595,0.975481178202121,2.42853824264551));
#4565=CARTESIAN_POINT('Ctrl Pts',(3.91537836815592,1.07579959823276,2.51610516441578));
#4566=CARTESIAN_POINT('Ctrl Pts',(3.9302395803928,1.20329253551957,2.65986489289857));
#4567=CARTESIAN_POINT('Ctrl Pts',(3.93481226237696,1.24022315403313,2.70666307428741));
#4568=CARTESIAN_POINT('Ctrl Pts',(3.94069738495624,1.28553665769888,2.77140690163977));
#4569=CARTESIAN_POINT('Ctrl Pts',(3.94213095783939,1.29639246572689,2.78755414106253));
#4570=CARTESIAN_POINT('Ctrl Pts',(3.94463099181762,1.31504202698692,2.81645055925576));
#4571=CARTESIAN_POINT('Ctrl Pts',(3.94570457421527,1.32295931239138,2.82911456180249));
#4572=CARTESIAN_POINT('Ctrl Pts',(3.94833055590118,1.34208104326945,2.86070376855959));
#4573=CARTESIAN_POINT('Ctrl Pts',(3.94986991580466,1.35306867879814,2.87975583757066));
#4574=CARTESIAN_POINT('Ctrl Pts',(3.95716047724157,1.40379912232059,2.97219618430927));
#4575=CARTESIAN_POINT('Ctrl Pts',(3.96265200893647,1.43800116895935,3.04847820183902));
#4576=CARTESIAN_POINT('Ctrl Pts',(3.97255653176305,1.48831473982964,3.19024780674964));
#4577=CARTESIAN_POINT('Ctrl Pts',(3.97695707524958,1.50661116414811,3.25472924498381));
#4578=CARTESIAN_POINT('Ctrl Pts',(3.98463974755486,1.53066914784216,3.36653822113341));
#4579=CARTESIAN_POINT('Ctrl Pts',(3.98786841186562,1.53851744739748,3.41331832020172));
#4580=CARTESIAN_POINT('Ctrl Pts',(3.99308676380265,1.54754519080994,3.48786243751187));
#4581=CARTESIAN_POINT('Ctrl Pts',(3.9950318376677,1.55013900021883,3.51542669523062));
#4582=CARTESIAN_POINT('Ctrl Pts',(3.99890865359388,1.5537959718898,3.56981652850039));
#4583=CARTESIAN_POINT('Ctrl Pts',(4.0008383074917,1.55490289421904,3.59662950069241));
#4584=CARTESIAN_POINT('Ctrl Pts',(4.0058148796882,1.55595583761273,3.66504128398193));
#4585=CARTESIAN_POINT('Ctrl Pts',(4.00889081730036,1.55492777078369,3.70663136778311));
#4586=CARTESIAN_POINT('Ctrl Pts',(4.02021507583115,1.5451581658646,3.85717591500451));
#4587=CARTESIAN_POINT('Ctrl Pts',(4.02872846159367,1.52661002056276,3.96516491297887));
#4588=CARTESIAN_POINT('Ctrl Pts',(4.0416298553189,1.4812328812758,4.12578027454465));
#4589=CARTESIAN_POINT('Ctrl Pts',(4.04605113103239,1.46248512658162,4.18035078001407));
#4590=CARTESIAN_POINT('Ctrl Pts',(4.05178295040139,1.43346189450557,4.25166337019466));
#4591=CARTESIAN_POINT('Ctrl Pts',(4.05320695329046,1.42584152590384,4.26943140330701));
#4592=CARTESIAN_POINT('Ctrl Pts',(4.05569830103502,1.4117442759695,4.30067986094914));
#4593=CARTESIAN_POINT('Ctrl Pts',(4.05677251003104,1.40540142053741,4.31421572277039));
#4594=CARTESIAN_POINT('Ctrl Pts',(4.05941129017011,1.38916956655271,4.34759409175537));
#4595=CARTESIAN_POINT('Ctrl Pts',(4.06096245831637,1.37904990282173,4.3673202275207));
#4596=CARTESIAN_POINT('Ctrl Pts',(4.06771803553348,1.33258346637705,4.45331867323967));
#4597=CARTESIAN_POINT('Ctrl Pts',(4.07271401779842,1.29185274847035,4.51711374837032));
#4598=CARTESIAN_POINT('Ctrl Pts',(4.08240829927575,1.20385374876517,4.63503528730301));
#4599=CARTESIAN_POINT('Ctrl Pts',(4.08709734636856,1.15716490630705,4.68934792617514));
#4600=CARTESIAN_POINT('Ctrl Pts',(4.09428522760558,1.08186035945405,4.76562036350551));
#4601=CARTESIAN_POINT('Ctrl Pts',(4.09669956078721,1.05595219040481,4.79011739420133));
#4602=CARTESIAN_POINT('Ctrl Pts',(4.10133405586615,1.0053685171172,4.83475578174971));
#4603=CARTESIAN_POINT('Ctrl Pts',(4.10354607254252,0.980871428792938,4.85507146753235));
#4604=CARTESIAN_POINT('Ctrl Pts',(4.10761129536024,0.935369985281612,4.89050822931019));
#4605=CARTESIAN_POINT('Ctrl Pts',(4.1094534041472,0.914578126148205,4.90588385487765));
#4606=CARTESIAN_POINT('Ctrl Pts',(4.11364728350535,0.86692424435567,4.93931928796557));
#4607=CARTESIAN_POINT('Ctrl Pts',(4.11600971701674,0.839863119069872,4.95707268674783));
#4608=CARTESIAN_POINT('Ctrl Pts',(4.12776720776442,0.704269964340975,5.04009727419388));
#4609=CARTESIAN_POINT('Ctrl Pts',(4.13760696901566,0.58861472270949,5.09277969498722));
#4610=CARTESIAN_POINT('Ctrl Pts',(4.15209204024162,0.410052301754927,5.14909841878641));
#4611=CARTESIAN_POINT('Ctrl Pts',(4.15675058905871,0.351195803164859,5.16394339408211));
#4612=CARTESIAN_POINT('Ctrl Pts',(4.16272218540384,0.272443798948657,5.17897392928248));
#4613=CARTESIAN_POINT('Ctrl Pts',(4.16416081350884,0.253201732900082,5.18227239520491));
#4614=CARTESIAN_POINT('Ctrl Pts',(4.16666552363156,0.219141589904864,5.18745294356212));
#4615=CARTESIAN_POINT('Ctrl Pts',(4.16773886117159,0.204350985223939,5.18948520955101));
#4616=CARTESIAN_POINT('Ctrl Pts',(4.17035850698454,0.167793747187004,5.19397300024505));
#4617=CARTESIAN_POINT('Ctrl Pts',(4.17189195897003,0.146000645682124,5.19618232992628));
#4618=CARTESIAN_POINT('Ctrl Pts',(4.18062243716554,0.0201587373252086,5.20625972862681));
#4619=CARTESIAN_POINT('Ctrl Pts',(4.18740359634422,-0.0844369124588652,
5.20410360241846));
#4620=CARTESIAN_POINT('Ctrl Pts',(4.19917557832368,-0.261661543952743,5.18252119934615));
#4621=CARTESIAN_POINT('Ctrl Pts',(4.2040987530863,-0.334540989733271,5.1683025951143));
#4622=CARTESIAN_POINT('Ctrl Pts',(4.21147563304062,-0.438580618065651,5.14016296928556));
#4623=CARTESIAN_POINT('Ctrl Pts',(4.21380525218518,-0.470741964500488,5.13033494943032));
#4624=CARTESIAN_POINT('Ctrl Pts',(4.21799003989885,-0.527071454822542,5.11110444380182));
#4625=CARTESIAN_POINT('Ctrl Pts',(4.21983064183914,-0.551370894405368,5.10212509645781));
#4626=CARTESIAN_POINT('Ctrl Pts',(4.22390400242872,-0.604033807235253,5.08115563162041));
#4627=CARTESIAN_POINT('Ctrl Pts',(4.22614440236696,-0.632287646929261,5.06892181386123));
#4628=CARTESIAN_POINT('Ctrl Pts',(4.23812145992241,-0.779459349230403,4.99994128604649));
#4629=CARTESIAN_POINT('Ctrl Pts',(4.24835666459985,-0.891152971317602,4.92910139579836));
#4630=CARTESIAN_POINT('Ctrl Pts',(4.2632016428346,-1.03891283267353,4.80664626364936));
#4631=CARTESIAN_POINT('Ctrl Pts',(4.26782534952745,-1.08300182460265,4.76556847845416));
#4632=CARTESIAN_POINT('Ctrl Pts',(4.2737618948435,-1.13806943313479,4.70794065377742));
#4633=CARTESIAN_POINT('Ctrl Pts',(4.27519850063879,-1.15127156698492,4.69359431729355));
#4634=CARTESIAN_POINT('Ctrl Pts',(4.27770133638681,-1.17410413686269,4.667827065502));
#4635=CARTESIAN_POINT('Ctrl Pts',(4.27877476820538,-1.18384496852476,4.65651008880306));
#4636=CARTESIAN_POINT('Ctrl Pts',(4.28114087800316,-1.2051827631869,4.63098531790359));
#4637=CARTESIAN_POINT('Ctrl Pts',(4.28242797244066,-1.21669392899853,4.61670990418397));
#4638=CARTESIAN_POINT('Ctrl Pts',(4.2908026717144,-1.29072584311949,4.52150271466698));
#4639=CARTESIAN_POINT('Ctrl Pts',(4.29746748967359,-1.345395616747,4.43476660068686));
#4640=CARTESIAN_POINT('Ctrl Pts',(4.30949517736764,-1.42707242919977,4.27148493600978));
#4641=CARTESIAN_POINT('Ctrl Pts',(4.31481006451829,-1.45737082104822,4.19702433963268));
#4642=CARTESIAN_POINT('Ctrl Pts',(4.32259461685936,-1.4919546781145,4.08872067062042));
#4643=CARTESIAN_POINT('Ctrl Pts',(4.32491140714319,-1.50109295279396,4.05656098880324));
#4644=CARTESIAN_POINT('Ctrl Pts',(4.32908270041734,-1.51545879030477,3.99901259731048));
#4645=CARTESIAN_POINT('Ctrl Pts',(4.33092301439652,-1.52110124708773,3.97374014819923));
#4646=CARTESIAN_POINT('Ctrl Pts',(4.33500692163564,-1.53209368873157,3.91799691542913));
#4647=CARTESIAN_POINT('Ctrl Pts',(4.33725843599312,-1.53717057127464,3.88748431756645));
#4648=CARTESIAN_POINT('Ctrl Pts',(4.34470269924416,-1.55076865302059,3.78741568145514));
#4649=CARTESIAN_POINT('Ctrl Pts',(4.35000710688228,-1.55550000000259,3.71744083094465));
#4650=CARTESIAN_POINT('Ctrl Pts',(4.35539415465377,-1.5555,3.64739446822634));
#4651=CARTESIAN_POINT('Origin',(1.2059437743963,0.,3.64739446828387));
#4652=CARTESIAN_POINT('',(5.19405622556279,-1.55549955406273,3.6485723098073));
#4653=CARTESIAN_POINT('',(5.05594377443823,-1.5554999873946,3.64759249708933));
#4654=CARTESIAN_POINT('',(1.2059437743963,-1.5555,3.64739446828386));
#4655=CARTESIAN_POINT('Ctrl Pts',(4.49405622566528,-1.55549997006787,3.64769962209176));
#4656=CARTESIAN_POINT('Ctrl Pts',(4.49818264884198,-1.5555112048523,3.59043110243973));
#4657=CARTESIAN_POINT('Ctrl Pts',(4.50230907201867,-1.55235548796177,3.53303695693617));
#4658=CARTESIAN_POINT('Ctrl Pts',(4.50643549519536,-1.54601728863954,3.47589871548614));
#4659=CARTESIAN_POINT('Ctrl Pts',(4.51055471403468,-1.53969015520277,3.41886023190159));
#4660=CARTESIAN_POINT('Ctrl Pts',(4.514673932874,-1.53019162173892,3.36207728507756));
#4661=CARTESIAN_POINT('Ctrl Pts',(4.51879315171332,-1.5175581507441,3.3059306940557));
#4662=CARTESIAN_POINT('Ctrl Pts',(4.52290838596156,-1.50493690032262,3.24983841459506));
#4663=CARTESIAN_POINT('Ctrl Pts',(4.52702362020979,-1.48918683358188,3.1943817831957));
#4664=CARTESIAN_POINT('Ctrl Pts',(4.53113885445802,-1.47039588386744,3.13993393316247));
#4665=CARTESIAN_POINT('Ctrl Pts',(4.53525173244782,-1.45161569328144,3.0855172583184));
#4666=CARTESIAN_POINT('Ctrl Pts',(4.53936461043761,-1.42979824176697,3.0321087172434));
#4667=CARTESIAN_POINT('Ctrl Pts',(4.5434774884274,-1.40508135768999,2.98006649174457));
#4668=CARTESIAN_POINT('Ctrl Pts',(4.54758963497004,-1.38036886934142,2.92803352159878));
#4669=CARTESIAN_POINT('Ctrl Pts',(4.55170178151268,-1.35275819858068,2.87736686006037));
#4670=CARTESIAN_POINT('Ctrl Pts',(4.55581392805532,-1.32243444548001,2.82840277882177));
#4671=CARTESIAN_POINT('Ctrl Pts',(4.55992988829277,-1.2920825694662,2.77939328722124));
#4672=CARTESIAN_POINT('Ctrl Pts',(4.56404584853023,-1.25901286363784,2.73208997848163));
#4673=CARTESIAN_POINT('Ctrl Pts',(4.56816180876768,-1.22345458874825,2.68680136021426));
#4674=CARTESIAN_POINT('Ctrl Pts',(4.5722797249649,-1.18787941608731,2.64149122018524));
#4675=CARTESIAN_POINT('Ctrl Pts',(4.57639764116213,-1.14981366757698,2.59819807345484));
#4676=CARTESIAN_POINT('Ctrl Pts',(4.58051555735935,-1.10952573337367,2.55719590977188));
#4677=CARTESIAN_POINT('Ctrl Pts',(4.58464111268066,-1.06916306124124,2.51611768319655));
#4678=CARTESIAN_POINT('Ctrl Pts',(4.58876666800197,-1.02657036213306,2.47733928112313));
#4679=CARTESIAN_POINT('Ctrl Pts',(4.59289222332329,-0.9820506777324,2.44109570082809));
#4680=CARTESIAN_POINT('Ctrl Pts',(4.59576290545572,-0.95107257839864,2.41587635694221));
#4681=CARTESIAN_POINT('Ctrl Pts',(4.59863358758815,-0.919162176237036,2.39188346783216));
#4682=CARTESIAN_POINT('Ctrl Pts',(4.60150426972059,-0.886429325065602,2.36918349130717));
#4683=CARTESIAN_POINT('Ctrl Pts',(4.60565268890353,-0.839127122506235,2.33637978343416));
#4684=CARTESIAN_POINT('Ctrl Pts',(4.60980110808647,-0.789902466076869,2.30613665572479));
#4685=CARTESIAN_POINT('Ctrl Pts',(4.61394952726942,-0.739063605726851,2.27868513585056));
#4686=CARTESIAN_POINT('Ctrl Pts',(4.61809058315377,-0.688314982571362,2.25128234146157));
#4687=CARTESIAN_POINT('Ctrl Pts',(4.62223163903812,-0.63595829684667,2.22666156523234));
#4688=CARTESIAN_POINT('Ctrl Pts',(4.62637269492247,-0.582330668195458,2.20501059327728));
#4689=CARTESIAN_POINT('Ctrl Pts',(4.6305096393609,-0.528756283716943,2.18338111748229));
#4690=CARTESIAN_POINT('Ctrl Pts',(4.63464658379934,-0.473913936833424,2.16471579788024));
#4691=CARTESIAN_POINT('Ctrl Pts',(4.63878352823778,-0.418163666519841,2.14915570293214));
#4692=CARTESIAN_POINT('Ctrl Pts',(4.64291795482279,-0.362447327290285,2.13360507826797));
#4693=CARTESIAN_POINT('Ctrl Pts',(4.64705238140779,-0.305824660527237,2.12115607155639));
#4694=CARTESIAN_POINT('Ctrl Pts',(4.6511868079928,-0.248671830850126,2.11190022520067));
#4695=CARTESIAN_POINT('Ctrl Pts',(4.65532030671694,-0.191531827588675,2.10264645607075));
#4696=CARTESIAN_POINT('Ctrl Pts',(4.65945380544109,-0.133862411372917,2.09658450778816));
#4697=CARTESIAN_POINT('Ctrl Pts',(4.66358730416523,-0.0760487419178204,
2.09375460047257));
#4698=CARTESIAN_POINT('Ctrl Pts',(4.66772453540496,-0.0181828671914085,
2.09092213777379));
#4699=CARTESIAN_POINT('Ctrl Pts',(4.67186176664469,0.0398269998097328,2.09132757497707));
#4700=CARTESIAN_POINT('Ctrl Pts',(4.67599899788442,0.0975931575226902,2.09495901854538));
#4701=CARTESIAN_POINT('Ctrl Pts',(4.68013794257913,0.155383239378352,2.09859196609417));
#4702=CARTESIAN_POINT('Ctrl Pts',(4.68427688727384,0.21292889243015,2.10545352302033));
#4703=CARTESIAN_POINT('Ctrl Pts',(4.68841583196855,0.269848249449869,2.1154799235821));
#4704=CARTESIAN_POINT('Ctrl Pts',(4.69256282156823,0.326878241148732,2.1255258125511));
#4705=CARTESIAN_POINT('Ctrl Pts',(4.69670981116791,0.383278995100267,2.13874871992924));
#4706=CARTESIAN_POINT('Ctrl Pts',(4.7008568007676,0.438680449723801,2.15503401818137));
#4707=CARTESIAN_POINT('Ctrl Pts',(4.70474847060895,0.490670975608444,2.17031667142703));
#4708=CARTESIAN_POINT('Ctrl Pts',(4.70864014045031,0.541781273715245,2.18829563175242));
#4709=CARTESIAN_POINT('Ctrl Pts',(4.71253181029166,0.59172248829761,2.20883798804304));
#4710=CARTESIAN_POINT('Ctrl Pts',(4.71668022643349,0.644958489593126,2.23073559136017));
#4711=CARTESIAN_POINT('Ctrl Pts',(4.72082864257532,0.697088813768266,2.25563816533532));
#4712=CARTESIAN_POINT('Ctrl Pts',(4.72497705871715,0.747752051956174,2.28341238673172));
#4713=CARTESIAN_POINT('Ctrl Pts',(4.7291181115616,0.798325364621586,2.31113730983097));
#4714=CARTESIAN_POINT('Ctrl Pts',(4.73325916440605,0.84743630712596,2.34172351508062));
#4715=CARTESIAN_POINT('Ctrl Pts',(4.7374002172505,0.894744095649229,2.3749899519052));
#4716=CARTESIAN_POINT('Ctrl Pts',(4.74153715865178,0.942004914647769,2.40822336015719));
#4717=CARTESIAN_POINT('Ctrl Pts',(4.74567410005306,0.987465702944323,2.44413142958443));
#4718=CARTESIAN_POINT('Ctrl Pts',(4.74981104145434,1.0308124524694,2.4824884901749));
#4719=CARTESIAN_POINT('Ctrl Pts',(4.75394546500998,1.07413282008236,2.5208222057023));
#4720=CARTESIAN_POINT('Ctrl Pts',(4.75807988856561,1.11534131031358,2.56160161338362));
#4721=CARTESIAN_POINT('Ctrl Pts',(4.76221431212125,1.1541567390143,2.60456060242226));
#4722=CARTESIAN_POINT('Ctrl Pts',(4.76634780782885,1.19296345674993,2.64750995059728));
#4723=CARTESIAN_POINT('Ctrl Pts',(4.77048130353644,1.22937783025481,2.69263752287338));
#4724=CARTESIAN_POINT('Ctrl Pts',(4.77461479924404,1.26315688060035,2.73964177895049));
#4725=CARTESIAN_POINT('Ctrl Pts',(4.77875202751133,1.29696643353513,2.78668848001941));
#4726=CARTESIAN_POINT('Ctrl Pts',(4.78288925577862,1.32813560223623,2.83561482825154));
#4727=CARTESIAN_POINT('Ctrl Pts',(4.78702648404591,1.35646378270176,2.88608884225813));
#4728=CARTESIAN_POINT('Ctrl Pts',(4.79116542578736,1.38480369556448,2.93658376057877));
#4729=CARTESIAN_POINT('Ctrl Pts',(4.79530436752881,1.41030004380517,2.98862715446279));
#4730=CARTESIAN_POINT('Ctrl Pts',(4.79944330927026,1.43279894537414,3.04186376540024));
#4731=CARTESIAN_POINT('Ctrl Pts',(4.8035902959877,1.4553415786828,3.09520385381655));
#4732=CARTESIAN_POINT('Ctrl Pts',(4.80773728270514,1.47487494518795,3.14974130245457));
#4733=CARTESIAN_POINT('Ctrl Pts',(4.81188426942258,1.49129427990581,3.20510313814026));
#4734=CARTESIAN_POINT('Ctrl Pts',(4.81577596323597,1.50670282295052,3.25705684045857));
#4735=CARTESIAN_POINT('Ctrl Pts',(4.81966765704935,1.51936934366868,3.30973606651607));
#4736=CARTESIAN_POINT('Ctrl Pts',(4.82355935086274,1.529248536561,3.36282608735225));
#4737=CARTESIAN_POINT('Ctrl Pts',(4.82770776987243,1.53977943481765,3.41941832256454));
#4738=CARTESIAN_POINT('Ctrl Pts',(4.83185618888211,1.54718672201663,3.47671443938878));
#4739=CARTESIAN_POINT('Ctrl Pts',(4.8360046078918,1.55138603020247,3.53433857373336));
#4740=CARTESIAN_POINT('Ctrl Pts',(4.84014566356742,1.5555778847273,3.59186042676296));
#4741=CARTESIAN_POINT('Ctrl Pts',(4.84428671924304,1.55657302470185,3.64970862663667));
#4742=CARTESIAN_POINT('Ctrl Pts',(4.84842777491866,1.55433835797629,3.7074987021079));
#4743=CARTESIAN_POINT('Ctrl Pts',(4.85256471912704,1.55210590995044,3.76523140042202));
#4744=CARTESIAN_POINT('Ctrl Pts',(4.85670166333542,1.54665002876786,3.82290557099121));
#4745=CARTESIAN_POINT('Ctrl Pts',(4.8608386075438,1.53798962954334,3.88013498778392));
#4746=CARTESIAN_POINT('Ctrl Pts',(4.86497303387806,1.52933450130966,3.93732957295696));
#4747=CARTESIAN_POINT('Ctrl Pts',(4.86910746021232,1.51747879900517,3.99407942716112));
#4748=CARTESIAN_POINT('Ctrl Pts',(4.87324188654659,1.50249322175681,4.0500039174711));
#4749=CARTESIAN_POINT('Ctrl Pts',(4.87737538499991,1.48751100769124,4.10591585676085));
#4750=CARTESIAN_POINT('Ctrl Pts',(4.88150888345323,1.46940044792973,4.16100229719957));
#4751=CARTESIAN_POINT('Ctrl Pts',(4.88564238190656,1.44828274104247,4.21489543920685));
#4752=CARTESIAN_POINT('Ctrl Pts',(4.88977961284657,1.42714596518473,4.26883724590764));
#4753=CARTESIAN_POINT('Ctrl Pts',(4.89391684378659,1.40299680515486,4.32158311447311));
#4754=CARTESIAN_POINT('Ctrl Pts',(4.89805407472661,1.37600503548618,4.37278428921926));
#4755=CARTESIAN_POINT('Ctrl Pts',(4.90219301910532,1.34900208714669,4.4240066689877));
#4756=CARTESIAN_POINT('Ctrl Pts',(4.90633196348404,1.31915444986936,4.47368263163854));
#4757=CARTESIAN_POINT('Ctrl Pts',(4.91047090786276,1.28667682036269,4.52149000650688));
#4758=CARTESIAN_POINT('Ctrl Pts',(4.9146178971234,1.25413606396402,4.56939030475157));
#4759=CARTESIAN_POINT('Ctrl Pts',(4.91876488638405,1.21895541635315,4.61541434136031));
#4760=CARTESIAN_POINT('Ctrl Pts',(4.9229118756447,1.18139112703999,4.6592715630692));
#4761=CARTESIAN_POINT('Ctrl Pts',(4.9268035475744,1.14613955509435,4.70042863098328));
#4762=CARTESIAN_POINT('Ctrl Pts',(4.93069521950411,1.10878944216813,4.73967755409276));
#4763=CARTESIAN_POINT('Ctrl Pts',(4.93458689143382,1.06958042727821,4.77680934315641));
#4764=CARTESIAN_POINT('Ctrl Pts',(4.93873531572807,1.02778460459304,4.81639089541027));
#4765=CARTESIAN_POINT('Ctrl Pts',(4.94288374002232,0.983701114049866,4.85373212912805));
#4766=CARTESIAN_POINT('Ctrl Pts',(4.94703216431657,0.937599712680949,4.88855804685867));
#4767=CARTESIAN_POINT('Ctrl Pts',(4.95117322534675,0.89158013919844,4.92332215017247));
#4768=CARTESIAN_POINT('Ctrl Pts',(4.95531428637694,0.843550176143952,4.95557948781594));
#4769=CARTESIAN_POINT('Ctrl Pts',(4.95945534740713,0.793814658995242,4.98509343933987));
#4770=CARTESIAN_POINT('Ctrl Pts',(4.96359229700889,0.744128521466237,5.01457808810822));
#4771=CARTESIAN_POINT('Ctrl Pts',(4.96772924661065,0.692740630421661,5.04132448297694));
#4772=CARTESIAN_POINT('Ctrl Pts',(4.97186619621242,0.639985543720192,5.06513871666902));
#4773=CARTESIAN_POINT('Ctrl Pts',(4.97600062796938,0.587262565004926,5.08893845645853));
#4774=CARTESIAN_POINT('Ctrl Pts',(4.98013505972634,0.53317451373346,5.10980935885719));
#4775=CARTESIAN_POINT('Ctrl Pts',(4.98426949148331,0.478079379464018,5.12760403349121));
#4776=CARTESIAN_POINT('Ctrl Pts',(4.98840299537921,0.422996609803011,5.14539471459318));
#4777=CARTESIAN_POINT('Ctrl Pts',(4.99253649927511,0.366907701096048,5.16011037858374));
#4778=CARTESIAN_POINT('Ctrl Pts',(4.99667000317101,0.310187297829131,5.17165300615252));
#4779=CARTESIAN_POINT('Ctrl Pts',(5.00080723954057,0.253415677140779,5.18320605648958));
#4780=CARTESIAN_POINT('Ctrl Pts',(5.00494447591013,0.196011933603237,5.19158023947205));
#4781=CARTESIAN_POINT('Ctrl Pts',(5.00908171227969,0.138361107359043,5.19672866527637));
#4782=CARTESIAN_POINT('Ctrl Pts',(5.01322066208979,0.0806864049679458,5.20187922330634));
#4783=CARTESIAN_POINT('Ctrl Pts',(5.0173596118999,0.0227649373575623,5.20380134227935));
#4784=CARTESIAN_POINT('Ctrl Pts',(5.02149856171001,-0.0350161759652235,
5.20250029022036));
#4785=CARTESIAN_POINT('Ctrl Pts',(5.02564555633343,-0.0929095975523984,
5.20119670932643));
#4786=CARTESIAN_POINT('Ctrl Pts',(5.02979255095684,-0.150661598631284,5.19665747786722));
#4787=CARTESIAN_POINT('Ctrl Pts',(5.03393954558026,-0.207889035771002,5.18893992619493));
#4788=CARTESIAN_POINT('Ctrl Pts',(5.03783117438847,-0.261592491699183,5.18169760997701));
#4789=CARTESIAN_POINT('Ctrl Pts',(5.04172280319669,-0.31483371984599,5.17165692314211));
#4790=CARTESIAN_POINT('Ctrl Pts',(5.0456144320049,-0.367307093263548,5.15890554969819));
#4791=CARTESIAN_POINT('Ctrl Pts',(5.04976283477336,-0.423242717724022,5.14531282657291));
#4792=CARTESIAN_POINT('Ctrl Pts',(5.05391123754182,-0.478539950070369,5.12858247703885));
#4793=CARTESIAN_POINT('Ctrl Pts',(5.05805964031028,-0.532821374525066,5.10879161924908));
#4794=CARTESIAN_POINT('Ctrl Pts',(5.06220067980811,-0.587006451339394,5.08903588954351));
#4795=CARTESIAN_POINT('Ctrl Pts',(5.06634171930595,-0.640178813856002,5.06623061086352));
#4796=CARTESIAN_POINT('Ctrl Pts',(5.07048275880378,-0.69197421424734,5.04050319943761));
#4797=CARTESIAN_POINT('Ctrl Pts',(5.07461968688348,-0.743718189737107,5.01480133139181));
#4798=CARTESIAN_POINT('Ctrl Pts',(5.07875661496318,-0.794087447787288,4.98618330930369));
#4799=CARTESIAN_POINT('Ctrl Pts',(5.08289354304288,-0.842737458631716,4.95482470574167));
#4800=CARTESIAN_POINT('Ctrl Pts',(5.08702795332396,-0.891357860324755,4.92348518751229));
#4801=CARTESIAN_POINT('Ctrl Pts',(5.09116236360505,-0.938260652246804,4.88940867573679));
#4802=CARTESIAN_POINT('Ctrl Pts',(5.09529677388614,-0.983127633410414,4.85281568363759));
#4803=CARTESIAN_POINT('Ctrl Pts',(5.09943025638825,-1.0279845462356,4.81623090315903));
#4804=CARTESIAN_POINT('Ctrl Pts',(5.10356373889036,-1.07080615196526,4.77713109241526));
#4805=CARTESIAN_POINT('Ctrl Pts',(5.10769722139246,-1.11130665585478,4.73577756565945));
#4806=CARTESIAN_POINT('Ctrl Pts',(5.11183443666738,-1.15184373403227,4.69438669428688));
#4807=CARTESIAN_POINT('Ctrl Pts',(5.11597165194229,-1.19005515556612,4.65073841184166));
#4808=CARTESIAN_POINT('Ctrl Pts',(5.1201088672172,-1.22569240828007,4.60513053332716));
#4809=CARTESIAN_POINT('Ctrl Pts',(5.12424779606124,-1.26134442138042,4.55950376475076));
#4810=CARTESIAN_POINT('Ctrl Pts',(5.12838672490527,-1.29441984130356,4.51191620982779));
#4811=CARTESIAN_POINT('Ctrl Pts',(5.13252565374931,-1.32471281917244,4.46269576027366));
#4812=CARTESIAN_POINT('Ctrl Pts',(5.1366726278983,-1.35506468093469,4.41337963535488));
#4813=CARTESIAN_POINT('Ctrl Pts',(5.14081960204729,-1.38262304284483,4.36242473206691));
#4814=CARTESIAN_POINT('Ctrl Pts',(5.14496657619628,-1.4072279282867,4.31018388269083));
#4815=CARTESIAN_POINT('Ctrl Pts',(5.14885837498951,-1.43031880371297,4.26115756440314));
#4816=CARTESIAN_POINT('Ctrl Pts',(5.15275017378274,-1.45080881805192,4.21099922990181));
#4817=CARTESIAN_POINT('Ctrl Pts',(5.15664197257597,-1.46860557248654,4.16001315938037));
#4818=CARTESIAN_POINT('Ctrl Pts',(5.16149448951435,-1.49079558202462,4.09644081559507));
#4819=CARTESIAN_POINT('Ctrl Pts',(5.16634700645272,-1.50887543297736,4.03136398579808));
#4820=CARTESIAN_POINT('Ctrl Pts',(5.1711995233911,-1.52267165228913,3.96528012274959));
#4821=CARTESIAN_POINT('Ctrl Pts',(5.17600347704233,-1.53632980103497,3.89985761743711));
#4822=CARTESIAN_POINT('Ctrl Pts',(5.18080743069357,-1.54578953856301,3.83344827699785));
#4823=CARTESIAN_POINT('Ctrl Pts',(5.18561138434481,-1.55092904889536,3.76655543207882));
#4824=CARTESIAN_POINT('Ctrl Pts',(5.18842633141747,-1.55394062032491,3.72735858888317));
#4825=CARTESIAN_POINT('Ctrl Pts',(5.19124127849013,-1.55546970192271,3.6879961113706));
#4826=CARTESIAN_POINT('Ctrl Pts',(5.19405622556279,-1.55549955406273,3.64857230980729));
#4827=CARTESIAN_POINT('Ctrl Pts',(4.35539415465377,-1.5555,3.64739446822634));
#4828=CARTESIAN_POINT('Ctrl Pts',(4.35542999814836,-1.55549999999998,3.64692840471077));
#4829=CARTESIAN_POINT('Ctrl Pts',(4.35546584504022,-1.55549979055614,3.64646233800919));
#4830=CARTESIAN_POINT('Ctrl Pts',(4.36188857679378,-1.55542473595912,3.56296395502291));
#4831=CARTESIAN_POINT('Ctrl Pts',(4.3683744954262,-1.54870199287245,3.48007311827889));
#4832=CARTESIAN_POINT('Ctrl Pts',(4.37785809760788,-1.52889270440881,3.35806064973541));
#4833=CARTESIAN_POINT('Ctrl Pts',(4.38093859904207,-1.52082399216784,3.31827147924459));
#4834=CARTESIAN_POINT('Ctrl Pts',(4.38531873479868,-1.50684734298434,3.2609621066012));
#4835=CARTESIAN_POINT('Ctrl Pts',(4.3866710431493,-1.50217004120609,3.24316169155456));
#4836=CARTESIAN_POINT('Ctrl Pts',(4.38910145249918,-1.49307977307113,3.21090706305394));
#4837=CARTESIAN_POINT('Ctrl Pts',(4.39018445434306,-1.48877062776986,3.19642827795493));
#4838=CARTESIAN_POINT('Ctrl Pts',(4.39294051384069,-1.47714668947666,3.15935583138246));
#4839=CARTESIAN_POINT('Ctrl Pts',(4.3945968999736,-1.46952431871857,3.13686289014797));
#4840=CARTESIAN_POINT('Ctrl Pts',(4.3983386853491,-1.45091238522659,3.08581728243223));
#4841=CARTESIAN_POINT('Ctrl Pts',(4.40040948261443,-1.43958953000532,3.05739624327089));
#4842=CARTESIAN_POINT('Ctrl Pts',(4.40816645041642,-1.39359871348182,2.95118001327666));
#4843=CARTESIAN_POINT('Ctrl Pts',(4.41370528325849,-1.3534009877825,2.87594199554479));
#4844=CARTESIAN_POINT('Ctrl Pts',(4.42377475954006,-1.27096408468807,2.7481102953198));
#4845=CARTESIAN_POINT('Ctrl Pts',(4.42825545667103,-1.23109277752972,2.69425711502341));
#4846=CARTESIAN_POINT('Ctrl Pts',(4.43498426132566,-1.16800436737407,2.61963291254183));
#4847=CARTESIAN_POINT('Ctrl Pts',(4.43712901503915,-1.14743635971122,2.59671964265138));
#4848=CARTESIAN_POINT('Ctrl Pts',(4.44113146877616,-1.10833588627031,2.55567895097272));
#4849=CARTESIAN_POINT('Ctrl Pts',(4.44298009405443,-1.09000387279486,2.53737527190498));
#4850=CARTESIAN_POINT('Ctrl Pts',(4.4472756489092,-1.04684672837059,2.49638511099431));
#4851=CARTESIAN_POINT('Ctrl Pts',(4.44973562529083,-1.02172668075679,2.47402970038334));
#4852=CARTESIAN_POINT('Ctrl Pts',(4.45772661735186,-0.938928703210286,2.40501999259118));
#4853=CARTESIAN_POINT('Ctrl Pts',(4.46337778056004,-0.878637787054404,2.36167507033744));
#4854=CARTESIAN_POINT('Ctrl Pts',(4.47715923622267,-0.726626581277186,2.26808858605382));
#4855=CARTESIAN_POINT('Ctrl Pts',(4.48533743175627,-0.632476451274925,2.22245708528392));
#4856=CARTESIAN_POINT('Ctrl Pts',(4.49479424411113,-0.513896047406532,2.17907206156494));
#4857=CARTESIAN_POINT('Ctrl Pts',(4.49641661501248,-0.493171773749606,2.17198212850311));
#4858=CARTESIAN_POINT('Ctrl Pts',(4.49910532165137,-0.458079326012556,2.16079887788346));
#4859=CARTESIAN_POINT('Ctrl Pts',(4.50018369446635,-0.443790664739438,2.1564709188448));
#4860=CARTESIAN_POINT('Ctrl Pts',(4.50264447935619,-0.41067826895064,2.14695964673776));
#4861=CARTESIAN_POINT('Ctrl Pts',(4.50401897428641,-0.391815574230527,2.14192379497556));
#4862=CARTESIAN_POINT('Ctrl Pts',(4.50959855783353,-0.313977050032548,2.12270516721578));
#4863=CARTESIAN_POINT('Ctrl Pts',(4.51366228573272,-0.25428516122497,2.11162111071013));
#4864=CARTESIAN_POINT('Ctrl Pts',(4.52606993601889,-0.0684829468292242,
2.08825446455552));
#4865=CARTESIAN_POINT('Ctrl Pts',(4.53425766468571,0.0585741758225829,2.08785139797019));
#4866=CARTESIAN_POINT('Ctrl Pts',(4.5451646093482,0.216408854517286,2.10668202767637));
#4867=CARTESIAN_POINT('Ctrl Pts',(4.54741203071619,0.24841434475502,2.11151762772885));
#4868=CARTESIAN_POINT('Ctrl Pts',(4.55151215067338,0.305677513143337,2.12200596710734));
#4869=CARTESIAN_POINT('Ctrl Pts',(4.55335270308443,0.330989559565052,2.12729756806459));
#4870=CARTESIAN_POINT('Ctrl Pts',(4.5575039691887,0.387127098001942,2.14050193863269));
#4871=CARTESIAN_POINT('Ctrl Pts',(4.55982431334069,0.417864477660873,2.14873457099207));
#4872=CARTESIAN_POINT('Ctrl Pts',(4.56922601848365,0.539747479762893,2.18542045337305));
#4873=CARTESIAN_POINT('Ctrl Pts',(4.57653994180552,0.628426750286668,2.22129153993351));
#4874=CARTESIAN_POINT('Ctrl Pts',(4.59078706731346,0.791868255272748,2.30562245244562));
#4875=CARTESIAN_POINT('Ctrl Pts',(4.597679539285,0.866892415079856,2.35282605929805));
#4876=CARTESIAN_POINT('Ctrl Pts',(4.60592319943792,0.954771650292071,2.41920075137131));
#4877=CARTESIAN_POINT('Ctrl Pts',(4.6075258349408,0.97176988712405,2.43260554580481));
#4878=CARTESIAN_POINT('Ctrl Pts',(4.6101937199705,0.999998791079666,2.45583873107124));
#4879=CARTESIAN_POINT('Ctrl Pts',(4.61127050077445,1.01137685470935,2.46548094434886));
#4880=CARTESIAN_POINT('Ctrl Pts',(4.613742968741,1.03747024495647,2.4882463572274));
#4881=CARTESIAN_POINT('Ctrl Pts',(4.61513033147309,1.05207774628456,2.50148811569253));
#4882=CARTESIAN_POINT('Ctrl Pts',(4.62097017138366,1.11320178934594,2.55905182138824));
#4883=CARTESIAN_POINT('Ctrl Pts',(4.62526321254511,1.15720499907292,2.6059596510751));
#4884=CARTESIAN_POINT('Ctrl Pts',(4.63745006339755,1.27467787353898,2.74785836622972));
#4885=CARTESIAN_POINT('Ctrl Pts',(4.6452288041292,1.34022062815111,2.84878601565727));
#4886=CARTESIAN_POINT('Ctrl Pts',(4.65570114374138,1.40816552533107,2.98577733975348));
#4887=CARTESIAN_POINT('Ctrl Pts',(4.65798652166037,1.42187189399599,3.01577162522033));
#4888=CARTESIAN_POINT('Ctrl Pts',(4.66212562874524,1.44462423359303,3.07006283812805));
#4889=CARTESIAN_POINT('Ctrl Pts',(4.66396610915149,1.4540356366406,3.09419359364092));
#4890=CARTESIAN_POINT('Ctrl Pts',(4.66804353334394,1.47332480837505,3.14754915902081));
#4891=CARTESIAN_POINT('Ctrl Pts',(4.67028822661346,1.48294422274814,3.17685488018609));
#4892=CARTESIAN_POINT('Ctrl Pts',(4.67824178661334,1.51353851851047,3.28034753753506));
#4893=CARTESIAN_POINT('Ctrl Pts',(4.68409277103487,1.52986293152239,3.35578087399551));
#4894=CARTESIAN_POINT('Ctrl Pts',(4.69864160539919,1.55598401909998,3.54269161394477));
#4895=CARTESIAN_POINT('Ctrl Pts',(4.70741080660326,1.55948670067154,3.65462557599081));
#4896=CARTESIAN_POINT('Ctrl Pts',(4.71730637109817,1.54938978687576,3.78668991388579));
#4897=CARTESIAN_POINT('Ctrl Pts',(4.71884206424525,1.54739089558878,3.80737404655244));
#4898=CARTESIAN_POINT('Ctrl Pts',(4.72144090338253,1.5432497279148,3.8427967889763));
#4899=CARTESIAN_POINT('Ctrl Pts',(4.72251385516975,1.54130938448318,3.85755446356819));
#4900=CARTESIAN_POINT('Ctrl Pts',(4.72503404277329,1.5361989712694,3.89253042639371));
#4901=CARTESIAN_POINT('Ctrl Pts',(4.72647139029881,1.53284133217306,3.91271781506562));
#4902=CARTESIAN_POINT('Ctrl Pts',(4.73343568334681,1.51442895415891,4.01135192369608));
#4903=CARTESIAN_POINT('Ctrl Pts',(4.73871374853264,1.49374387002476,4.08863427287779));
#4904=CARTESIAN_POINT('Ctrl Pts',(4.750684797881,1.43339664767971,4.26002840439575));
#4905=CARTESIAN_POINT('Ctrl Pts',(4.75735105332211,1.39023993880161,4.35250204427422));
#4906=CARTESIAN_POINT('Ctrl Pts',(4.76659517836645,1.32141431672016,4.46870457304304));
#4907=CARTESIAN_POINT('Ctrl Pts',(4.76889899232322,1.30355572206415,4.49676381389284));
#4908=CARTESIAN_POINT('Ctrl Pts',(4.77305760987036,1.27020392361317,4.5456337947288));
#4909=CARTESIAN_POINT('Ctrl Pts',(4.77489863236737,1.25506321549494,4.56667030988139));
#4910=CARTESIAN_POINT('Ctrl Pts',(4.77896090515028,1.22089527603014,4.6117249588905));
#4911=CARTESIAN_POINT('Ctrl Pts',(4.78118949796384,1.20167003309675,4.63557838549447));
#4912=CARTESIAN_POINT('Ctrl Pts',(4.78889779482462,1.13362552026516,4.71507977555612));
#4913=CARTESIAN_POINT('Ctrl Pts',(4.79450670797288,1.08155148228075,4.76779718023151));
#4914=CARTESIAN_POINT('Ctrl Pts',(4.80862472208468,0.94372030124631,4.888738261238));
#4915=CARTESIAN_POINT('Ctrl Pts',(4.81721382787897,0.85413091192074,4.95200322046696));
#4916=CARTESIAN_POINT('Ctrl Pts',(4.82721213351643,0.737985491933357,5.01688987330132));
#4917=CARTESIAN_POINT('Ctrl Pts',(4.82897088054911,0.717064268724508,5.02795929747552));
#4918=CARTESIAN_POINT('Ctrl Pts',(4.83180750888367,0.682396168718489,5.0453013342007));
#4919=CARTESIAN_POINT('Ctrl Pts',(4.8329009139097,0.668796918936155,5.05185838695539));
#4920=CARTESIAN_POINT('Ctrl Pts',(4.83530242752549,0.638375372114797,5.06598435427532));
#4921=CARTESIAN_POINT('Ctrl Pts',(4.83660495433967,0.621510239991016,5.07345389440286));
#4922=CARTESIAN_POINT('Ctrl Pts',(4.84118905144667,0.56101894520581,5.09896826849431));
#4923=CARTESIAN_POINT('Ctrl Pts',(4.84438720824956,0.516705411285167,5.11532675360132));
#4924=CARTESIAN_POINT('Ctrl Pts',(4.85446620191945,0.37294074930458,5.16107846928913));
#4925=CARTESIAN_POINT('Ctrl Pts',(4.86116949193477,0.271274634416704,5.18256064697489));
#4926=CARTESIAN_POINT('Ctrl Pts',(4.87159525689092,0.116302225914969,5.19941957635496));
#4927=CARTESIAN_POINT('Ctrl Pts',(4.87513613217272,0.0641326501568996,5.20244889535822));
#4928=CARTESIAN_POINT('Ctrl Pts',(4.88072251576621,-0.0164446018107013,
5.20306604165799));
#4929=CARTESIAN_POINT('Ctrl Pts',(4.88271056757386,-0.0448014086357122,
5.20250768550618));
#4930=CARTESIAN_POINT('Ctrl Pts',(4.88660061734454,-0.0995476006223623,
5.19993116531816));
#4931=CARTESIAN_POINT('Ctrl Pts',(4.88849875925825,-0.125932011716523,5.19801398626185));
#4932=CARTESIAN_POINT('Ctrl Pts',(4.89323784166347,-0.190919086001194,5.1916223202721));
#4933=CARTESIAN_POINT('Ctrl Pts',(4.89610204047956,-0.229425390676273,5.18637245868275));
#4934=CARTESIAN_POINT('Ctrl Pts',(4.90261128007893,-0.315167928486089,5.17139321982818));
#4935=CARTESIAN_POINT('Ctrl Pts',(4.90627528374493,-0.362228767899446,5.16089788706049));
#4936=CARTESIAN_POINT('Ctrl Pts',(4.91631346841617,-0.48828377189565,5.12656943373389));
#4937=CARTESIAN_POINT('Ctrl Pts',(4.92275265020067,-0.565993017195498,5.09861154329901));
#4938=CARTESIAN_POINT('Ctrl Pts',(4.9324802103248,-0.681318222210005,5.04644144098251));
#4939=CARTESIAN_POINT('Ctrl Pts',(4.93583549528687,-0.720729797261556,5.02655227388476));
#4940=CARTESIAN_POINT('Ctrl Pts',(4.94047542075217,-0.775274249858286,4.99604837298498));
#4941=CARTESIAN_POINT('Ctrl Pts',(4.94182485360825,-0.791143832536963,4.98680069427455));
#4942=CARTESIAN_POINT('Ctrl Pts',(4.94425300457878,-0.819770156054677,4.9694329050093));
#4943=CARTESIAN_POINT('Ctrl Pts',(4.94533654303652,-0.832577515460654,4.96140490989313));
#4944=CARTESIAN_POINT('Ctrl Pts',(4.94809827914855,-0.865263047690833,4.94024692315991));
#4945=CARTESIAN_POINT('Ctrl Pts',(4.94975964888325,-0.884960198690081,4.92684482764504));
#4946=CARTESIAN_POINT('Ctrl Pts',(4.95351556659746,-0.929341003110109,4.89513222517167));
#4947=CARTESIAN_POINT('Ctrl Pts',(4.95559534563289,-0.953805791714416,4.87653195418727));
#4948=CARTESIAN_POINT('Ctrl Pts',(4.96342313172155,-1.04466894829505,4.80310194256126));
#4949=CARTESIAN_POINT('Ctrl Pts',(4.96902121029276,-1.10702655824849,4.74351781423349));
#4950=CARTESIAN_POINT('Ctrl Pts',(4.97912162544132,-1.20817945042595,4.62937846219486));
#4951=CARTESIAN_POINT('Ctrl Pts',(4.98356951491534,-1.24899155391738,4.57691519101357));
#4952=CARTESIAN_POINT('Ctrl Pts',(4.99024979490359,-1.30351071678685,4.49673206698423));
#4953=CARTESIAN_POINT('Ctrl Pts',(4.99238028670559,-1.31994736541699,4.47095580374915));
#4954=CARTESIAN_POINT('Ctrl Pts',(4.99637018492174,-1.34890043924445,4.42245564211075));
#4955=CARTESIAN_POINT('Ctrl Pts',(4.99822095401451,-1.36162847951736,4.39987035028918));
#4956=CARTESIAN_POINT('Ctrl Pts',(5.00254252365421,-1.38970350501572,4.34700591126335));
#4957=CARTESIAN_POINT('Ctrl Pts',(5.00502696997582,-1.40463496537909,4.31652247066382));
#4958=CARTESIAN_POINT('Ctrl Pts',(5.01380759801659,-1.45319750922058,4.20857734789363));
#4959=CARTESIAN_POINT('Ctrl Pts',(5.02026927270878,-1.48150659564499,4.1288958746411));
#4960=CARTESIAN_POINT('Ctrl Pts',(5.03432931649413,-1.52821031127595,3.95335084451619));
#4961=CARTESIAN_POINT('Ctrl Pts',(5.04192309163973,-1.54434640482295,3.85723503067018));
#4962=CARTESIAN_POINT('Ctrl Pts',(5.05064964285584,-1.5528331032241,3.74055544888774));
#4963=CARTESIAN_POINT('Ctrl Pts',(5.05210625422466,-1.55389003551992,3.72084835309325));
#4964=CARTESIAN_POINT('Ctrl Pts',(5.05424920512365,-1.5549065266014,3.69143861100837));
#4965=CARTESIAN_POINT('Ctrl Pts',(5.05495023095125,-1.55515079715118,3.68174869778304));
#4966=CARTESIAN_POINT('Ctrl Pts',(5.05622915306735,-1.55543323587685,3.6639366758968));
#4967=CARTESIAN_POINT('Ctrl Pts',(5.05680862740202,-1.55549840327986,3.65581588846268));
#4968=CARTESIAN_POINT('Ctrl Pts',(5.05738485701521,-1.55549997101641,3.64769474805265));
#4969=CARTESIAN_POINT('Origin',(1.2059437743963,0.,3.64739446828387));
#4970=CARTESIAN_POINT('',(5.89405622564623,-1.55549964733824,3.6463470282533));
#4971=CARTESIAN_POINT('',(5.7559437743963,-1.5554995134887,3.64862472695888));
#4972=CARTESIAN_POINT('',(1.2059437743963,-1.5555,3.64739446828386));
#4973=CARTESIAN_POINT('Ctrl Pts',(5.1940562256037,-1.55549955406316,3.6485723092344));
#4974=CARTESIAN_POINT('Ctrl Pts',(5.19818989105023,-1.55554339101516,3.59067963768889));
#4975=CARTESIAN_POINT('Ctrl Pts',(5.20232355649676,-1.55235092862268,3.53275114493701));
#4976=CARTESIAN_POINT('Ctrl Pts',(5.20645722194329,-1.54593674727678,3.47517419241811));
#4977=CARTESIAN_POINT('Ctrl Pts',(5.21059031289217,-1.5395234573751,3.41760524195563));
#4978=CARTESIAN_POINT('Ctrl Pts',(5.21472340384104,-1.52988939577036,3.36038825123365));
#4979=CARTESIAN_POINT('Ctrl Pts',(5.21885649478992,-1.51710097035121,3.30390517331323));
#4980=CARTESIAN_POINT('Ctrl Pts',(5.22299383790471,-1.50429938807019,3.24736398502896));
#4981=CARTESIAN_POINT('Ctrl Pts',(5.22713118101951,-1.48833707342143,3.19155872648217));
#4982=CARTESIAN_POINT('Ctrl Pts',(5.2312685241343,-1.46933126780931,3.13685957678488));
#4983=CARTESIAN_POINT('Ctrl Pts',(5.23540787466692,-1.45031624067703,3.08213388733853));
#4984=CARTESIAN_POINT('Ctrl Pts',(5.23954722519954,-1.4282549783926,3.02851585791735));
#4985=CARTESIAN_POINT('Ctrl Pts',(5.24368657573216,-1.40331301745095,2.97635585162107));
#4986=CARTESIAN_POINT('Ctrl Pts',(5.2478343970707,-1.37832001504543,2.92408910459649));
#4987=CARTESIAN_POINT('Ctrl Pts',(5.25198221840925,-1.35043478546565,2.87328680009944));
#4988=CARTESIAN_POINT('Ctrl Pts',(5.2561300397478,-1.31986857258938,2.82427406330604));
#4989=CARTESIAN_POINT('Ctrl Pts',(5.25997653088088,-1.29152292864664,2.77882199531746));
#4990=CARTESIAN_POINT('Ctrl Pts',(5.26382302201397,-1.26087236047468,2.73490888339631));
#4991=CARTESIAN_POINT('Ctrl Pts',(5.26766951314705,-1.22811608950118,2.69276830024303));
#4992=CARTESIAN_POINT('Ctrl Pts',(5.27181796799075,-1.19278833069971,2.64731952621756));
#4993=CARTESIAN_POINT('Ctrl Pts',(5.27596642283445,-1.15486031021855,2.60373928251713));
#4994=CARTESIAN_POINT('Ctrl Pts',(5.28011487767815,-1.11455708914478,2.5623402092548));
#4995=CARTESIAN_POINT('Ctrl Pts',(5.28425596954489,-1.07432540113559,2.52101461405459));
#4996=CARTESIAN_POINT('Ctrl Pts',(5.28839706141163,-1.03172724032225,2.48186287528169));
#4997=CARTESIAN_POINT('Ctrl Pts',(5.29253815327836,-0.987028147397986,2.4451650033962));
#4998=CARTESIAN_POINT('Ctrl Pts',(5.29667513386998,-0.942373431723689,2.40850356515013));
#4999=CARTESIAN_POINT('Ctrl Pts',(5.30081211446159,-0.895622316970591,2.37429149565249));
#5000=CARTESIAN_POINT('Ctrl Pts',(5.3049490950532,-0.847076184934748,2.34277107936414));
#5001=CARTESIAN_POINT('Ctrl Pts',(5.3090835578996,-0.798559597826428,2.31126984623985));
#5002=CARTESIAN_POINT('Ctrl Pts',(5.31321802074599,-0.748250594795285,2.28245730203281));
#5003=CARTESIAN_POINT('Ctrl Pts',(5.31735248359239,-0.696480755874123,2.25653329379628));
#5004=CARTESIAN_POINT('Ctrl Pts',(5.32148601862379,-0.644722534624844,2.2306151031676));
#5005=CARTESIAN_POINT('Ctrl Pts',(5.32561955365519,-0.591504593667726,2.20758439462339));
#5006=CARTESIAN_POINT('Ctrl Pts',(5.32975308868659,-0.537182444298235,2.18759473149195));
#5007=CARTESIAN_POINT('Ctrl Pts',(5.3338903560124,-0.482811245809103,2.16758701908613));
#5008=CARTESIAN_POINT('Ctrl Pts',(5.33802762333821,-0.427334335914779,2.150626020662));
#5009=CARTESIAN_POINT('Ctrl Pts',(5.34216489066402,-0.371125235975002,2.1368163308734));
#5010=CARTESIAN_POINT('Ctrl Pts',(5.34630387138358,-0.314892857790565,2.12300092198703));
#5011=CARTESIAN_POINT('Ctrl Pts',(5.35044285210315,-0.257928197727282,2.11233952072552));
#5012=CARTESIAN_POINT('Ctrl Pts',(5.35458183282272,-0.20061472232637,2.10488547862257));
#5013=CARTESIAN_POINT('Ctrl Pts',(5.35872885786935,-0.143189855166912,2.09741694919614));
#5014=CARTESIAN_POINT('Ctrl Pts',(5.36287588291597,-0.0854153389819193,
2.09316827547533));
#5015=CARTESIAN_POINT('Ctrl Pts',(5.3670229079626,-0.0276785853040992,2.09214074431612));
#5016=CARTESIAN_POINT('Ctrl Pts',(5.37091428988111,0.0264989894077606,2.09117655525801));
#5017=CARTESIAN_POINT('Ctrl Pts',(5.37480567179962,0.0806429526473318,2.09304809442987));
#5018=CARTESIAN_POINT('Ctrl Pts',(5.37869705371814,0.134437993166185,2.0977149285101));
#5019=CARTESIAN_POINT('Ctrl Pts',(5.38284535886403,0.191784778467865,2.10268988399774));
#5020=CARTESIAN_POINT('Ctrl Pts',(5.38699366400992,0.248975180305846,2.11086278502762));
#5021=CARTESIAN_POINT('Ctrl Pts',(5.39114196915581,0.30562447496996,2.12221450175555));
#5022=CARTESIAN_POINT('Ctrl Pts',(5.39528291111001,0.362173217817999,2.13354606932294));
#5023=CARTESIAN_POINT('Ctrl Pts',(5.3994238530642,0.418182253502628,2.14804515179915));
#5024=CARTESIAN_POINT('Ctrl Pts',(5.4035647950184,0.473272264851125,2.16564090803079));
#5025=CARTESIAN_POINT('Ctrl Pts',(5.40770162566673,0.528307580459115,2.18321919443635));
#5026=CARTESIAN_POINT('Ctrl Pts',(5.41183845631507,0.58242518603099,2.20388790541525));
#5027=CARTESIAN_POINT('Ctrl Pts',(5.4159752869634,0.63525797006916,2.2275256146697));
#5028=CARTESIAN_POINT('Ctrl Pts',(5.42010960008704,0.6880586019962,2.25114893887388));
#5029=CARTESIAN_POINT('Ctrl Pts',(5.42424391321067,0.739575487986191,2.27773746746319));
#5030=CARTESIAN_POINT('Ctrl Pts',(5.42837822633431,0.789460743674109,2.30712136768179));
#5031=CARTESIAN_POINT('Ctrl Pts',(5.43251161211457,0.839334809894721,2.33649867697113));
#5032=CARTESIAN_POINT('Ctrl Pts',(5.43664499789482,0.887577523941647,2.36866984892292));
#5033=CARTESIAN_POINT('Ctrl Pts',(5.44077838367508,0.933866862659701,2.40341981708469));
#5034=CARTESIAN_POINT('Ctrl Pts',(5.44491550368043,0.980198020559258,2.43820117941337));
#5035=CARTESIAN_POINT('Ctrl Pts',(5.44905262368578,1.02457185839104,2.47556568122312));
#5036=CARTESIAN_POINT('Ctrl Pts',(5.45318974369113,1.06669768505829,2.51525653556928));
#5037=CARTESIAN_POINT('Ctrl Pts',(5.45732857790152,1.10884096645357,2.55496383571892));
#5038=CARTESIAN_POINT('Ctrl Pts',(5.46146741211191,1.14873401962117,2.59699903237818));
#5039=CARTESIAN_POINT('Ctrl Pts',(5.46560624632231,1.18612377654655,2.6410691547242));
#5040=CARTESIAN_POINT('Ctrl Pts',(5.4697531281496,1.22358623472658,2.68522496773663));
#5041=CARTESIAN_POINT('Ctrl Pts',(5.4739000099769,1.25853535357738,2.73142319730464));
#5042=CARTESIAN_POINT('Ctrl Pts',(5.4780468918042,1.29075963708495,2.77933928036531));
#5043=CARTESIAN_POINT('Ctrl Pts',(5.48193945929921,1.3210077135326,2.82431683101126));
#5044=CARTESIAN_POINT('Ctrl Pts',(5.48583202679421,1.34885515567857,2.87080740986868));
#5045=CARTESIAN_POINT('Ctrl Pts',(5.48972459428922,1.3741645240919,2.91852403348268));
#5046=CARTESIAN_POINT('Ctrl Pts',(5.49387311339754,1.40113808296194,2.96937821265901));
#5047=CARTESIAN_POINT('Ctrl Pts',(5.49802163250585,1.42534134831132,3.02183823319594));
#5048=CARTESIAN_POINT('Ctrl Pts',(5.50217015161417,1.44658140734486,3.07557064758019));
#5049=CARTESIAN_POINT('Ctrl Pts',(5.50631130597707,1.46778375951884,3.12920767237063));
#5050=CARTESIAN_POINT('Ctrl Pts',(5.51045246033997,1.48603315695587,3.18411212726835));
#5051=CARTESIAN_POINT('Ctrl Pts',(5.51459361470287,1.50118304248143,3.23992701809158));
#5052=CARTESIAN_POINT('Ctrl Pts',(5.51873065667904,1.51631788336419,3.29568648175706));
#5053=CARTESIAN_POINT('Ctrl Pts',(5.52286769865521,1.52835917507792,3.35235409006662));
#5054=CARTESIAN_POINT('Ctrl Pts',(5.52700474063139,1.53720946298209,3.40955562175472));
#5055=CARTESIAN_POINT('Ctrl Pts',(5.53113926366132,1.54605436215693,3.46672232479381));
#5056=CARTESIAN_POINT('Ctrl Pts',(5.53527378669126,1.55171202954511,3.52442179328069));
#5057=CARTESIAN_POINT('Ctrl Pts',(5.5394083097212,1.5541360973046,3.58226965692266));
#5058=CARTESIAN_POINT('Ctrl Pts',(5.54354190364442,1.55655962032951,3.6401045210389));
#5059=CARTESIAN_POINT('Ctrl Pts',(5.54767549756765,1.55575096456502,3.69808719414855));
#5060=CARTESIAN_POINT('Ctrl Pts',(5.55180909149087,1.5517157883933,3.75583044963218));
#5061=CARTESIAN_POINT('Ctrl Pts',(5.55594641523553,1.54767697120437,3.81362580796774));
#5062=CARTESIAN_POINT('Ctrl Pts',(5.56008373898019,1.54040585086493,3.87118079622951));
#5063=CARTESIAN_POINT('Ctrl Pts',(5.56422106272485,1.52996013383855,3.92811183302058));
#5064=CARTESIAN_POINT('Ctrl Pts',(5.56836009860536,1.51951009409348,3.98506642940609));
#5065=CARTESIAN_POINT('Ctrl Pts',(5.57249913448588,1.50588296008869,4.04139605210127));
#5066=CARTESIAN_POINT('Ctrl Pts',(5.5766381703664,1.48918725521302,4.09672905287659));
#5067=CARTESIAN_POINT('Ctrl Pts',(5.58078524774395,1.47245911320341,4.15216955698711));
#5068=CARTESIAN_POINT('Ctrl Pts',(5.5849323251215,1.45265066422468,4.20660907835341));
#5069=CARTESIAN_POINT('Ctrl Pts',(5.58907940249905,1.4299195384331,4.25969371179743));
#5070=CARTESIAN_POINT('Ctrl Pts',(5.59297031328613,1.40859252316597,4.30949928668583));
#5071=CARTESIAN_POINT('Ctrl Pts',(5.59686122407321,1.38469337269004,4.35811207240157));
#5072=CARTESIAN_POINT('Ctrl Pts',(5.60075213486029,1.35838814834895,4.40526113757677));
#5073=CARTESIAN_POINT('Ctrl Pts',(5.60490076102295,1.33034059139177,4.45553313198486));
#5074=CARTESIAN_POINT('Ctrl Pts',(5.60904938718561,1.29943983349391,4.50435122582026));
#5075=CARTESIAN_POINT('Ctrl Pts',(5.61319801334826,1.26586108932031,4.55137231787135));
#5076=CARTESIAN_POINT('Ctrl Pts',(5.61733927881018,1.23234192223975,4.5983099827412));
#5077=CARTESIAN_POINT('Ctrl Pts',(5.6214805442721,1.19615449993237,4.64345655405967));
#5078=CARTESIAN_POINT('Ctrl Pts',(5.62562180973402,1.15751898488018,4.68649506478161));
#5079=CARTESIAN_POINT('Ctrl Pts',(5.62975896518301,1.11892181377581,4.72949086178775));
#5080=CARTESIAN_POINT('Ctrl Pts',(5.63389612063199,1.07788170981579,4.77038235794146));
#5081=CARTESIAN_POINT('Ctrl Pts',(5.63803327608097,1.03465996895198,4.80888445904931));
#5082=CARTESIAN_POINT('Ctrl Pts',(5.64216791473878,0.991464521539555,4.84736313784459));
#5083=CARTESIAN_POINT('Ctrl Pts',(5.6463025533966,0.946090456058802,4.88345495740182));
#5084=CARTESIAN_POINT('Ctrl Pts',(5.65043719205441,0.898835336805132,4.91691220636806));
#5085=CARTESIAN_POINT('Ctrl Pts',(5.65457090354483,0.851590814222553,4.95036195275112));
#5086=CARTESIAN_POINT('Ctrl Pts',(5.65870461503524,0.802466500010036,4.98117800074397));
#5087=CARTESIAN_POINT('Ctrl Pts',(5.66283832652566,0.751790614076111,5.0091547711959));
#5088=CARTESIAN_POINT('Ctrl Pts',(5.66697576989225,0.701068978425046,5.03715679881524));
#5089=CARTESIAN_POINT('Ctrl Pts',(5.67111321325884,0.648793428175627,5.06231417327505));
#5090=CARTESIAN_POINT('Ctrl Pts',(5.67525065662543,0.595317392221242,5.08446699690548));
#5091=CARTESIAN_POINT('Ctrl Pts',(5.67938981344787,0.541819210023769,5.10662899477271));
#5092=CARTESIAN_POINT('Ctrl Pts',(5.68352897027031,0.487120043009846,5.12578378759081));
#5093=CARTESIAN_POINT('Ctrl Pts',(5.68766812709275,0.431590901758435,5.14182062688768));
#5094=CARTESIAN_POINT('Ctrl Pts',(5.69181532602098,0.375953871087131,5.15788862469429));
#5095=CARTESIAN_POINT('Ctrl Pts',(5.69596252494921,0.319484152727989,5.17082644518598));
#5096=CARTESIAN_POINT('Ctrl Pts',(5.70010972387744,0.26256453222091,5.18057420869907));
#5097=CARTESIAN_POINT('Ctrl Pts',(5.70399970772875,0.209175146173399,5.18971740228792));
#5098=CARTESIAN_POINT('Ctrl Pts',(5.70788969158006,0.155390369769301,5.19605443380859));
#5099=CARTESIAN_POINT('Ctrl Pts',(5.71177967543137,0.101527643020569,5.19957757207758));
#5100=CARTESIAN_POINT('Ctrl Pts',(5.71592728595477,0.0440976842286693,5.20333404149196));
#5101=CARTESIAN_POINT('Ctrl Pts',(5.72007489647816,-0.0136615881029595,
5.20390677509005));
#5102=CARTESIAN_POINT('Ctrl Pts',(5.72422250700156,-0.0713670981046394,
5.20125642718116));
#5103=CARTESIAN_POINT('Ctrl Pts',(5.72836275413177,-0.128970161563501,5.19861078452452));
#5104=CARTESIAN_POINT('Ctrl Pts',(5.73250300126198,-0.186519136065158,5.1927534414133));
#5105=CARTESIAN_POINT('Ctrl Pts',(5.73664324839219,-0.243628457187391,5.18369698564446));
#5106=CARTESIAN_POINT('Ctrl Pts',(5.74077938455052,-0.300681072802417,5.17464952229416));
#5107=CARTESIAN_POINT('Ctrl Pts',(5.74491552070884,-0.357294388064169,5.16240932097463));
#5108=CARTESIAN_POINT('Ctrl Pts',(5.74905165686716,-0.413087244050113,5.14704081952908));
#5109=CARTESIAN_POINT('Ctrl Pts',(5.75318527698905,-0.468846160907,5.13168166683518));
#5110=CARTESIAN_POINT('Ctrl Pts',(5.75731889711093,-0.523785106630128,5.11319812425796));
#5111=CARTESIAN_POINT('Ctrl Pts',(5.76145251723282,-0.577534600719312,5.09170538874802));
#5112=CARTESIAN_POINT('Ctrl Pts',(5.7655852126536,-0.631272070913043,5.07021746121644));
#5113=CARTESIAN_POINT('Ctrl Pts',(5.76971790807439,-0.683820134277736,5.045721870491));
#5114=CARTESIAN_POINT('Ctrl Pts',(5.77385060349517,-0.734828029057465,5.01838243967951));
#5115=CARTESIAN_POINT('Ctrl Pts',(5.77798704277871,-0.785882132555135,4.99101824172064));
#5116=CARTESIAN_POINT('Ctrl Pts',(5.78212348206224,-0.835392818450879,4.960805301017));
#5117=CARTESIAN_POINT('Ctrl Pts',(5.78625992134577,-0.883033984203595,4.92795342153106));
#5118=CARTESIAN_POINT('Ctrl Pts',(5.79039807897013,-0.930694940833091,4.89508789486649));
#5119=CARTESIAN_POINT('Ctrl Pts',(5.79453623659449,-0.97648441580041,4.85958156294093));
#5120=CARTESIAN_POINT('Ctrl Pts',(5.79867439421885,-1.02010802560609,4.82168568688939));
#5121=CARTESIAN_POINT('Ctrl Pts',(5.80282061530434,-1.06381663876689,4.78371596833321));
#5122=CARTESIAN_POINT('Ctrl Pts',(5.80696683638983,-1.10535057742057,4.74334776458121));
#5123=CARTESIAN_POINT('Ctrl Pts',(5.81111305747532,-1.14445177490562,4.70086985238897));
#5124=CARTESIAN_POINT('Ctrl Pts',(5.8150111103177,-1.18121260623954,4.66093441649565));
#5125=CARTESIAN_POINT('Ctrl Pts',(5.81890916316007,-1.21582333906808,4.61913487527536));
#5126=CARTESIAN_POINT('Ctrl Pts',(5.82280721600245,-1.24810396751099,4.57573531963284));
#5127=CARTESIAN_POINT('Ctrl Pts',(5.82697531032831,-1.28262086856104,4.52932921665444));
#5128=CARTESIAN_POINT('Ctrl Pts',(5.83114340465418,-1.3146187716897,4.48089784141534));
#5129=CARTESIAN_POINT('Ctrl Pts',(5.83531149898004,-1.34385418886963,4.43074379588781));
#5130=CARTESIAN_POINT('Ctrl Pts',(5.83947293308479,-1.3730428906138,4.38066989178867));
#5131=CARTESIAN_POINT('Ctrl Pts',(5.84363436718954,-1.3994776017878,4.32887921504193));
#5132=CARTESIAN_POINT('Ctrl Pts',(5.84779580129429,-1.4229568142114,4.27570502437007));
#5133=CARTESIAN_POINT('Ctrl Pts',(5.85195179078339,-1.44640530758853,4.22260040419334));
#5134=CARTESIAN_POINT('Ctrl Pts',(5.85610778027248,-1.46690577030666,4.16811633035365));
#5135=CARTESIAN_POINT('Ctrl Pts',(5.86026376976158,-1.48430262546907,4.11261051059714));
#5136=CARTESIAN_POINT('Ctrl Pts',(5.86441651567438,-1.50168590311234,4.05714801081562));
#5137=CARTESIAN_POINT('Ctrl Pts',(5.86856926158719,-1.51597022498911,4.00066583607906));
#5138=CARTESIAN_POINT('Ctrl Pts',(5.8727220075,-1.52704887102889,3.94353969530837));
#5139=CARTESIAN_POINT('Ctrl Pts',(5.87687406419901,-1.53812567839231,3.88642303552336));
#5140=CARTESIAN_POINT('Ctrl Pts',(5.88102612089801,-1.54599775636006,3.82866312385761));
#5141=CARTESIAN_POINT('Ctrl Pts',(5.88517817759702,-1.55060925665613,3.77064698619864));
#5142=CARTESIAN_POINT('Ctrl Pts',(5.88813752693258,-1.55389607119803,3.72929639036649));
#5143=CARTESIAN_POINT('Ctrl Pts',(5.89109687626814,-1.55552757156221,3.68781588946899));
#5144=CARTESIAN_POINT('Ctrl Pts',(5.8940562256037,-1.55549964733864,3.64634702884923));
#5145=CARTESIAN_POINT('Ctrl Pts',(5.05594377443823,-1.5554999873946,3.64759249708933));
#5146=CARTESIAN_POINT('Ctrl Pts',(5.06007749260067,-1.55550729033478,3.59022850230279));
#5147=CARTESIAN_POINT('Ctrl Pts',(5.06421121076312,-1.55233707856484,3.53274024496005));
#5148=CARTESIAN_POINT('Ctrl Pts',(5.06834492892557,-1.54597416002809,3.47551036045114));
#5149=CARTESIAN_POINT('Ctrl Pts',(5.07247136321427,-1.53962245335762,3.41838131863085));
#5150=CARTESIAN_POINT('Ctrl Pts',(5.07659779750297,-1.53008926129689,3.36151026343839));
#5151=CARTESIAN_POINT('Ctrl Pts',(5.08072423179167,-1.51741138191812,3.30527906666425));
#5152=CARTESIAN_POINT('Ctrl Pts',(5.08484662303307,-1.50474592422411,3.24910296476677));
#5153=CARTESIAN_POINT('Ctrl Pts',(5.08896901427447,-1.48894199726885,3.19356598886568));
#5154=CARTESIAN_POINT('Ctrl Pts',(5.09309140551587,-1.47008786542628,3.13904230892346));
#5155=CARTESIAN_POINT('Ctrl Pts',(5.09721137132577,-1.45124482651565,3.08455070828753));
#5156=CARTESIAN_POINT('Ctrl Pts',(5.10133133713566,-1.42935531067887,3.03107171707736));
#5157=CARTESIAN_POINT('Ctrl Pts',(5.10545130294555,-1.40455747949944,2.97896456411876));
#5158=CARTESIAN_POINT('Ctrl Pts',(5.10957045738072,-1.37976453193662,2.92686767299941));
#5159=CARTESIAN_POINT('Ctrl Pts',(5.11368961181589,-1.35206463182605,2.87614255733836));
#5160=CARTESIAN_POINT('Ctrl Pts',(5.11780876625106,-1.32164322904374,2.82712656989771));
#5161=CARTESIAN_POINT('Ctrl Pts',(5.12193169705873,-1.29119393642367,2.77806564541236));
#5162=CARTESIAN_POINT('Ctrl Pts',(5.1260546278664,-1.25801843387567,2.73071742648835));
#5163=CARTESIAN_POINT('Ctrl Pts',(5.13017755867406,-1.22234637900808,2.68539156822284));
#5164=CARTESIAN_POINT('Ctrl Pts',(5.13430235332377,-1.18665819797236,2.64004521962074));
#5165=CARTESIAN_POINT('Ctrl Pts',(5.13842714797347,-1.14847156347865,2.59672344769724));
#5166=CARTESIAN_POINT('Ctrl Pts',(5.14255194262318,-1.10805533127382,2.55570145610706));
#5167=CARTESIAN_POINT('Ctrl Pts',(5.14668451858051,-1.06756285499803,2.51460207769811));
#5168=CARTESIAN_POINT('Ctrl Pts',(5.15081709453784,-1.02483276916801,2.47581149899195));
#5169=CARTESIAN_POINT('Ctrl Pts',(5.15494967049517,-0.98016873643688,2.43956604581993));
#5170=CARTESIAN_POINT('Ctrl Pts',(5.15818677156541,-0.945182812488239,2.41117450590248));
#5171=CARTESIAN_POINT('Ctrl Pts',(5.16142387263565,-0.90901099518197,2.38434383327531));
#5172=CARTESIAN_POINT('Ctrl Pts',(5.16466097370589,-0.87181086109517,2.35916852828868));
#5173=CARTESIAN_POINT('Ctrl Pts',(5.16880939807082,-0.824137977463928,2.32690575788553));
#5174=CARTESIAN_POINT('Ctrl Pts',(5.17295782243574,-0.774571930974871,2.29722530939671));
#5175=CARTESIAN_POINT('Ctrl Pts',(5.17710624680067,-0.723423584423073,2.27035468400003));
#5176=CARTESIAN_POINT('Ctrl Pts',(5.18124730790192,-0.672366023849053,2.24353175273551));
#5177=CARTESIAN_POINT('Ctrl Pts',(5.18538836900317,-0.619732194895642,2.2195089855796));
#5178=CARTESIAN_POINT('Ctrl Pts',(5.18952943010441,-0.565861335505651,2.19847031603167));
#5179=CARTESIAN_POINT('Ctrl Pts',(5.19366637977742,-0.51204396148264,2.17745253460347));
#5180=CARTESIAN_POINT('Ctrl Pts',(5.19780332945043,-0.456992472997546,2.15941316913124));
#5181=CARTESIAN_POINT('Ctrl Pts',(5.20194027912344,-0.401068493576879,2.14448917736898));
#5182=CARTESIAN_POINT('Ctrl Pts',(5.20607471095171,-0.345178550803598,2.12957426869863));
#5183=CARTESIAN_POINT('Ctrl Pts',(5.21020914277998,-0.28841767179534,2.11777110909837));
#5184=CARTESIAN_POINT('Ctrl Pts',(5.21434357460825,-0.231163040437644,2.10916694976276));
#5185=CARTESIAN_POINT('Ctrl Pts',(5.2184770785754,-0.173921258329485,2.1005647213974));
#5186=CARTESIAN_POINT('Ctrl Pts',(5.22261058254255,-0.116186458521795,2.09516014532916));
#5187=CARTESIAN_POINT('Ctrl Pts',(5.2267440865097,-0.0583442347286329,2.09298905132408));
#5188=CARTESIAN_POINT('Ctrl Pts',(5.23088132294986,-0.000449780542021196,
2.09081599686371));
#5189=CARTESIAN_POINT('Ctrl Pts',(5.23501855939001,0.0575517699355676,2.09188227998785));
#5190=CARTESIAN_POINT('Ctrl Pts',(5.23915579583016,0.115272874994651,2.09617159123155));
#5191=CARTESIAN_POINT('Ctrl Pts',(5.24329474571062,0.17301788530289,2.10046267889748));
#5192=CARTESIAN_POINT('Ctrl Pts',(5.24743369559108,0.230481701072782,2.1079793893101));
#5193=CARTESIAN_POINT('Ctrl Pts',(5.25157264547153,0.287283205458235,2.11865361062956));
#5194=CARTESIAN_POINT('Ctrl Pts',(5.25571964016397,0.344195114037021,2.12934857926561));
#5195=CARTESIAN_POINT('Ctrl Pts',(5.2598666348564,0.400441631038254,2.143213199152));
#5196=CARTESIAN_POINT('Ctrl Pts',(5.26401362954884,0.455654023892158,2.16012863444283));
#5197=CARTESIAN_POINT('Ctrl Pts',(5.26790525779155,0.507466510599637,2.17600243959517));
#5198=CARTESIAN_POINT('Ctrl Pts',(5.27179688603426,0.558368129507118,2.19456229161852));
#5199=CARTESIAN_POINT('Ctrl Pts',(5.27568851427696,0.608071567144026,2.21567200242989));
#5200=CARTESIAN_POINT('Ctrl Pts',(5.27983691690473,0.661054498308648,2.23817455774597));
#5201=CARTESIAN_POINT('Ctrl Pts',(5.28398531953249,0.712897604072687,2.26366927627787));
#5202=CARTESIAN_POINT('Ctrl Pts',(5.28813372216025,0.763241019271921,2.2920187283133));
#5203=CARTESIAN_POINT('Ctrl Pts',(5.29227476151772,0.813495076661168,2.32031786105796));
#5204=CARTESIAN_POINT('Ctrl Pts',(5.29641580087518,0.862254277030835,2.35146141648703));
#5205=CARTESIAN_POINT('Ctrl Pts',(5.30055684023265,0.909179922442309,2.38526447552251));
#5206=CARTESIAN_POINT('Ctrl Pts',(5.30469376817226,0.956058977874934,2.41903397329758));
#5207=CARTESIAN_POINT('Ctrl Pts',(5.30883069611188,1.00110766483917,2.4554574402608));
#5208=CARTESIAN_POINT('Ctrl Pts',(5.3129676240515,1.04401456758386,2.49430564574127));
#5209=CARTESIAN_POINT('Ctrl Pts',(5.31710203419302,1.08689535652629,2.53313020760517));
#5210=CARTESIAN_POINT('Ctrl Pts',(5.32123644433453,1.12763656001703,2.57437623387099));
#5211=CARTESIAN_POINT('Ctrl Pts',(5.32537085447605,1.1659600447182,2.6177744295702));
#5212=CARTESIAN_POINT('Ctrl Pts',(5.32950433683933,1.20427492947547,2.66116288653999));
#5213=CARTESIAN_POINT('Ctrl Pts',(5.3336378192026,1.24017282806972,2.70670216401733));
#5214=CARTESIAN_POINT('Ctrl Pts',(5.33777130156588,1.2734142134817,2.75408797502258));
#5215=CARTESIAN_POINT('Ctrl Pts',(5.34190851670423,1.30668561779882,2.80151657817226));
#5216=CARTESIAN_POINT('Ctrl Pts',(5.34604573184259,1.33729541416731,2.85079462055169));
#5217=CARTESIAN_POINT('Ctrl Pts',(5.35018294698094,1.3650467945119,2.90158785877121));
#5218=CARTESIAN_POINT('Ctrl Pts',(5.35432187568943,1.39280966904645,2.9524021347597));
#5219=CARTESIAN_POINT('Ctrl Pts',(5.35846080439792,1.41771154198748,3.00473238704078));
#5220=CARTESIAN_POINT('Ctrl Pts',(5.36259973310641,1.43960258938017,3.05822162891506));
#5221=CARTESIAN_POINT('Ctrl Pts',(5.36674670712333,1.46153618890178,3.1118148439376));
#5222=CARTESIAN_POINT('Ctrl Pts',(5.37089368114024,1.48044709586661,3.16657105698239));
#5223=CARTESIAN_POINT('Ctrl Pts',(5.37504065515716,1.49623480202497,3.22211612741838));
#5224=CARTESIAN_POINT('Ctrl Pts',(5.37893245505412,1.51105104947425,3.27424336489753));
#5225=CARTESIAN_POINT('Ctrl Pts',(5.38282425495108,1.52311703828431,3.32706488305068));
#5226=CARTESIAN_POINT('Ctrl Pts',(5.38671605484805,1.53239104897987,3.3802654301649));
#5227=CARTESIAN_POINT('Ctrl Pts',(5.39086448300385,1.54227659502676,3.43697406200514));
#5228=CARTESIAN_POINT('Ctrl Pts',(5.39501291115965,1.54903070265895,3.49435094749466));
#5229=CARTESIAN_POINT('Ctrl Pts',(5.39916133931546,1.55257329113124,3.55201928458327));
#5230=CARTESIAN_POINT('Ctrl Pts',(5.40330240395167,1.55610959145807,3.60958525954483));
#5231=CARTESIAN_POINT('Ctrl Pts',(5.40744346858788,1.55644565569209,3.6674411438386));
#5232=CARTESIAN_POINT('Ctrl Pts',(5.41158453322409,1.55355277362111,3.7252021129864));
#5233=CARTESIAN_POINT('Ctrl Pts',(5.41572148627486,1.55066276383851,3.78290573235077));
#5234=CARTESIAN_POINT('Ctrl Pts',(5.41985843932563,1.54455018566779,3.84051410586875));
#5235=CARTESIAN_POINT('Ctrl Pts',(5.42399539237639,1.53523835277221,3.89764124683911));
#5236=CARTESIAN_POINT('Ctrl Pts',(5.42812982742146,1.52593218763452,3.95473361669534));
#5237=CARTESIAN_POINT('Ctrl Pts',(5.43226426246652,1.51343071143482,4.01134482177348));
#5238=CARTESIAN_POINT('Ctrl Pts',(5.43639869751159,1.49780895477388,4.06709505798939));
#5239=CARTESIAN_POINT('Ctrl Pts',(5.44053220453062,1.48219070461306,4.12283278036237));
#5240=CARTESIAN_POINT('Ctrl Pts',(5.44466571154965,1.46345370489618,4.17770941640907));
#5241=CARTESIAN_POINT('Ctrl Pts',(5.44879921856868,1.44172333621154,4.23135856976878));
#5242=CARTESIAN_POINT('Ctrl Pts',(5.45293645778093,1.41997334691554,4.28505616359459));
#5243=CARTESIAN_POINT('Ctrl Pts',(5.45707369699318,1.39522478243109,4.33752357571333));
#5244=CARTESIAN_POINT('Ctrl Pts',(5.46121093620544,1.36765137923423,4.38841400573123));
#5245=CARTESIAN_POINT('Ctrl Pts',(5.46534988870973,1.34006655748271,4.43932551022996));
#5246=CARTESIAN_POINT('Ctrl Pts',(5.46948884121402,1.30965483767951,4.48865828586473));
#5247=CARTESIAN_POINT('Ctrl Pts',(5.4736277937183,1.27663457277861,4.53609262715806));
#5248=CARTESIAN_POINT('Ctrl Pts',(5.47777479075219,1.24355012920017,4.583619162542));
#5249=CARTESIAN_POINT('Ctrl Pts',(5.48192178778607,1.20784733002492,4.62923947777156));
#5250=CARTESIAN_POINT('Ctrl Pts',(5.48606878481995,1.16978571820354,4.67266595598215));
#5251=CARTESIAN_POINT('Ctrl Pts',(5.48996038835301,1.13406813706523,4.71341800732238));
#5252=CARTESIAN_POINT('Ctrl Pts',(5.49385199188607,1.09627396077849,4.7522381990619));
#5253=CARTESIAN_POINT('Ctrl Pts',(5.49774359541912,1.05664517948853,4.78892029570244));
#5254=CARTESIAN_POINT('Ctrl Pts',(5.50189205063471,1.01440083906867,4.82802346585695));
#5255=CARTESIAN_POINT('Ctrl Pts',(5.50604050585029,0.969894475223361,4.86486035709219));
#5256=CARTESIAN_POINT('Ctrl Pts',(5.51018896106588,0.923398966675619,4.89915906210429));
#5257=CARTESIAN_POINT('Ctrl Pts',(5.51433005330703,0.876985981675375,4.93339689132644));
#5258=CARTESIAN_POINT('Ctrl Pts',(5.51847114554817,0.828591275070482,4.96510516952081));
#5259=CARTESIAN_POINT('Ctrl Pts',(5.52261223778932,0.778522364130185,4.99405076390987));
#5260=CARTESIAN_POINT('Ctrl Pts',(5.52674921875662,0.728503161574032,5.02296762113054));
#5261=CARTESIAN_POINT('Ctrl Pts',(5.53088619972392,0.676813496421476,5.04912696958262));
#5262=CARTESIAN_POINT('Ctrl Pts',(5.53502318069122,0.623790119403851,5.07233872576699));
#5263=CARTESIAN_POINT('Ctrl Pts',(5.53915764391395,0.570799012131047,5.09553635540019));
#5264=CARTESIAN_POINT('Ctrl Pts',(5.54329210713667,0.516476278018534,5.11578974041628));
#5265=CARTESIAN_POINT('Ctrl Pts',(5.54742657035939,0.461181567724821,5.1329555782995));
#5266=CARTESIAN_POINT('Ctrl Pts',(5.55156010576712,0.405899266118407,5.15011756399662));
#5267=CARTESIAN_POINT('Ctrl Pts',(5.55569364117484,0.349645918398539,5.16419322383587));
#5268=CARTESIAN_POINT('Ctrl Pts',(5.55982717658257,0.292797266398232,5.17508881297122));
#5269=CARTESIAN_POINT('Ctrl Pts',(5.5639644442817,0.23589728406829,5.18599424005633));
#5270=CARTESIAN_POINT('Ctrl Pts',(5.56810171198083,0.178401435691303,5.19371375896983));
#5271=CARTESIAN_POINT('Ctrl Pts',(5.57223897967996,0.120695275443563,5.19820486948887));
#5272=CARTESIAN_POINT('Ctrl Pts',(5.57637796077182,0.0629652169802013,5.2026978399398));
#5273=CARTESIAN_POINT('Ctrl Pts',(5.58051694186368,0.00502519466772049,
5.2039597239652));
#5274=CARTESIAN_POINT('Ctrl Pts',(5.58465592295554,-0.052737752275355,5.2020001994855));
#5275=CARTESIAN_POINT('Ctrl Pts',(5.58880294836785,-0.110612964446214,5.20003686657022));
#5276=CARTESIAN_POINT('Ctrl Pts',(5.59294997378016,-0.168309892939789,5.19483965925702));
#5277=CARTESIAN_POINT('Ctrl Pts',(5.59709699919246,-0.225446067434026,5.18647026910673));
#5278=CARTESIAN_POINT('Ctrl Pts',(5.60098837812504,-0.279060039765914,5.17861681626492));
#5279=CARTESIAN_POINT('Ctrl Pts',(5.60487975705762,-0.332179991546574,5.16797080129299));
#5280=CARTESIAN_POINT('Ctrl Pts',(5.6087711359902,-0.384501375266137,5.15462336344825));
#5281=CARTESIAN_POINT('Ctrl Pts',(5.61291944031003,-0.440277239262854,5.14039467099006));
#5282=CARTESIAN_POINT('Ctrl Pts',(5.61706774462986,-0.495379075984277,5.12303596400892));
#5283=CARTESIAN_POINT('Ctrl Pts',(5.62121604894968,-0.549430385441002,5.1026286424133));
#5284=CARTESIAN_POINT('Ctrl Pts',(5.62535699007877,-0.603385754467424,5.08225754357037));
#5285=CARTESIAN_POINT('Ctrl Pts',(5.62949793120785,-0.656293814205497,5.05884875313523));
#5286=CARTESIAN_POINT('Ctrl Pts',(5.63363887233693,-0.707791803328169,5.03253381619853));
#5287=CARTESIAN_POINT('Ctrl Pts',(5.63777570216127,-0.759238663028705,5.00624500586488));
#5288=CARTESIAN_POINT('Ctrl Pts',(5.64191253198561,-0.809277764543035,4.97705600153309));
#5289=CARTESIAN_POINT('Ctrl Pts',(5.64604936180995,-0.857566610935389,4.9451462773016));
#5290=CARTESIAN_POINT('Ctrl Pts',(5.65018367411206,-0.905826070514834,4.9132559721527));
#5291=CARTESIAN_POINT('Ctrl Pts',(5.65431798641418,-0.952336952841748,4.87864851574978));
#5292=CARTESIAN_POINT('Ctrl Pts',(5.65845229871629,-0.996783599410652,4.84154802036415));
#5293=CARTESIAN_POINT('Ctrl Pts',(5.66258568367884,-1.04122027645361,4.8044558467391));
#5294=CARTESIAN_POINT('Ctrl Pts',(5.66671906864139,-1.0835932373993,4.76487207783195));
#5295=CARTESIAN_POINT('Ctrl Pts',(5.67085245360394,-1.12361969242601,4.72306125534782));
#5296=CARTESIAN_POINT('Ctrl Pts',(5.67498957280401,-1.16368230868409,4.68121265957538));
#5297=CARTESIAN_POINT('Ctrl Pts',(5.67912669200407,-1.20139382085462,4.63713336577384));
#5298=CARTESIAN_POINT('Ctrl Pts',(5.68326381120414,-1.23650913495909,4.5911239894724));
#5299=CARTESIAN_POINT('Ctrl Pts',(5.68740264461471,-1.27163899905286,4.54509554923974));
#5300=CARTESIAN_POINT('Ctrl Pts',(5.69154147802527,-1.30417022656221,4.49713586336789));
#5301=CARTESIAN_POINT('Ctrl Pts',(5.69568031143583,-1.33390072694455,4.44757513579391));
#5302=CARTESIAN_POINT('Ctrl Pts',(5.69982719248294,-1.36368903595013,4.39791804127718));
#5303=CARTESIAN_POINT('Ctrl Pts',(5.70397407353005,-1.39066549083395,4.34665414594301));
#5304=CARTESIAN_POINT('Ctrl Pts',(5.70812095457716,-1.41467415468538,4.2941380697715));
#5305=CARTESIAN_POINT('Ctrl Pts',(5.71201352857186,-1.43721048970298,4.2448425365534));
#5306=CARTESIAN_POINT('Ctrl Pts',(5.71590610256657,-1.45713220257551,4.19444423214096));
#5307=CARTESIAN_POINT('Ctrl Pts',(5.71979867656128,-1.47435032060801,4.14324866270301));
#5308=CARTESIAN_POINT('Ctrl Pts',(5.7247075388849,-1.49606381173456,4.07868675526277));
#5309=CARTESIAN_POINT('Ctrl Pts',(5.72961640120853,-1.51355274598842,4.01263698113696));
#5310=CARTESIAN_POINT('Ctrl Pts',(5.73452526353215,-1.52664550808754,3.94561207781779));
#5311=CARTESIAN_POINT('Ctrl Pts',(5.73937986058867,-1.53959353558512,3.879328104686));
#5312=CARTESIAN_POINT('Ctrl Pts',(5.7442344576452,-1.54824196854562,3.81209054589745));
#5313=CARTESIAN_POINT('Ctrl Pts',(5.74908905470172,-1.55247128364616,3.74441592701353));
#5314=CARTESIAN_POINT('Ctrl Pts',(5.75137396126658,-1.55446188960699,3.71256360659188));
#5315=CARTESIAN_POINT('Ctrl Pts',(5.75365886783144,-1.55547421228667,3.68061475333113));
#5316=CARTESIAN_POINT('Ctrl Pts',(5.7559437743963,-1.5554995134887,3.64862472695888));
#5317=CARTESIAN_POINT('Origin',(1.2059437743963,0.,3.64739446828387));
#5318=CARTESIAN_POINT('',(6.5940562256037,-1.55549999978822,3.64736879997355));
#5319=CARTESIAN_POINT('',(6.4559437743963,-1.55498804050902,3.64654572419703));
#5320=CARTESIAN_POINT('',(1.2059437743963,-1.5555,3.64739446828386));
#5321=CARTESIAN_POINT('Ctrl Pts',(5.89405622564623,-1.55549964733824,3.64634702825331));
#5322=CARTESIAN_POINT('Ctrl Pts',(5.89876645506611,-1.55545520190131,3.58034338179285));
#5323=CARTESIAN_POINT('Ctrl Pts',(5.90347668448599,-1.55120566093629,3.51450400917026));
#5324=CARTESIAN_POINT('Ctrl Pts',(5.90818691390588,-1.54283758956267,3.44932270797349));
#5325=CARTESIAN_POINT('Ctrl Pts',(5.91293853705445,-1.53439597916469,3.38356859028381));
#5326=CARTESIAN_POINT('Ctrl Pts',(5.91769016020302,-1.52176325341198,3.31848438005927));
#5327=CARTESIAN_POINT('Ctrl Pts',(5.92244178335159,-1.50507796139423,3.25455788632466));
#5328=CARTESIAN_POINT('Ctrl Pts',(5.92623944109224,-1.49174251234766,3.20346567295395));
#5329=CARTESIAN_POINT('Ctrl Pts',(5.93003709883289,-1.47581937761418,3.1531126421748));
#5330=CARTESIAN_POINT('Ctrl Pts',(5.93383475657354,-1.45740100965981,3.10373782384496));
#5331=CARTESIAN_POINT('Ctrl Pts',(5.93798424644059,-1.43727628109979,3.04978869984821));
#5332=CARTESIAN_POINT('Ctrl Pts',(5.94213373630765,-1.4141099876031,2.99684609065118));
#5333=CARTESIAN_POINT('Ctrl Pts',(5.94628322617471,-1.38802361564245,2.94527575152803));
#5334=CARTESIAN_POINT('Ctrl Pts',(5.95042537286349,-1.36198340764075,2.89379667427226));
#5335=CARTESIAN_POINT('Ctrl Pts',(5.95456751955227,-1.33303361120314,2.84368550740766));
#5336=CARTESIAN_POINT('Ctrl Pts',(5.95870966624105,-1.30134408932065,2.79528895181879));
#5337=CARTESIAN_POINT('Ctrl Pts',(5.96284771292947,-1.26968593451924,2.7469403003507));
#5338=CARTESIAN_POINT('Ctrl Pts',(5.9669857596179,-1.23529371105071,2.70030333063743));
#5339=CARTESIAN_POINT('Ctrl Pts',(5.97112380630632,-1.19838275428231,2.65569944246255));
#5340=CARTESIAN_POINT('Ctrl Pts',(5.97525934459577,-1.16149417217827,2.61112259224915));
#5341=CARTESIAN_POINT('Ctrl Pts',(5.97939488288523,-1.1220902145225,2.56857678059709));
#5342=CARTESIAN_POINT('Ctrl Pts',(5.98353042117469,-1.08042771304446,2.5283519280355));
#5343=CARTESIAN_POINT('Ctrl Pts',(5.98766503908136,-1.03877448374493,2.48813602769715));
#5344=CARTESIAN_POINT('Ctrl Pts',(5.99179965698802,-0.994864082749133,2.45024042219371));
#5345=CARTESIAN_POINT('Ctrl Pts',(5.99593427489469,-0.948990009129827,2.41491801310439));
#5346=CARTESIAN_POINT('Ctrl Pts',(6.00007262786637,-0.903074494523489,2.379563695022));
#5347=CARTESIAN_POINT('Ctrl Pts',(6.00421098083804,-0.855192174986954,2.3467875377524));
#5348=CARTESIAN_POINT('Ctrl Pts',(6.00834933380971,-0.805668371193064,2.31680109476245));
#5349=CARTESIAN_POINT('Ctrl Pts',(6.01248940347486,-0.756124023672935,2.28680221263761));
#5350=CARTESIAN_POINT('Ctrl Pts',(6.01662947314,-0.704937294292704,2.25959559774776));
#5351=CARTESIAN_POINT('Ctrl Pts',(6.02076954280515,-0.652458312882652,2.2353468770355));
#5352=CARTESIAN_POINT('Ctrl Pts',(6.02491764792839,-0.599877475057004,2.21105109199942));
#5353=CARTESIAN_POINT('Ctrl Pts',(6.02906575305164,-0.545999858230309,2.18972486694799));
#5354=CARTESIAN_POINT('Ctrl Pts',(6.03321385817488,-0.491194922589014,2.17148532540861));
#5355=CARTESIAN_POINT('Ctrl Pts',(6.03709667116479,-0.439895037533872,2.15441229405697));
#5356=CARTESIAN_POINT('Ctrl Pts',(6.0409794841547,-0.387783153444902,2.14004335041998));
#5357=CARTESIAN_POINT('Ctrl Pts',(6.04486229714461,-0.335170067944933,2.12843387776357));
#5358=CARTESIAN_POINT('Ctrl Pts',(6.04900508487511,-0.279034259797718,2.11604708988489));
#5359=CARTESIAN_POINT('Ctrl Pts',(6.05314787260561,-0.222091363974047,2.10675003836955));
#5360=CARTESIAN_POINT('Ctrl Pts',(6.05729066033611,-0.164713239438949,2.10063986630154));
#5361=CARTESIAN_POINT('Ctrl Pts',(6.06142607839208,-0.107437185811405,2.09454056372104));
#5362=CARTESIAN_POINT('Ctrl Pts',(6.06556149644804,-0.0497279550305901,
2.09161694391283));
#5363=CARTESIAN_POINT('Ctrl Pts',(6.069696914504,0.00803220328821814,2.09191520654158));
#5364=CARTESIAN_POINT('Ctrl Pts',(6.07382822078269,0.0657349316439135,2.09221317261277));
#5365=CARTESIAN_POINT('Ctrl Pts',(6.07795952706138,0.123487967648581,2.09572667211674));
#5366=CARTESIAN_POINT('Ctrl Pts',(6.08209083334006,0.180905515728952,2.10244998889995));
#5367=CARTESIAN_POINT('Ctrl Pts',(6.08621963067589,0.23828819412462,2.10916922261197));
#5368=CARTESIAN_POINT('Ctrl Pts',(6.09034842801171,0.295335270781277,2.11909434928144));
#5369=CARTESIAN_POINT('Ctrl Pts',(6.09447722534754,0.351664776387409,2.13216770801055));
#5370=CARTESIAN_POINT('Ctrl Pts',(6.09860511296698,0.407981870661623,2.14523818622805));
#5371=CARTESIAN_POINT('Ctrl Pts',(6.10273300058642,0.463581199258392,2.16145540146296));
#5372=CARTESIAN_POINT('Ctrl Pts',(6.10686088820587,0.518091919598055,2.18071078976038));
#5373=CARTESIAN_POINT('Ctrl Pts',(6.11099258125585,0.57265289245891,2.19998392927815));
#5374=CARTESIAN_POINT('Ctrl Pts',(6.11512427430583,0.626122757588663,2.22230066550838));
#5375=CARTESIAN_POINT('Ctrl Pts',(6.11925596735582,0.678148079973918,2.24750324692855));
#5376=CARTESIAN_POINT('Ctrl Pts',(6.12338940431176,0.73019536121932,2.27271646586013));
#5377=CARTESIAN_POINT('Ctrl Pts',(6.12752284126771,0.780796426362209,2.30081770465715));
#5378=CARTESIAN_POINT('Ctrl Pts',(6.13165627822366,0.829622938255546,2.33160343992099));
#5379=CARTESIAN_POINT('Ctrl Pts',(6.13579788374345,0.878545941878112,2.36245001444441));
#5380=CARTESIAN_POINT('Ctrl Pts',(6.13993948926323,0.925686956785624,2.39599138361087));
#5381=CARTESIAN_POINT('Ctrl Pts',(6.14408109478302,0.970747883840817,2.43198145370052));
#5382=CARTESIAN_POINT('Ctrl Pts',(6.14801734242724,1.0135745043676,2.466186987745));
#5383=CARTESIAN_POINT('Ctrl Pts',(6.15195359007147,1.05452218822353,2.50260381659366));
#5384=CARTESIAN_POINT('Ctrl Pts',(6.15588983771569,1.09336663524267,2.54099054071577));
#5385=CARTESIAN_POINT('Ctrl Pts',(6.16004611115688,1.13438238376155,2.58152298084242));
#5386=CARTESIAN_POINT('Ctrl Pts',(6.16420238459808,1.1732257260731,2.62442275623431));
#5387=CARTESIAN_POINT('Ctrl Pts',(6.16835865803927,1.2096124064122,2.66942817221141));
#5388=CARTESIAN_POINT('Ctrl Pts',(6.17250750719807,1.24593408982704,2.71435319575958));
#5389=CARTESIAN_POINT('Ctrl Pts',(6.17665635635688,1.2798074992649,2.76137599322712));
#5390=CARTESIAN_POINT('Ctrl Pts',(6.18080520551568,1.31098563418944,2.81019860293998));
#5391=CARTESIAN_POINT('Ctrl Pts',(6.18494990073539,1.34213255272877,2.85897233014605));
#5392=CARTESIAN_POINT('Ctrl Pts',(6.1890945959551,1.37058926659055,2.90954186382701));
#5393=CARTESIAN_POINT('Ctrl Pts',(6.19323929117481,1.3961505096662,2.9615781631709));
#5394=CARTESIAN_POINT('Ctrl Pts',(6.19738141319725,1.42169588327081,3.01358215623988));
#5395=CARTESIAN_POINT('Ctrl Pts',(6.20152353521969,1.44434912188287,3.0670506450801));
#5396=CARTESIAN_POINT('Ctrl Pts',(6.20566565724214,1.46395068420032,3.1216296499198));
#5397=CARTESIAN_POINT('Ctrl Pts',(6.20980678316089,1.48354753270481,3.17619552951893));
#5398=CARTESIAN_POINT('Ctrl Pts',(6.21394790907965,1.50009398675634,3.23187090709963));
#5399=CARTESIAN_POINT('Ctrl Pts',(6.2180890349984,1.513479294399,3.28828351686983));
#5400=CARTESIAN_POINT('Ctrl Pts',(6.22223372590763,1.52687612511417,3.34474469082774));
#5401=CARTESIAN_POINT('Ctrl Pts',(6.22637841681686,1.53710624944037,3.40194385993305));
#5402=CARTESIAN_POINT('Ctrl Pts',(6.23052310772609,1.5441096675528,3.45949666475761));
#5403=CARTESIAN_POINT('Ctrl Pts',(6.23466943240518,1.55111584629894,3.51707215596342));
#5404=CARTESIAN_POINT('Ctrl Pts',(6.23881575708427,1.55489274683005,3.575001042381));
#5405=CARTESIAN_POINT('Ctrl Pts',(6.24296208176337,1.55543242157753,3.63289509224646));
#5406=CARTESIAN_POINT('Ctrl Pts',(6.24711622102969,1.55597311345118,3.69089825515485));
#5407=CARTESIAN_POINT('Ctrl Pts',(6.25127036029601,1.55326440933669,3.74886593033461));
#5408=CARTESIAN_POINT('Ctrl Pts',(6.25542449956233,1.54735052601686,3.80641207622514));
#5409=CARTESIAN_POINT('Ctrl Pts',(6.25925545913714,1.54189672524708,3.85948130295521));
#5410=CARTESIAN_POINT('Ctrl Pts',(6.26308641871195,1.53371769744794,3.9121917842015));
#5411=CARTESIAN_POINT('Ctrl Pts',(6.26691737828676,1.52288640708489,3.96424970512882));
#5412=CARTESIAN_POINT('Ctrl Pts',(6.27107106646946,1.51114266458232,4.02069310181546));
#5413=CARTESIAN_POINT('Ctrl Pts',(6.27522475465216,1.49623281783692,4.07659759798716));
#5414=CARTESIAN_POINT('Ctrl Pts',(6.27937844283485,1.47822260570092,4.13158263211564));
#5415=CARTESIAN_POINT('Ctrl Pts',(6.28352491304002,1.460243690403,4.18647211724689));
#5416=CARTESIAN_POINT('Ctrl Pts',(6.2876713832452,1.43917526453003,4.24044482260319));
#5417=CARTESIAN_POINT('Ctrl Pts',(6.29181785345036,1.41513374529266,4.29313182428395));
#5418=CARTESIAN_POINT('Ctrl Pts',(6.29596029630497,1.39111557691066,4.34576765255325));
#5419=CARTESIAN_POINT('Ctrl Pts',(6.30010273915958,1.3641302517053,4.39711978172299));
#5420=CARTESIAN_POINT('Ctrl Pts',(6.30424518201418,1.33434292531336,4.44683752921203));
#5421=CARTESIAN_POINT('Ctrl Pts',(6.30838518050274,1.30457317577931,4.49652593933218));
#5422=CARTESIAN_POINT('Ctrl Pts',(6.31252517899129,1.27200496925219,4.54458143538889));
#5423=CARTESIAN_POINT('Ctrl Pts',(6.31666517747985,1.23684919659391,4.59067826168064));
#5424=CARTESIAN_POINT('Ctrl Pts',(6.32080431108983,1.2017007682558,4.6367654579792));
#5425=CARTESIAN_POINT('Ctrl Pts',(6.32494344469982,1.16396616180008,4.68089438451619));
#5426=CARTESIAN_POINT('Ctrl Pts',(6.3290825783098,1.12389806613614,4.72277039647617));
#5427=CARTESIAN_POINT('Ctrl Pts',(6.33322549552921,1.08379334396076,4.76468468757585));
#5428=CARTESIAN_POINT('Ctrl Pts',(6.33736841274863,1.04135122909553,4.80434157222007));
#5429=CARTESIAN_POINT('Ctrl Pts',(6.34151132996804,0.996862078378707,4.84148250804077));
#5430=CARTESIAN_POINT('Ctrl Pts',(6.34565599776481,0.95235412890351,4.87863913765349));
#5431=CARTESIAN_POINT('Ctrl Pts',(6.34980066556158,0.905797835747466,4.91327738756307));
#5432=CARTESIAN_POINT('Ctrl Pts',(6.35394533335835,0.857514990188481,4.94518038730212));
#5433=CARTESIAN_POINT('Ctrl Pts',(6.35809803176834,0.809138592895799,4.97714520156145));
#5434=CARTESIAN_POINT('Ctrl Pts',(6.36225073017833,0.759029407425852,5.0063639114422));
#5435=CARTESIAN_POINT('Ctrl Pts',(6.36640342858832,0.707535639226755,5.03266468352131));
#5436=CARTESIAN_POINT('Ctrl Pts',(6.37025059201149,0.659830527519035,5.05703037501979));
#5437=CARTESIAN_POINT('Ctrl Pts',(6.37409775543467,0.610937638366414,5.07889208943651));
#5438=CARTESIAN_POINT('Ctrl Pts',(6.37794491885785,0.561147201320722,5.09815084633289));
#5439=CARTESIAN_POINT('Ctrl Pts',(6.38204949143226,0.50802534506297,5.11869818385905));
#5440=CARTESIAN_POINT('Ctrl Pts',(6.38615406400668,0.453648599692888,5.13637204992538));
#5441=CARTESIAN_POINT('Ctrl Pts',(6.3902586365811,0.398362951921499,5.15101915833667));
#5442=CARTESIAN_POINT('Ctrl Pts',(6.39437171253309,0.342962769754888,5.16569661092899));
#5443=CARTESIAN_POINT('Ctrl Pts',(6.39848478848509,0.286650394655892,5.17733450259257));
#5444=CARTESIAN_POINT('Ctrl Pts',(6.40259786443708,0.229794572184286,5.18582701623475));
#5445=CARTESIAN_POINT('Ctrl Pts',(6.40669109440536,0.173213084478161,5.19427855268872));
#5446=CARTESIAN_POINT('Ctrl Pts',(6.41078432437364,0.116093905813112,5.19961488454923));
#5447=CARTESIAN_POINT('Ctrl Pts',(6.41487755434192,0.058813295256594,5.20178220829634));
#5448=CARTESIAN_POINT('Ctrl Pts',(6.41896840146112,0.00156603026121408,
5.20394827034903));
#5449=CARTESIAN_POINT('Ctrl Pts',(6.42305924858032,-0.0558419493354018,
5.20294895786843));
#5450=CARTESIAN_POINT('Ctrl Pts',(6.42715009569952,-0.113030086156676,5.19878237903457));
#5451=CARTESIAN_POINT('Ctrl Pts',(6.43124021285904,-0.170208018481599,5.19461654367375));
#5452=CARTESIAN_POINT('Ctrl Pts',(6.43533033001855,-0.227165654833645,5.18728460211641));
#5453=CARTESIAN_POINT('Ctrl Pts',(6.43942044717806,-0.283525656181346,5.17683667127388));
#5454=CARTESIAN_POINT('Ctrl Pts',(6.4435497815323,-0.340426053087751,5.16628856272926));
#5455=CARTESIAN_POINT('Ctrl Pts',(6.44767911588654,-0.396716744592947,5.15256446132537));
#5456=CARTESIAN_POINT('Ctrl Pts',(6.45180845024078,-0.45202073919452,5.13576858164988));
#5457=CARTESIAN_POINT('Ctrl Pts',(6.45590494376929,-0.506884898051893,5.11910628053936));
#5458=CARTESIAN_POINT('Ctrl Pts',(6.4600014372978,-0.560777515795708,5.0994211367842));
#5459=CARTESIAN_POINT('Ctrl Pts',(6.46409793082631,-0.613349278357512,5.07686391977219));
#5460=CARTESIAN_POINT('Ctrl Pts',(6.46824368559341,-0.666553227964335,5.05403544724825));
#5461=CARTESIAN_POINT('Ctrl Pts',(6.47238944036051,-0.718403838885281,5.02826561058247));
#5462=CARTESIAN_POINT('Ctrl Pts',(6.47653519512761,-0.768565993296113,4.99975779370673));
#5463=CARTESIAN_POINT('Ctrl Pts',(6.48068094989472,-0.818728147706942,4.97124997683098));
#5464=CARTESIAN_POINT('Ctrl Pts',(6.48482670466182,-0.86720142445848,4.94000455072264));
#5465=CARTESIAN_POINT('Ctrl Pts',(6.48897245942892,-0.913684566917064,4.90626728242261));
#5466=CARTESIAN_POINT('Ctrl Pts',(6.4933509496862,-0.962777192462079,4.87063606232941));
#5467=CARTESIAN_POINT('Ctrl Pts',(6.49772943994349,-1.00987680836232,4.83206076559067));
#5468=CARTESIAN_POINT('Ctrl Pts',(6.50210793020077,-1.05462032230713,4.79079126108015));
#5469=CARTESIAN_POINT('Ctrl Pts',(6.50633096419065,-1.09777523852538,4.75098701120122));
#5470=CARTESIAN_POINT('Ctrl Pts',(6.51055399818052,-1.13873813199972,4.70867701401803));
#5471=CARTESIAN_POINT('Ctrl Pts',(6.5147770321704,-1.17721363608816,4.66412860512009));
#5472=CARTESIAN_POINT('Ctrl Pts',(6.51899490443744,-1.2156421124026,4.61963464677595));
#5473=CARTESIAN_POINT('Ctrl Pts',(6.52321277670448,-1.25158891032136,4.5729080796287));
#5474=CARTESIAN_POINT('Ctrl Pts',(6.52743064897153,-1.28479547448399,4.52425297382821));
#5475=CARTESIAN_POINT('Ctrl Pts',(6.53164476649455,-1.31797247820946,4.47564118073514));
#5476=CARTESIAN_POINT('Ctrl Pts',(6.53585888401758,-1.3484138122942,4.42510466592988));
#5477=CARTESIAN_POINT('Ctrl Pts',(6.5400730015406,-1.3759023907967,4.37297896439712));
#5478=CARTESIAN_POINT('Ctrl Pts',(6.5442847660271,-1.40337562050344,4.32088236828888));
#5479=CARTESIAN_POINT('Ctrl Pts',(6.5484965305136,-1.42789913910852,4.26719878661905));
#5480=CARTESIAN_POINT('Ctrl Pts',(6.55270829500011,-1.4493012164244,4.21228935591408));
#5481=CARTESIAN_POINT('Ctrl Pts',(6.55692040483961,-1.47070504865126,4.1573754227881));
#5482=CARTESIAN_POINT('Ctrl Pts',(6.56113251467912,-1.4889867388586,4.10123589863111));
#5483=CARTESIAN_POINT('Ctrl Pts',(6.56534462451863,-1.50402284555278,4.04425153330266));
#5484=CARTESIAN_POINT('Ctrl Pts',(6.56955693078515,-1.51905965343891,3.9872645105723));
#5485=CARTESIAN_POINT('Ctrl Pts',(6.57376923705167,-1.53085045935568,3.92943305061999));
#5486=CARTESIAN_POINT('Ctrl Pts',(6.5779815433182,-1.53932242567223,3.87115040635603));
#5487=CARTESIAN_POINT('Ctrl Pts',(6.58219714361556,-1.54780101708121,3.81282218496265));
#5488=CARTESIAN_POINT('Ctrl Pts',(6.58641274391292,-1.55295552961871,3.75404256799044));
#5489=CARTESIAN_POINT('Ctrl Pts',(6.59062834421029,-1.55476488354477,3.6952108556006));
#5490=CARTESIAN_POINT('Ctrl Pts',(6.59177097134143,-1.55525530406377,3.6792646780681));
#5491=CARTESIAN_POINT('Ctrl Pts',(6.59291359847256,-1.55550026292146,3.66331467869627));
#5492=CARTESIAN_POINT('Ctrl Pts',(6.5940562256037,-1.55549999978822,3.64736879997355));
#5493=CARTESIAN_POINT('Ctrl Pts',(5.7559437743963,-1.55415988380114,3.64862366743361));
#5494=CARTESIAN_POINT('Ctrl Pts',(5.78090458864165,-1.55156969786396,3.29945639063284));
#5495=CARTESIAN_POINT('Ctrl Pts',(5.84287458307737,-1.26257785748728,2.42869791902303));
#5496=CARTESIAN_POINT('Ctrl Pts',(5.94185375770342,0.17968266065122,1.81826775193874));
#5497=CARTESIAN_POINT('Ctrl Pts',(6.05288129827453,1.63338127522104,2.80478342088779));
#5498=CARTESIAN_POINT('Ctrl Pts',(6.16390883884558,1.5946610617751,4.56100604319437));
#5499=CARTESIAN_POINT('Ctrl Pts',(6.27493637941668,0.0991443931483699,5.48278383251785));
#5500=CARTESIAN_POINT('Ctrl Pts',(6.37228135793357,-1.29176384967164,4.82025828670267));
#5501=CARTESIAN_POINT('Ctrl Pts',(6.43261715626011,-1.55167090461383,3.97306868873034));
#5502=CARTESIAN_POINT('Ctrl Pts',(6.4559437743963,-1.55356356749417,3.64654650170336));
#5503=CARTESIAN_POINT('Origin',(0.,0.,3.64739446828387));
#5504=CARTESIAN_POINT('',(2.72586969217418,-1.95399957629683,3.64868125956087));
#5505=CARTESIAN_POINT('',(2.6241303079204,-1.95399895847038,3.64941196591101));
#5506=CARTESIAN_POINT('',(0.,-1.954,3.64739446828387));
#5507=CARTESIAN_POINT('',(2.50004110459941,0.86152797471893,5.40121474093917));
#5508=CARTESIAN_POINT('Ctrl Pts',(2.72586969212423,-1.95399957629626,3.64868126043292));
#5509=CARTESIAN_POINT('Ctrl Pts',(2.72192515475357,-1.95395422424648,3.71754854884412));
#5510=CARTESIAN_POINT('Ctrl Pts',(2.71798061738291,-1.95026833624108,3.78630291233304));
#5511=CARTESIAN_POINT('Ctrl Pts',(2.71403608001225,-1.94297611333583,3.85466198384382));
#5512=CARTESIAN_POINT('Ctrl Pts',(2.71011016029676,-1.93571830868518,3.92269841026298));
#5513=CARTESIAN_POINT('Ctrl Pts',(2.70618424058128,-1.92486848969711,3.99048552896683));
#5514=CARTESIAN_POINT('Ctrl Pts',(2.70225832086579,-1.91045410367946,4.05761528410667));
#5515=CARTESIAN_POINT('Ctrl Pts',(2.69833831584264,-1.89606143401484,4.12464390323834));
#5516=CARTESIAN_POINT('Ctrl Pts',(2.69441831081949,-1.87811495873734,4.19101664947758));
#5517=CARTESIAN_POINT('Ctrl Pts',(2.69049830579634,-1.85669380632836,4.25633133655668));
#5518=CARTESIAN_POINT('Ctrl Pts',(2.6865829619205,-1.83529812509765,4.32156836011862));
#5519=CARTESIAN_POINT('Ctrl Pts',(2.68266761804465,-1.81043612540169,4.38574936031743));
#5520=CARTESIAN_POINT('Ctrl Pts',(2.6787522741688,-1.78223740886531,4.44848486171089));
#5521=CARTESIAN_POINT('Ctrl Pts',(2.67483942124938,-1.75405663245792,4.5111804505436));
#5522=CARTESIAN_POINT('Ctrl Pts',(2.67092656832996,-1.7225435511983,4.57243191939858));
#5523=CARTESIAN_POINT('Ctrl Pts',(2.66701371541053,-1.68787623580068,4.63186885221639));
#5524=CARTESIAN_POINT('Ctrl Pts',(2.663102024005,-1.65321921124944,4.69128814143135));
#5525=CARTESIAN_POINT('Ctrl Pts',(2.65919033259946,-1.61541005819062,4.74889354119087));
#5526=CARTESIAN_POINT('Ctrl Pts',(2.65527864119393,-1.57467238540547,4.80433996338788));
#5527=CARTESIAN_POINT('Ctrl Pts',(2.65136678355455,-1.53393298140502,4.859788741873));
#5528=CARTESIAN_POINT('Ctrl Pts',(2.64745492591517,-1.49026510259596,4.91307796744342));
#5529=CARTESIAN_POINT('Ctrl Pts',(2.64354306827579,-1.44393413822889,4.96389369139689));
#5530=CARTESIAN_POINT('Ctrl Pts',(2.63962720909831,-1.39755578074682,5.01476139603935));
#5531=CARTESIAN_POINT('Ctrl Pts',(2.63571134992084,-1.34850923151089,5.06315018672228));
#5532=CARTESIAN_POINT('Ctrl Pts',(2.63179549074336,-1.29709774028617,5.10878197751765));
#5533=CARTESIAN_POINT('Ctrl Pts',(2.6278773663268,-1.24565650863569,5.15444016530821));
#5534=CARTESIAN_POINT('Ctrl Pts',(2.62395924191025,-1.19184799458207,5.19733787283971));
#5535=CARTESIAN_POINT('Ctrl Pts',(2.62004111749369,-1.13600746521167,5.23723818355382));
#5536=CARTESIAN_POINT('Ctrl Pts',(2.61611645127961,-1.08007370311117,5.27720511281438));
#5537=CARTESIAN_POINT('Ctrl Pts',(2.61219178506554,-1.0221015668269,5.31416439325073));
#5538=CARTESIAN_POINT('Ctrl Pts',(2.60826711885147,-0.962453365995261,5.34792365600291));
#5539=CARTESIAN_POINT('Ctrl Pts',(2.60651425904804,-0.935812900823969,5.36300143623801));
#5540=CARTESIAN_POINT('Ctrl Pts',(2.6047613992446,-0.908838399945064,5.37744152154705));
#5541=CARTESIAN_POINT('Ctrl Pts',(2.60300853944117,-0.881563413985287,5.39122988113756));
#5542=CARTESIAN_POINT('Ctrl Pts',(2.59912724522269,-0.821169396672931,5.42176094828629));
#5543=CARTESIAN_POINT('Ctrl Pts',(2.59524595100421,-0.759058631374259,5.44921582459445));
#5544=CARTESIAN_POINT('Ctrl Pts',(2.59136465678574,-0.695580341215257,5.47339665582771));
#5545=CARTESIAN_POINT('Ctrl Pts',(2.58748986314907,-0.632208367608115,5.49753698781955));
#5546=CARTESIAN_POINT('Ctrl Pts',(2.58361506951239,-0.567473881608454,5.51841398464901));
#5547=CARTESIAN_POINT('Ctrl Pts',(2.57974027587572,-0.50174941555497,5.53587627227094));
#5548=CARTESIAN_POINT('Ctrl Pts',(2.57586910437471,-0.436086388368726,5.55332223624301));
#5549=CARTESIAN_POINT('Ctrl Pts',(2.57199793287369,-0.369435697939428,5.56735968916254));
#5550=CARTESIAN_POINT('Ctrl Pts',(2.56812676137267,-0.302187103605631,5.57788636270209));
#5551=CARTESIAN_POINT('Ctrl Pts',(2.56425781933617,-0.23497723872495,5.58840697377574));
#5552=CARTESIAN_POINT('Ctrl Pts',(2.56038887729968,-0.16717064773718,5.5954207372019));
#5553=CARTESIAN_POINT('Ctrl Pts',(2.55651993526318,-0.0991674998868228,
5.59887641976746));
#5554=CARTESIAN_POINT('Ctrl Pts',(2.55265183306664,-0.0311791136327506,
5.60233135220023));
#5555=CARTESIAN_POINT('Ctrl Pts',(2.54878373087009,0.0370052435431303,5.60222971205842));
#5556=CARTESIAN_POINT('Ctrl Pts',(2.54491562867355,0.104982014579131,5.59857226044298));
#5557=CARTESIAN_POINT('Ctrl Pts',(2.54104440908414,0.173013569664301,5.59491186120284));
#5558=CARTESIAN_POINT('Ctrl Pts',(2.53717318949473,0.240836701823915,5.58768995036121));
#5559=CARTESIAN_POINT('Ctrl Pts',(2.53330196990532,0.308050758920962,5.57695937518082));
#5560=CARTESIAN_POINT('Ctrl Pts',(2.52942926989751,0.375290519785128,5.566224696451));
#5561=CARTESIAN_POINT('Ctrl Pts',(2.52555656988971,0.441920249618249,5.55197878458951));
#5562=CARTESIAN_POINT('Ctrl Pts',(2.5216838698819,0.507550177318446,5.53432552624651));
#5563=CARTESIAN_POINT('Ctrl Pts',(2.51780443308886,0.573294272066705,5.51664155904151));
#5564=CARTESIAN_POINT('Ctrl Pts',(2.51392499629581,0.638034611784042,5.49553856038448));
#5565=CARTESIAN_POINT('Ctrl Pts',(2.51004555950277,0.701398004787308,5.47116990371456));
#5566=CARTESIAN_POINT('Ctrl Pts',(2.50671074120165,0.755866066488274,5.4502222645154));
#5567=CARTESIAN_POINT('Ctrl Pts',(2.50337592290053,0.809316799860291,5.42686240189679));
#5568=CARTESIAN_POINT('Ctrl Pts',(2.50004110459941,0.86152797471893,5.40121474093917));
#5569=CARTESIAN_POINT('',(2.5,-0.861525859670532,5.40121577991141));
#5570=CARTESIAN_POINT('Origin',(2.5,0.,3.64739446828387));
#5571=CARTESIAN_POINT('Ctrl Pts',(2.5,-0.861525859670532,5.40121577991141));
#5572=CARTESIAN_POINT('Ctrl Pts',(2.50400926879465,-0.924640824599854,5.37021195183708));
#5573=CARTESIAN_POINT('Ctrl Pts',(2.5080185375893,-0.986127805684975,5.33577388677798));
#5574=CARTESIAN_POINT('Ctrl Pts',(2.51202780638395,-1.04560615745962,5.29809848884072));
#5575=CARTESIAN_POINT('Ctrl Pts',(2.51615279530842,-1.1068012418708,5.25933566021138));
#5576=CARTESIAN_POINT('Ctrl Pts',(2.52027778423288,-1.16586949339279,5.21714593155206));
#5577=CARTESIAN_POINT('Ctrl Pts',(2.52440277315734,-1.22242491847297,5.17179379874041));
#5578=CARTESIAN_POINT('Ctrl Pts',(2.52840911791387,-1.27735367946413,5.1277460975673));
#5579=CARTESIAN_POINT('Ctrl Pts',(2.53241546267039,-1.32991185917089,5.08071578688039));
#5580=CARTESIAN_POINT('Ctrl Pts',(2.53642180742692,-1.37977792362143,5.03098721236969));
#5581=CARTESIAN_POINT('Ctrl Pts',(2.54042822966511,-1.42964495246871,4.98125767612127));
#5582=CARTESIAN_POINT('Ctrl Pts',(2.5444346519033,-1.47681943741634,4.92883009647148));
#5583=CARTESIAN_POINT('Ctrl Pts',(2.54844107414149,-1.52101670404322,4.87402570301643));
#5584=CARTESIAN_POINT('Ctrl Pts',(2.55244865861312,-1.56522679197001,4.81920541121248));
#5585=CARTESIAN_POINT('Ctrl Pts',(2.55645624308475,-1.60645765682523,4.76200729257378));
#5586=CARTESIAN_POINT('Ctrl Pts',(2.56046382755638,-1.64446579811897,4.70278455674261));
#5587=CARTESIAN_POINT('Ctrl Pts',(2.56467747030761,-1.68442820694246,4.64051676093959));
#5588=CARTESIAN_POINT('Ctrl Pts',(2.56889111305883,-1.72082726588746,4.57601102517087));
#5589=CARTESIAN_POINT('Ctrl Pts',(2.57310475581006,-1.75343383018518,4.50970868199146));
#5590=CARTESIAN_POINT('Ctrl Pts',(2.57712095959757,-1.78451254633696,4.4465130725106));
#5591=CARTESIAN_POINT('Ctrl Pts',(2.58113716338509,-1.81214608686427,4.38168590917152));
#5592=CARTESIAN_POINT('Ctrl Pts',(2.5851533671726,-1.83618572392645,4.3156294473509));
#5593=CARTESIAN_POINT('Ctrl Pts',(2.58917326103715,-1.86024744854125,4.24951229303426));
#5594=CARTESIAN_POINT('Ctrl Pts',(2.59319315490169,-1.8807085593928,4.18216402918133));
#5595=CARTESIAN_POINT('Ctrl Pts',(2.59721304876624,-1.89747052412525,4.1140009513891));
#5596=CARTESIAN_POINT('Ctrl Pts',(2.6012402368791,-1.91426290407195,4.04571418913341));
#5597=CARTESIAN_POINT('Ctrl Pts',(2.60526742499197,-1.92734265511497,3.97661011190267));
#5598=CARTESIAN_POINT('Ctrl Pts',(2.60929461310484,-1.93666260885462,3.90711343074987));
#5599=CARTESIAN_POINT('Ctrl Pts',(2.60987225559358,-1.93799942281074,3.89714512662903));
#5600=CARTESIAN_POINT('Ctrl Pts',(2.61044989808233,-1.93925897094148,3.88716874862355));
#5601=CARTESIAN_POINT('Ctrl Pts',(2.61102754057108,-1.94044120187923,3.87718555176946));
#5602=CARTESIAN_POINT('Ctrl Pts',(2.61539512967265,-1.94938012008528,3.80170200852605));
#5603=CARTESIAN_POINT('Ctrl Pts',(2.61976271877421,-1.95392024650498,3.72564652348674));
#5604=CARTESIAN_POINT('Ctrl Pts',(2.62413030787577,-1.95399895846957,3.64941196669006));
#5605=CARTESIAN_POINT('Origin',(0.,0.,3.64739446828387));
#5606=CARTESIAN_POINT('',(3.42586969208078,-1.95399979033444,3.64829966051471));
#5607=CARTESIAN_POINT('',(3.3241303078362,-1.95399983251307,3.64820350405597));
#5608=CARTESIAN_POINT('',(0.,-1.954,3.64739446828387));
#5609=CARTESIAN_POINT('Ctrl Pts',(3.42586969208078,-1.95399979033444,3.64829966051471));
#5610=CARTESIAN_POINT('Ctrl Pts',(3.42158392528816,-1.95396480342059,3.72382441647484));
#5611=CARTESIAN_POINT('Ctrl Pts',(3.41729815849555,-1.94954693631289,3.79920428739692));
#5612=CARTESIAN_POINT('Ctrl Pts',(3.41301239170294,-1.94082130003993,3.87395280803618));
#5613=CARTESIAN_POINT('Ctrl Pts',(3.40871252448995,-1.93206695591947,3.94894725562724));
#5614=CARTESIAN_POINT('Ctrl Pts',(3.40441265727697,-1.91897658649658,4.0233058867645));
#5615=CARTESIAN_POINT('Ctrl Pts',(3.40011279006398,-1.90167612158761,4.09655360331678));
#5616=CARTESIAN_POINT('Ctrl Pts',(3.39579316317008,-1.88429615383603,4.1701379236373));
#5617=CARTESIAN_POINT('Ctrl Pts',(3.39147353627618,-1.86266745413098,4.24260079990365));
#5618=CARTESIAN_POINT('Ctrl Pts',(3.38715390938228,-1.83696603276114,4.3134813954051));
#5619=CARTESIAN_POINT('Ctrl Pts',(3.38483638073443,-1.82317692972559,4.35150963596525));
#5620=CARTESIAN_POINT('Ctrl Pts',(3.38251885208658,-1.80821632797972,4.3890828085135));
#5621=CARTESIAN_POINT('Ctrl Pts',(3.38020132343873,-1.79211686507899,4.4261326411632));
#5622=CARTESIAN_POINT('Ctrl Pts',(3.37628273639694,-1.76489513180678,4.48877825042292));
#5623=CARTESIAN_POINT('Ctrl Pts',(3.37236414935515,-1.73433083910883,4.55011866002973));
#5624=CARTESIAN_POINT('Ctrl Pts',(3.36844556231337,-1.70057119742648,4.60977360484257));
#5625=CARTESIAN_POINT('Ctrl Pts',(3.36453286752669,-1.66686231904712,4.669338848406));
#5626=CARTESIAN_POINT('Ctrl Pts',(3.36062017274002,-1.62996786774874,4.72722323253677));
#5627=CARTESIAN_POINT('Ctrl Pts',(3.35670747795334,-1.59008264753985,4.78306747315484));
#5628=CARTESIAN_POINT('Ctrl Pts',(3.35279937593377,-1.55024424507097,4.83884616314728));
#5629=CARTESIAN_POINT('Ctrl Pts',(3.3488912739142,-1.50742233031501,4.89258906739674));
#5630=CARTESIAN_POINT('Ctrl Pts',(3.34498317189463,-1.46185610518546,4.94396406831775));
#5631=CARTESIAN_POINT('Ctrl Pts',(3.34107751390498,-1.4163183760412,4.99530694058938));
#5632=CARTESIAN_POINT('Ctrl Pts',(3.33717185591533,-1.36804006657401,5.044284479995));
#5633=CARTESIAN_POINT('Ctrl Pts',(3.33326619792568,-1.3173009502997,5.0905972282381));
#5634=CARTESIAN_POINT('Ctrl Pts',(3.32936164377851,-1.26657617424465,5.13689688727089));
#5635=CARTESIAN_POINT('Ctrl Pts',(3.32545708963134,-1.21339233509802,5.18053291892595));
#5636=CARTESIAN_POINT('Ctrl Pts',(3.32155253548417,-1.15806508986369,5.22124365027019));
#5637=CARTESIAN_POINT('Ctrl Pts',(3.31764774663011,-1.10273451885,5.26195682877965));
#5638=CARTESIAN_POINT('Ctrl Pts',(3.31374295777605,-1.04526068354753,5.29974406850757));
#5639=CARTESIAN_POINT('Ctrl Pts',(3.30983816892199,-0.985989779129678,5.33438591919636));
#5640=CARTESIAN_POINT('Ctrl Pts',(3.30592922772634,-0.926655846197141,5.36906460793269));
#5641=CARTESIAN_POINT('Ctrl Pts',(3.30202028653069,-0.865521455784667,5.40059098391655));
#5642=CARTESIAN_POINT('Ctrl Pts',(3.29811134533503,-0.802958182434663,5.42879115551028));
#5643=CARTESIAN_POINT('Ctrl Pts',(3.29420006241485,-0.740357429382513,5.45700822094564));
#5644=CARTESIAN_POINT('Ctrl Pts',(3.29028877949467,-0.676326548180478,5.48189493811238));
#5645=CARTESIAN_POINT('Ctrl Pts',(3.2863774965745,-0.611255279002647,5.50332630536502));
#5646=CARTESIAN_POINT('Ctrl Pts',(3.28245948400635,-0.546072049952974,5.5247945468505));
#5647=CARTESIAN_POINT('Ctrl Pts',(3.2785414714382,-0.479845334551296,5.54279544405974));
#5648=CARTESIAN_POINT('Ctrl Pts',(3.27462345887005,-0.412977281260257,5.55725461111184));
#5649=CARTESIAN_POINT('Ctrl Pts',(3.27280690020258,-0.381974383829492,5.56395850110098));
#5650=CARTESIAN_POINT('Ctrl Pts',(3.27099034153511,-0.350833722259847,5.56990177297914));
#5651=CARTESIAN_POINT('Ctrl Pts',(3.26917378286764,-0.319595685371469,5.57508080114302));
#5652=CARTESIAN_POINT('Ctrl Pts',(3.2652550933095,-0.252208833978631,5.58625302692934));
#5653=CARTESIAN_POINT('Ctrl Pts',(3.26133640375136,-0.184102294733243,5.59390957506827));
#5654=CARTESIAN_POINT('Ctrl Pts',(3.25741771419322,-0.115675333849631,5.59796751668241));
#5655=CARTESIAN_POINT('Ctrl Pts',(3.25350491429959,-0.0473512164897911,
5.60201935934069));
#5656=CARTESIAN_POINT('Ctrl Pts',(3.24959211440596,0.0212918798043963,5.60248330086764));
#5657=CARTESIAN_POINT('Ctrl Pts',(3.24567931451233,0.0898464570696467,5.59932776994969));
#5658=CARTESIAN_POINT('Ctrl Pts',(3.24177110411623,0.158320623613178,5.59617594029471));
#5659=CARTESIAN_POINT('Ctrl Pts',(3.23786289372013,0.226705988457194,5.58941309229315));
#5660=CARTESIAN_POINT('Ctrl Pts',(3.23395468332404,0.29459375043913,5.5790596882954));
#5661=CARTESIAN_POINT('Ctrl Pts',(3.23004891499837,0.362439092315871,5.56871275368881));
#5662=CARTESIAN_POINT('Ctrl Pts',(3.2261431466727,0.429786963122525,5.55477978767467));
#5663=CARTESIAN_POINT('Ctrl Pts',(3.22223737834704,0.496233948595613,5.53733305677324));
#5664=CARTESIAN_POINT('Ctrl Pts',(3.21833271208874,0.562662185118795,5.51989124871191));
#5665=CARTESIAN_POINT('Ctrl Pts',(3.21442804583045,0.628189565578153,5.49893776883435));
#5666=CARTESIAN_POINT('Ctrl Pts',(3.21052337957215,0.692424912524464,5.47459553563127));
#5667=CARTESIAN_POINT('Ctrl Pts',(3.20661847701429,0.75666414681581,5.45025182930376));
#5668=CARTESIAN_POINT('Ctrl Pts',(3.20271357445642,0.819610733474399,5.42251913914844));
#5669=CARTESIAN_POINT('Ctrl Pts',(3.19880867189856,0.880892360436765,5.39156895764098));
#5670=CARTESIAN_POINT('Ctrl Pts',(3.19489961540771,0.942239177187537,5.36058585214172));
#5671=CARTESIAN_POINT('Ctrl Pts',(3.19099055891686,1.00191705989154,5.32637864684416));
#5672=CARTESIAN_POINT('Ctrl Pts',(3.18708150242601,1.0595781643575,5.28916488878023));
#5673=CARTESIAN_POINT('Ctrl Pts',(3.18317010313604,1.11727382662158,5.25192882754416));
#5674=CARTESIAN_POINT('Ctrl Pts',(3.17925870384606,1.17294990653504,5.21168291548388));
#5675=CARTESIAN_POINT('Ctrl Pts',(3.17534730455609,1.22628974279198,5.16868650688894));
#5676=CARTESIAN_POINT('Ctrl Pts',(3.1714291752118,1.27972135694444,5.12561611756641));
#5677=CARTESIAN_POINT('Ctrl Pts',(3.16751104586751,1.33080833887664,5.0797861145422));
#5678=CARTESIAN_POINT('Ctrl Pts',(3.16359291652321,1.37926978606372,5.03149376286202));
#5679=CARTESIAN_POINT('Ctrl Pts',(3.16177735844767,1.40172554595877,5.00911635737697));
#5680=CARTESIAN_POINT('Ctrl Pts',(3.15996180037212,1.42361812047926,4.98621072846779));
#5681=CARTESIAN_POINT('Ctrl Pts',(3.15814624229657,1.44492256927572,4.96280876378078));
#5682=CARTESIAN_POINT('Ctrl Pts',(3.15422851803746,1.49089463538646,4.91231054728197));
#5683=CARTESIAN_POINT('Ctrl Pts',(3.15031079377835,1.53430736323658,4.85929933663352));
#5684=CARTESIAN_POINT('Ctrl Pts',(3.14639306951924,1.57487428716368,4.80406511268991));
#5685=CARTESIAN_POINT('Ctrl Pts',(3.14248123821492,1.61538019121469,4.74891397085298));
#5686=CARTESIAN_POINT('Ctrl Pts',(3.1385694069106,1.65304849789036,4.69154684530576));
#5687=CARTESIAN_POINT('Ctrl Pts',(3.13465757560628,1.68763137962662,4.63228853695296));
#5688=CARTESIAN_POINT('Ctrl Pts',(3.13075033395481,1.72217368614138,4.57309975487636));
#5689=CARTESIAN_POINT('Ctrl Pts',(3.12684309230334,1.7536375103363,4.51202461959078));
#5690=CARTESIAN_POINT('Ctrl Pts',(3.12293585065187,1.78181799743233,4.44941730089291));
#5691=CARTESIAN_POINT('Ctrl Pts',(3.11903105060526,1.8099808747616,4.38684910502059));
#5692=CARTESIAN_POINT('Ctrl Pts',(3.11512625055865,1.83486428347826,4.32275107262859));
#5693=CARTESIAN_POINT('Ctrl Pts',(3.11122145051204,1.85630978619131,4.25750099807221));
#5694=CARTESIAN_POINT('Ctrl Pts',(3.10731775061606,1.87774924678109,4.19226930727672));
#5695=CARTESIAN_POINT('Ctrl Pts',(3.10341405072007,1.89575257068176,4.1258866858309));
#5696=CARTESIAN_POINT('Ctrl Pts',(3.09951035082408,1.91021049363009,4.05874817256462));
#5697=CARTESIAN_POINT('Ctrl Pts',(3.09560641125923,1.92466930422709,3.99160553730843));
#5698=CARTESIAN_POINT('Ctrl Pts',(3.09170247169438,1.93558218067504,3.92370739958937));
#5699=CARTESIAN_POINT('Ctrl Pts',(3.08779853212952,1.94289088911684,3.85545934515353));
#5700=CARTESIAN_POINT('Ctrl Pts',(3.08389042701198,1.95020739604261,3.78713846918396));
#5701=CARTESIAN_POINT('Ctrl Pts',(3.07998232189443,1.95391200778782,3.71846742150226));
#5702=CARTESIAN_POINT('Ctrl Pts',(3.07607421677689,1.95399844922611,3.64985626071567));
#5703=CARTESIAN_POINT('Ctrl Pts',(3.07216376361086,1.95408494259971,3.58120387730907));
#5704=CARTESIAN_POINT('Ctrl Pts',(3.06825331044483,1.95054896473043,3.51261194378154));
#5705=CARTESIAN_POINT('Ctrl Pts',(3.0643428572788,1.94343628034531,3.44448704053023));
#5706=CARTESIAN_POINT('Ctrl Pts',(3.0604256561111,1.93631132208704,3.37624457879108));
#5707=CARTESIAN_POINT('Ctrl Pts',(3.0565084549434,1.92559741588042,3.30847124143886));
#5708=CARTESIAN_POINT('Ctrl Pts',(3.0525912537757,1.91139157959021,3.24156417188939));
#5709=CARTESIAN_POINT('Ctrl Pts',(3.05076706975896,1.90477612677183,3.21040651578396));
#5710=CARTESIAN_POINT('Ctrl Pts',(3.04894288574222,1.8974041141819,3.17943651304369));
#5711=CARTESIAN_POINT('Ctrl Pts',(3.04711870172548,1.88928897332868,3.1486929791557));
#5712=CARTESIAN_POINT('Ctrl Pts',(3.04319933921464,1.87185313432429,3.08263875816405));
#5713=CARTESIAN_POINT('Ctrl Pts',(3.03927997670381,1.85091457533122,3.01736962809996));
#5714=CARTESIAN_POINT('Ctrl Pts',(3.03536061419297,1.82656137564056,2.95328385676861));
#5715=CARTESIAN_POINT('Ctrl Pts',(3.03144714733761,1.8022448089673,2.88929448571348));
#5716=CARTESIAN_POINT('Ctrl Pts',(3.02753368048225,1.77452396902811,2.8264853963439));
#5717=CARTESIAN_POINT('Ctrl Pts',(3.02362021362689,1.74353715277275,2.76524130873555));
#5718=CARTESIAN_POINT('Ctrl Pts',(3.01971134820263,1.712586770632,2.70406923156185));
#5719=CARTESIAN_POINT('Ctrl Pts',(3.01580248277837,1.67837825975927,2.64445893807874));
#5720=CARTESIAN_POINT('Ctrl Pts',(3.0118936173541,1.64109791096867,2.58677500466166));
#5721=CARTESIAN_POINT('Ctrl Pts',(3.00798720177113,1.60384092725407,2.52912722405786));
#5722=CARTESIAN_POINT('Ctrl Pts',(3.00408078618816,1.56351619100125,2.47340382040303));
#5723=CARTESIAN_POINT('Ctrl Pts',(3.00017437060518,1.52035503671783,2.41994322186847));
#5724=CARTESIAN_POINT('Ctrl Pts',(2.99626906576854,1.47720615483419,2.36649782426745));
#5725=CARTESIAN_POINT('Ctrl Pts',(2.9923637609319,1.43122276464048,2.31531433675206));
#5726=CARTESIAN_POINT('Ctrl Pts',(2.98845845609525,1.38267738706865,2.26669926539186));
#5727=CARTESIAN_POINT('Ctrl Pts',(2.98455292455489,1.334129191428,2.21808137191711));
#5728=CARTESIAN_POINT('Ctrl Pts',(2.98064739301452,1.28301906227193,2.17203253660856));
#5729=CARTESIAN_POINT('Ctrl Pts',(2.97674186147416,1.22965609646502,2.12882215047138));
#5730=CARTESIAN_POINT('Ctrl Pts',(2.97283219460914,1.17623662792971,2.0855660115415));
#5731=CARTESIAN_POINT('Ctrl Pts',(2.96892252774413,1.12055994499606,2.04515462963035));
#5732=CARTESIAN_POINT('Ctrl Pts',(2.96501286087911,1.0629671261776,2.00781620279432));
#5733=CARTESIAN_POINT('Ctrl Pts',(2.96110086095524,1.00533993935786,1.97045549458489));
#5734=CARTESIAN_POINT('Ctrl Pts',(2.95718886103137,0.945794766954623,1.93617163639366));
#5735=CARTESIAN_POINT('Ctrl Pts',(2.9532768611075,0.884698047574294,1.90514725143483));
#5736=CARTESIAN_POINT('Ctrl Pts',(2.94935815224908,0.823496549589784,1.87406966080826));
#5737=CARTESIAN_POINT('Ctrl Pts',(2.94543944339066,0.760738643192596,1.84626289884298));
#5738=CARTESIAN_POINT('Ctrl Pts',(2.94152073453225,0.696810697123036,1.82186143588623));
#5739=CARTESIAN_POINT('Ctrl Pts',(2.93971087673963,0.667285540868821,1.8105916071036));
#5740=CARTESIAN_POINT('Ctrl Pts',(2.93790101894702,0.637511017076795,1.80004744746111));
#5741=CARTESIAN_POINT('Ctrl Pts',(2.93609116115441,0.607526056778453,1.79023855389886));
#5742=CARTESIAN_POINT('Ctrl Pts',(2.93217164916576,0.542589235858846,1.76899595900015));
#5743=CARTESIAN_POINT('Ctrl Pts',(2.9282521371771,0.476409137969001,1.75112150272362));
#5744=CARTESIAN_POINT('Ctrl Pts',(2.92433262518844,0.409368097857593,1.73675746444027));
#5745=CARTESIAN_POINT('Ctrl Pts',(2.92041899100293,0.342427594251113,1.72241496684607));
#5746=CARTESIAN_POINT('Ctrl Pts',(2.91650535681742,0.274629187590677,1.71157254128802));
#5747=CARTESIAN_POINT('Ctrl Pts',(2.9125917226319,0.206371096701409,1.70432293834827));
#5748=CARTESIAN_POINT('Ctrl Pts',(2.9086826646809,0.138192820382506,1.6970818124101));
#5749=CARTESIAN_POINT('Ctrl Pts',(2.9047736067299,0.0695564137907122,1.69342521710811));
#5750=CARTESIAN_POINT('Ctrl Pts',(2.90086454877889,0.000869236631294919,
1.69339466162378));
#5751=CARTESIAN_POINT('Ctrl Pts',(2.89695792519361,-0.0677751655906955,
1.69336412516787));
#5752=CARTESIAN_POINT('Ctrl Pts',(2.89305130160832,-0.13646978528588,1.69695514921585));
#5753=CARTESIAN_POINT('Ctrl Pts',(2.88914467802303,-0.204804767933434,1.70415721899295));
#5754=CARTESIAN_POINT('Ctrl Pts',(2.88523915016671,-0.273120583999455,1.71135726873505));
#5755=CARTESIAN_POINT('Ctrl Pts',(2.88133362231038,-0.341076474743408,1.72216630200451));
#5756=CARTESIAN_POINT('Ctrl Pts',(2.87742809445405,-0.408267032846675,1.73652188490983));
#5757=CARTESIAN_POINT('Ctrl Pts',(2.87352232531877,-0.475461741904262,1.75087835468632));
#5758=CARTESIAN_POINT('Ctrl Pts',(2.86961655618349,-0.541890544378382,1.76878170389674));
#5759=CARTESIAN_POINT('Ctrl Pts',(2.86571078704821,-0.607159343224681,1.79011863202934));
#5760=CARTESIAN_POINT('Ctrl Pts',(2.86180086252258,-0.672497582257252,1.81147826075227));
#5761=CARTESIAN_POINT('Ctrl Pts',(2.85789093799696,-0.736672886706858,1.83627860561703));
#5762=CARTESIAN_POINT('Ctrl Pts',(2.85398101347133,-0.799308385936659,1.86435714277121));
#5763=CARTESIAN_POINT('Ctrl Pts',(2.85006874406609,-0.861981449243459,1.89245251932709));
#5764=CARTESIAN_POINT('Ctrl Pts',(2.84615647466084,-0.92311243215019,1.92382977654807));
#5765=CARTESIAN_POINT('Ctrl Pts',(2.84224420525559,-0.982348966787532,1.95828034915175));
#5766=CARTESIAN_POINT('Ctrl Pts',(2.83832521180535,-1.04168731167421,1.99279013219724));
#5767=CARTESIAN_POINT('Ctrl Pts',(2.83440621835512,-1.09912429892442,2.03038350381018));
#5768=CARTESIAN_POINT('Ctrl Pts',(2.83048722490489,-1.15433717467074,2.07080901637421));
#5769=CARTESIAN_POINT('Ctrl Pts',(2.8286793567977,-1.17980738747802,2.08945768109113));
#5770=CARTESIAN_POINT('Ctrl Pts',(2.82687148869051,-1.20480477019509,2.10870848800456));
#5771=CARTESIAN_POINT('Ctrl Pts',(2.82506362058333,-1.22930022257401,2.12853405245248));
#5772=CARTESIAN_POINT('Ctrl Pts',(2.82120048498969,-1.28164323011487,2.17089822900847));
#5773=CARTESIAN_POINT('Ctrl Pts',(2.81733734939605,-1.33191182350578,2.21606720796798));
#5774=CARTESIAN_POINT('Ctrl Pts',(2.81347421380241,-1.37978360123066,2.2638073861763));
#5775=CARTESIAN_POINT('Ctrl Pts',(2.80961772082684,-1.42757306397375,2.31146547568672));
#5776=CARTESIAN_POINT('Ctrl Pts',(2.80576122785128,-1.47297353608629,2.36168563392952));
#5777=CARTESIAN_POINT('Ctrl Pts',(2.80190473487571,-1.51569521873079,2.41419375310542));
#5778=CARTESIAN_POINT('Ctrl Pts',(2.79805193389146,-1.5583760020187,2.46665160393615));
#5779=CARTESIAN_POINT('Ctrl Pts',(2.79419913290721,-1.59838275892305,2.52139268472611));
#5780=CARTESIAN_POINT('Ctrl Pts',(2.79034633192297,-1.6354632437027,2.57810686501829));
#5781=CARTESIAN_POINT('Ctrl Pts',(2.78649581047917,-1.67252178951754,2.63478748991299));
#5782=CARTESIAN_POINT('Ctrl Pts',(2.78264528903538,-1.70665721873714,2.69343847657481));
#5783=CARTESIAN_POINT('Ctrl Pts',(2.77879476759159,-1.73765945873498,2.75371913267879));
#5784=CARTESIAN_POINT('Ctrl Pts',(2.7749451166011,-1.76865469033084,2.81398616166841));
#5785=CARTESIAN_POINT('Ctrl Pts',(2.77109546561061,-1.79651790755939,2.87588167785098));
#5786=CARTESIAN_POINT('Ctrl Pts',(2.76724581462012,-1.8210850163862,2.9390404867932));
#5787=CARTESIAN_POINT('Ctrl Pts',(2.76339335182704,-1.84567006914097,3.00224542721657));
#5788=CARTESIAN_POINT('Ctrl Pts',(2.75954088903397,-1.86695402027117,3.06671503024606));
#5789=CARTESIAN_POINT('Ctrl Pts',(2.75568842624089,-1.88482147805859,3.13206545119962));
#5790=CARTESIAN_POINT('Ctrl Pts',(2.75183446353511,-1.90269589233812,3.19744131559861));
#5791=CARTESIAN_POINT('Ctrl Pts',(2.74798050082933,-1.91715105613517,3.26369818508291));
#5792=CARTESIAN_POINT('Ctrl Pts',(2.74412653812355,-1.92812257189284,3.33044124183343));
#5793=CARTESIAN_POINT('Ctrl Pts',(2.74026661691283,-1.93911105040696,3.39728748817429));
#5794=CARTESIAN_POINT('Ctrl Pts',(2.73640669570212,-1.94660507416329,3.46462091816665));
#5795=CARTESIAN_POINT('Ctrl Pts',(2.73254677449141,-1.950592162525,3.53204189789178));
#5796=CARTESIAN_POINT('Ctrl Pts',(2.73032108038567,-1.95289118330322,3.57091794457406));
#5797=CARTESIAN_POINT('Ctrl Pts',(2.72809538627992,-1.95402516604589,3.60982308596664));
#5798=CARTESIAN_POINT('Ctrl Pts',(2.72586969217418,-1.95399957629683,3.64868125956087));
#5799=CARTESIAN_POINT('Ctrl Pts',(2.6241303079204,-1.95399895847038,3.64941196591101));
#5800=CARTESIAN_POINT('Ctrl Pts',(2.62795723854692,-1.9540679267512,3.58261439099596));
#5801=CARTESIAN_POINT('Ctrl Pts',(2.63178416917345,-1.95070752961312,3.51565940348063));
#5802=CARTESIAN_POINT('Ctrl Pts',(2.63561109979997,-1.94389595297049,3.44893912311788));
#5803=CARTESIAN_POINT('Ctrl Pts',(2.63943211787231,-1.93709490011831,3.38232192465323));
#5804=CARTESIAN_POINT('Ctrl Pts',(2.64325313594464,-1.92685329612979,3.31593922231409));
#5805=CARTESIAN_POINT('Ctrl Pts',(2.64707415401698,-1.91320133873363,3.25018339408295));
#5806=CARTESIAN_POINT('Ctrl Pts',(2.65089193660013,-1.89956094128292,3.18448324532438));
#5807=CARTESIAN_POINT('Ctrl Pts',(2.65470971918328,-1.88251601273262,3.11940942193861));
#5808=CARTESIAN_POINT('Ctrl Pts',(2.65852750176644,-1.86214838250633,3.05534767830098));
#5809=CARTESIAN_POINT('Ctrl Pts',(2.66234348743459,-1.84179033870868,2.991316086592));
#5810=CARTESIAN_POINT('Ctrl Pts',(2.66615947310275,-1.81811284795101,2.92829612128916));
#5811=CARTESIAN_POINT('Ctrl Pts',(2.6699754587709,-1.79124798235692,2.8666597721788));
#5812=CARTESIAN_POINT('Ctrl Pts',(2.67379108292622,-1.76438566184409,2.80502926227567));
#5813=CARTESIAN_POINT('Ctrl Pts',(2.67760670708154,-1.73433677346274,2.74478258014596));
#5814=CARTESIAN_POINT('Ctrl Pts',(2.68142233123687,-1.70128123276077,2.68627108023425));
#5815=CARTESIAN_POINT('Ctrl Pts',(2.68524158368121,-1.66819425944109,2.62770394155307));
#5816=CARTESIAN_POINT('Ctrl Pts',(2.68906083612556,-1.63209518231168,2.57087572752999));
#5817=CARTESIAN_POINT('Ctrl Pts',(2.6928800885699,-1.59320886633476,2.51611134358329));
#5818=CARTESIAN_POINT('Ctrl Pts',(2.6967013208578,-1.55430239227105,2.46131857059595));
#5819=CARTESIAN_POINT('Ctrl Pts',(2.70052255314571,-1.51260612827225,2.40859215759306));
#5820=CARTESIAN_POINT('Ctrl Pts',(2.70434378543361,-1.46838516792302,2.35822380517379));
#5821=CARTESIAN_POINT('Ctrl Pts',(2.70817168727,-1.42408702466089,2.30776754023233));
#5822=CARTESIAN_POINT('Ctrl Pts',(2.71199958910638,-1.37725575526887,2.25967791328992));
#5823=CARTESIAN_POINT('Ctrl Pts',(2.71582749094276,-1.32819236692954,2.21420884303147));
#5824=CARTESIAN_POINT('Ctrl Pts',(2.71790335434256,-1.30158539097325,2.18955105847827));
#5825=CARTESIAN_POINT('Ctrl Pts',(2.71997921774236,-1.27432254066741,2.16566323416872));
#5826=CARTESIAN_POINT('Ctrl Pts',(2.72205508114215,-1.24645540150732,2.14258054887282));
#5827=CARTESIAN_POINT('Ctrl Pts',(2.72597896352972,-1.19377978877061,2.09894870763556));
#5828=CARTESIAN_POINT('Ctrl Pts',(2.72990284591728,-1.1387078737066,2.0580010704438));
#5829=CARTESIAN_POINT('Ctrl Pts',(2.73382672830484,-1.0815439821845,2.02001048943914));
#5830=CARTESIAN_POINT('Ctrl Pts',(2.73774471994961,-1.02446590816368,1.98207694193321));
#5831=CARTESIAN_POINT('Ctrl Pts',(2.74166271159438,-0.965302496310311,1.94709190850392));
#5832=CARTESIAN_POINT('Ctrl Pts',(2.74558070323916,-0.904390978508758,1.91528795943634));
#5833=CARTESIAN_POINT('Ctrl Pts',(2.74949407661558,-0.843551259159038,1.88352149875172));
#5834=CARTESIAN_POINT('Ctrl Pts',(2.75340744999201,-0.780967959127539,1.85492890052282));
#5835=CARTESIAN_POINT('Ctrl Pts',(2.75732082336844,-0.717005575465294,1.82969839777272));
#5836=CARTESIAN_POINT('Ctrl Pts',(2.76123173332034,-0.653083455404191,1.80448377734034));
#5837=CARTESIAN_POINT('Ctrl Pts',(2.76514264327225,-0.587784428964692,1.78262723308188));
#5838=CARTESIAN_POINT('Ctrl Pts',(2.76905355322415,-0.521494381419604,1.76426950956557));
#5839=CARTESIAN_POINT('Ctrl Pts',(2.77296333134663,-0.455223518418963,1.74591709883114));
#5840=CARTESIAN_POINT('Ctrl Pts',(2.77687310946912,-0.38796267590892,1.73106162924765));
#5841=CARTESIAN_POINT('Ctrl Pts',(2.7807828875916,-0.320112646580565,1.71979391487578));
#5842=CARTESIAN_POINT('Ctrl Pts',(2.78469286381552,-0.252259179413235,1.70852562958908));
#5843=CARTESIAN_POINT('Ctrl Pts',(2.78860284003943,-0.183816950128083,1.70084553823986));
#5844=CARTESIAN_POINT('Ctrl Pts',(2.79251281626334,-0.115194905210512,1.69679298827481));
#5845=CARTESIAN_POINT('Ctrl Pts',(2.7964268527083,-0.0465016013759045,1.69273623003643));
#5846=CARTESIAN_POINT('Ctrl Pts',(2.80034088915327,0.022371400493301,1.69231455996694));
#5847=CARTESIAN_POINT('Ctrl Pts',(2.80425492559823,0.0910131025772247,1.69551521608632));
#5848=CARTESIAN_POINT('Ctrl Pts',(2.8081712582225,0.159695073488003,1.69871774987865));
#5849=CARTESIAN_POINT('Ctrl Pts',(2.81208759084677,0.228144986629836,1.70554679127174));
#5850=CARTESIAN_POINT('Ctrl Pts',(2.81600392347104,0.29595769599616,1.71593775321603));
#5851=CARTESIAN_POINT('Ctrl Pts',(2.8199268620398,0.363884789669683,1.72634624230227));
#5852=CARTESIAN_POINT('Ctrl Pts',(2.82384980060857,0.43117205460507,1.74032854398275));
#5853=CARTESIAN_POINT('Ctrl Pts',(2.82777273917733,0.497426112609791,1.75776930373564));
#5854=CARTESIAN_POINT('Ctrl Pts',(2.82954270002263,0.527318777624899,1.765638267609));
#5855=CARTESIAN_POINT('Ctrl Pts',(2.83131266086794,0.557001347279425,1.77421058611092));
#5856=CARTESIAN_POINT('Ctrl Pts',(2.83308262171324,0.586438997343527,1.78347244674039));
#5857=CARTESIAN_POINT('Ctrl Pts',(2.83700779777913,0.651721774515743,1.80401212916604));
#5858=CARTESIAN_POINT('Ctrl Pts',(2.84093297384501,0.71604823677107,1.82802469709653));
#5859=CARTESIAN_POINT('Ctrl Pts',(2.8448581499109,0.779023915909599,1.8554017957428));
#5860=CARTESIAN_POINT('Ctrl Pts',(2.84877757921274,0.841907393739763,1.88273881218038));
#5861=CARTESIAN_POINT('Ctrl Pts',(2.85269700851457,0.90344356815947,1.91343038786905));
#5862=CARTESIAN_POINT('Ctrl Pts',(2.85661643781641,0.96325406217776,1.94731870182579));
#5863=CARTESIAN_POINT('Ctrl Pts',(2.86053145588644,1.02299724079535,1.98116887522759));
#5864=CARTESIAN_POINT('Ctrl Pts',(2.86444647395646,1.08101817229185,2.01820840059012));
#5865=CARTESIAN_POINT('Ctrl Pts',(2.86836149202648,1.13696100915589,2.05823253076484));
#5866=CARTESIAN_POINT('Ctrl Pts',(2.87227417452959,1.192870472422,2.09823278390181));
#5867=CARTESIAN_POINT('Ctrl Pts',(2.8761868570327,1.24670390311263,2.14121382493048));
#5868=CARTESIAN_POINT('Ctrl Pts',(2.88009953953581,1.29813382908859,2.18692722737232));
#5869=CARTESIAN_POINT('Ctrl Pts',(2.8840112156736,1.34955052698037,2.23262887205398));
#5870=CARTESIAN_POINT('Ctrl Pts',(2.8879228918114,1.39856458168815,2.28106115747737));
#5871=CARTESIAN_POINT('Ctrl Pts',(2.89183456794919,1.44488245081876,2.33193610584286));
#5872=CARTESIAN_POINT('Ctrl Pts',(2.89574656539129,1.49120412448991,2.38281523306647));
#5873=CARTESIAN_POINT('Ctrl Pts',(2.89965856283338,1.53482884503913,2.43613705771197));
#5874=CARTESIAN_POINT('Ctrl Pts',(2.90357056027547,1.57550194059927,2.49157889685046));
#5875=CARTESIAN_POINT('Ctrl Pts',(2.90748679134103,1.61621905320547,2.54708073599519));
#5876=CARTESIAN_POINT('Ctrl Pts',(2.91140302240658,1.65397787595406,2.60470677256874));
#5877=CARTESIAN_POINT('Ctrl Pts',(2.91531925347213,1.6885664370755,2.66410438515369));
#5878=CARTESIAN_POINT('Ctrl Pts',(2.91923788309565,1.72317618251101,2.72353837675064));
#5879=CARTESIAN_POINT('Ctrl Pts',(2.92315651271918,1.75461157795443,2.78474566821742));
#5880=CARTESIAN_POINT('Ctrl Pts',(2.9270751423427,1.78270739879702,2.84735051306993));
#5881=CARTESIAN_POINT('Ctrl Pts',(2.93100051228645,1.81085154643947,2.91006304268541));
#5882=CARTESIAN_POINT('Ctrl Pts',(2.9349258822302,1.83564447823696,2.97417746692774));
#5883=CARTESIAN_POINT('Ctrl Pts',(2.93885125217395,1.85697002178265,3.03930044742808));
#5884=CARTESIAN_POINT('Ctrl Pts',(2.94060422221074,1.86649346527703,3.06838270850395));
#5885=CARTESIAN_POINT('Ctrl Pts',(2.94235719224753,1.87532608795664,3.09766593971382));
#5886=CARTESIAN_POINT('Ctrl Pts',(2.94411016228432,1.88346084202322,3.1271144892676));
#5887=CARTESIAN_POINT('Ctrl Pts',(2.9480236060212,1.90162139336457,3.19285733677376));
#5888=CARTESIAN_POINT('Ctrl Pts',(2.95193704975808,1.91637244034916,3.25968545217464));
#5889=CARTESIAN_POINT('Ctrl Pts',(2.95585049349497,1.92758891674177,3.32721175786014));
#5890=CARTESIAN_POINT('Ctrl Pts',(2.95975797103281,1.93878829317455,3.39463511703428));
#5891=CARTESIAN_POINT('Ctrl Pts',(2.96366544857066,1.94646371236138,3.46275407167435));
#5892=CARTESIAN_POINT('Ctrl Pts',(2.9675729261085,1.950540275588,3.53116782198833));
#5893=CARTESIAN_POINT('Ctrl Pts',(2.97147572681058,1.95461195960123,3.59949968830653));
#5894=CARTESIAN_POINT('Ctrl Pts',(2.97537852751266,1.95509331260623,3.6681251596545));
#5895=CARTESIAN_POINT('Ctrl Pts',(2.97928132821474,1.95196102673349,3.7366365554038));
#5896=CARTESIAN_POINT('Ctrl Pts',(2.98318163565292,1.94883074188923,3.80510418335578));
#5897=CARTESIAN_POINT('Ctrl Pts',(2.98708194309109,1.94209141961315,3.8734573886953));
#5898=CARTESIAN_POINT('Ctrl Pts',(2.99098225052927,1.93177183353233,3.94128829804409));
#5899=CARTESIAN_POINT('Ctrl Pts',(2.9948814128957,1.92145527712716,4.00909929325557));
#5900=CARTESIAN_POINT('Ctrl Pts',(2.99878057526213,1.90756061748983,4.07638780947079));
#5901=CARTESIAN_POINT('Ctrl Pts',(3.00267973762855,1.89016829610894,4.14275273498043));
#5902=CARTESIAN_POINT('Ctrl Pts',(3.00657910142912,1.87277507622552,4.20912108896016));
#5903=CARTESIAN_POINT('Ctrl Pts',(3.01047846522969,1.85188396342224,4.27456528104707));
#5904=CARTESIAN_POINT('Ctrl Pts',(3.01437782903025,1.82762570351886,4.33869779377652));
#5905=CARTESIAN_POINT('Ctrl Pts',(3.01828133160984,1.80334169593394,4.40289837666106));
#5906=CARTESIAN_POINT('Ctrl Pts',(3.02218483418944,1.77568358378569,4.46578403956246));
#5907=CARTESIAN_POINT('Ctrl Pts',(3.02608833676903,1.7448305018353,4.52698671464874));
#5908=CARTESIAN_POINT('Ctrl Pts',(3.02999416525936,1.71395903600712,4.58822585748564));
#5909=CARTESIAN_POINT('Ctrl Pts',(3.03389999374968,1.67988905689783,4.64777958873476));
#5910=CARTESIAN_POINT('Ctrl Pts',(3.03780582224,1.64284456515422,4.70530643756262));
#5911=CARTESIAN_POINT('Ctrl Pts',(3.04171841300615,1.60573593719169,4.7629328843171));
#5912=CARTESIAN_POINT('Ctrl Pts',(3.04563100377231,1.5656428070228,4.81852504529772));
#5913=CARTESIAN_POINT('Ctrl Pts',(3.04954359453846,1.52283064471812,4.87177301575495));
#5914=CARTESIAN_POINT('Ctrl Pts',(3.05140829731077,1.50242678382146,4.8971504814972));
#5915=CARTESIAN_POINT('Ctrl Pts',(3.05327300008308,1.48140588582222,4.92199601484909));
#5916=CARTESIAN_POINT('Ctrl Pts',(3.05513770285539,1.45979955695045,4.94627908730408));
#5917=CARTESIAN_POINT('Ctrl Pts',(3.05905724628881,1.41438376966934,4.9973213008931));
#5918=CARTESIAN_POINT('Ctrl Pts',(3.06297678972224,1.36619821726603,5.04607926715039));
#5919=CARTESIAN_POINT('Ctrl Pts',(3.06689633315566,1.31550159430471,5.09223755851262));
#5920=CARTESIAN_POINT('Ctrl Pts',(3.07080998965572,1.26488111481424,5.13832652272232));
#5921=CARTESIAN_POINT('Ctrl Pts',(3.07472364615578,1.21175741053974,5.18182323319347));
#5922=CARTESIAN_POINT('Ctrl Pts',(3.07863730265584,1.15642783819774,5.22244705630793));
#5923=CARTESIAN_POINT('Ctrl Pts',(3.08254636936972,1.10116315425515,5.26302323736141));
#5924=CARTESIAN_POINT('Ctrl Pts',(3.08645543608361,1.04369813440837,5.30073293304372));
#5925=CARTESIAN_POINT('Ctrl Pts',(3.09036450279749,0.984363832719194,5.33533517957511));
#5926=CARTESIAN_POINT('Ctrl Pts',(3.09427112673113,0.92506660910272,5.36991580312324));
#5927=CARTESIAN_POINT('Ctrl Pts',(3.09817775066478,0.863902844490097,5.40139258262384));
#5928=CARTESIAN_POINT('Ctrl Pts',(3.10208437459842,0.801231943442729,5.42956824567119));
#5929=CARTESIAN_POINT('Ctrl Pts',(3.10598989441529,0.738578754874032,5.45773594551995));
#5930=CARTESIAN_POINT('Ctrl Pts',(3.10989541423216,0.674419723535876,5.48260417968945));
#5931=CARTESIAN_POINT('Ctrl Pts',(3.11380093404903,0.609136553962107,5.50402277212586));
#5932=CARTESIAN_POINT('Ctrl Pts',(3.1177066867749,0.543849491171074,5.52544264187822));
#5933=CARTESIAN_POINT('Ctrl Pts',(3.12161243950076,0.477438624815858,5.54341231069807));
#5934=CARTESIAN_POINT('Ctrl Pts',(3.12551819222662,0.410301499896432,5.55783124535417));
#5935=CARTESIAN_POINT('Ctrl Pts',(3.12942808785887,0.343093161348362,5.5722654744492));
#5936=CARTESIAN_POINT('Ctrl Pts',(3.13333798349113,0.27515750827182,5.58314134960697));
#5937=CARTESIAN_POINT('Ctrl Pts',(3.13724787912339,0.206901985992685,5.59040953981376));
#5938=CARTESIAN_POINT('Ctrl Pts',(3.14116011246107,0.138605654106479,5.59768207563209));
#5939=CARTESIAN_POINT('Ctrl Pts',(3.14507234579874,0.0699895632146808,5.60134260730777));
#5940=CARTESIAN_POINT('Ctrl Pts',(3.14898457913642,0.0014631717957429,5.60139392046606));
#5941=CARTESIAN_POINT('Ctrl Pts',(3.15290352589339,-0.0671808113816727,
5.60144532167808));
#5942=CARTESIAN_POINT('Ctrl Pts',(3.15682247265035,-0.135734297356499,5.59787516888501));
#5943=CARTESIAN_POINT('Ctrl Pts',(3.16074141940731,-0.203791822251691,5.59073820864051));
#5944=CARTESIAN_POINT('Ctrl Pts',(3.16254936074703,-0.235189036954434,5.5874456899445));
#5945=CARTESIAN_POINT('Ctrl Pts',(3.16435730208675,-0.266480827607967,5.58339477144296));
#5946=CARTESIAN_POINT('Ctrl Pts',(3.16616524342647,-0.297628256975112,5.57859446327402));
#5947=CARTESIAN_POINT('Ctrl Pts',(3.1700845073386,-0.365149803826313,5.56818833218987));
#5948=CARTESIAN_POINT('Ctrl Pts',(3.17400377125072,-0.432257843245543,5.5542162717806));
#5949=CARTESIAN_POINT('Ctrl Pts',(3.17792303516284,-0.498547063155574,5.53672419753151));
#5950=CARTESIAN_POINT('Ctrl Pts',(3.18183642540956,-0.564736937702167,5.5192583380497));
#5951=CARTESIAN_POINT('Ctrl Pts',(3.18574981565628,-0.630109956738539,5.49828305905177));
#5952=CARTESIAN_POINT('Ctrl Pts',(3.189663205903,-0.694269029376674,5.47389563577552));
#5953=CARTESIAN_POINT('Ctrl Pts',(3.19357202746939,-0.758353199622102,5.44953668355224));
#5954=CARTESIAN_POINT('Ctrl Pts',(3.19748084903578,-0.821225780809679,5.42177367228869));
#5955=CARTESIAN_POINT('Ctrl Pts',(3.20138967060217,-0.8825046924029,5.39075371636984));
#5956=CARTESIAN_POINT('Ctrl Pts',(3.20529606267586,-0.943745516642773,5.35975304062406));
#5957=CARTESIAN_POINT('Ctrl Pts',(3.20920245474956,-1.00339419865752,5.32549965745876));
#5958=CARTESIAN_POINT('Ctrl Pts',(3.21310884682325,-1.06108995211075,5.28818821325294));
#5959=CARTESIAN_POINT('Ctrl Pts',(3.21701414846881,-1.11876960040304,5.25088718414316));
#5960=CARTESIAN_POINT('Ctrl Pts',(3.22091945011436,-1.17449698980819,5.21053005545042));
#5961=CARTESIAN_POINT('Ctrl Pts',(3.22482475175992,-1.22793877375843,5.1673557730218));
#5962=CARTESIAN_POINT('Ctrl Pts',(3.2287303004185,-1.28138393793846,5.12417875978997));
#5963=CARTESIAN_POINT('Ctrl Pts',(3.23263584907708,-1.33254282891501,5.07818454995117));
#5964=CARTESIAN_POINT('Ctrl Pts',(3.23654139773567,-1.38111518643624,5.0296523464655));
#5965=CARTESIAN_POINT('Ctrl Pts',(3.24045111216644,-1.4297393526517,4.98106837711507));
#5966=CARTESIAN_POINT('Ctrl Pts',(3.24436082659722,-1.47577113126628,4.92994135975682));
#5967=CARTESIAN_POINT('Ctrl Pts',(3.248270541028,-1.51894788216773,4.87658661406831));
#5968=CARTESIAN_POINT('Ctrl Pts',(3.25218260598123,-1.56215059095551,4.82319979147743));
#5969=CARTESIAN_POINT('Ctrl Pts',(3.25609467093447,-1.6024945673085,4.76758297297988));
#5970=CARTESIAN_POINT('Ctrl Pts',(3.2600067358877,-1.6397598443748,4.7100814648995));
#5971=CARTESIAN_POINT('Ctrl Pts',(3.26392553588139,-1.67708927762243,4.65248096179023));
#5972=CARTESIAN_POINT('Ctrl Pts',(3.26784433587508,-1.71132918811501,4.59298971906679));
#5973=CARTESIAN_POINT('Ctrl Pts',(3.27176313586877,-1.74230541245399,4.53197790116826));
#5974=CARTESIAN_POINT('Ctrl Pts',(3.27357301857837,-1.75661166256368,4.50379982765771));
#5975=CARTESIAN_POINT('Ctrl Pts',(3.27538290128796,-1.77022243794753,4.47529769357849));
#5976=CARTESIAN_POINT('Ctrl Pts',(3.27719278399755,-1.7831241210405,4.44650920908367));
#5977=CARTESIAN_POINT('Ctrl Pts',(3.2814779271289,-1.8136706080563,4.37834856202015));
#5978=CARTESIAN_POINT('Ctrl Pts',(3.28576307026025,-1.84034342649034,4.30834888308732));
#5979=CARTESIAN_POINT('Ctrl Pts',(3.29004821339159,-1.8629392632888,4.23694794448174));
#5980=CARTESIAN_POINT('Ctrl Pts',(3.29432122677543,-1.88547113914435,4.16574911706143));
#5981=CARTESIAN_POINT('Ctrl Pts',(3.29859424015927,-1.90394890645761,4.09315724465676));
#5982=CARTESIAN_POINT('Ctrl Pts',(3.3028672535431,-1.91821713524752,4.01962963863027));
#5983=CARTESIAN_POINT('Ctrl Pts',(3.30712062229899,-1.93241976769572,3.94644006628971));
#5984=CARTESIAN_POINT('Ctrl Pts',(3.31137399105488,-1.94245134242051,3.87232365766614));
#5985=CARTESIAN_POINT('Ctrl Pts',(3.31562735981078,-1.94820666808604,3.79774997508393));
#5986=CARTESIAN_POINT('Ctrl Pts',(3.31846167581925,-1.95204184265095,3.74805633352957));
#5987=CARTESIAN_POINT('Ctrl Pts',(3.32129599182773,-1.95397914847566,3.698160016538));
#5988=CARTESIAN_POINT('Ctrl Pts',(3.3241303078362,-1.95399983251307,3.64820350405597));
#5989=CARTESIAN_POINT('Origin',(0.,0.,3.64739446828387));
#5990=CARTESIAN_POINT('',(4.12586969212423,-1.95399924590383,3.64567778332306));
#5991=CARTESIAN_POINT('',(4.02413030792419,-1.95399922086733,3.64564951846532));
#5992=CARTESIAN_POINT('',(0.,-1.954,3.64739446828387));
#5993=CARTESIAN_POINT('Ctrl Pts',(4.12586969212423,-1.95399924590383,3.64567778332306));
#5994=CARTESIAN_POINT('Ctrl Pts',(4.12199411980701,-1.95405905160708,3.71375101849607));
#5995=CARTESIAN_POINT('Ctrl Pts',(4.11811854748978,-1.95055728305734,3.78189644852607));
#5996=CARTESIAN_POINT('Ctrl Pts',(4.11424297517256,-1.94349799785706,3.84970989608311));
#5997=CARTESIAN_POINT('Ctrl Pts',(4.11036920668271,-1.93644199829586,3.91749178088173));
#5998=CARTESIAN_POINT('Ctrl Pts',(4.10649543819285,-1.92583181766029,3.98494149260619));
#5999=CARTESIAN_POINT('Ctrl Pts',(4.102621669703,-1.91172349358431,4.05165834754814));
#6000=CARTESIAN_POINT('Ctrl Pts',(4.09874832349887,-1.89761670747941,4.11836792957855));
#6001=CARTESIAN_POINT('Ctrl Pts',(4.09487497729474,-1.88001263979045,4.18434432418101));
#6002=CARTESIAN_POINT('Ctrl Pts',(4.09100163109061,-1.85901836975748,4.24919734373748));
#6003=CARTESIAN_POINT('Ctrl Pts',(4.08712457443049,-1.83800398835026,4.31411248897616));
#6004=CARTESIAN_POINT('Ctrl Pts',(4.08324751777036,-1.81359307231316,4.37790163250603));
#6005=CARTESIAN_POINT('Ctrl Pts',(4.07937046111024,-1.78594218915509,4.44019109857181));
#6006=CARTESIAN_POINT('Ctrl Pts',(4.07549157612676,-1.75827826652926,4.50250993879827));
#6007=CARTESIAN_POINT('Ctrl Pts',(4.07161269114329,-1.7273715618897,4.56332724688191));
#6008=CARTESIAN_POINT('Ctrl Pts',(4.06773380615981,-1.69342499635027,4.62229332546655));
#6009=CARTESIAN_POINT('Ctrl Pts',(4.06384772938108,-1.65941549088091,4.68136873236748));
#6010=CARTESIAN_POINT('Ctrl Pts',(4.05996165260234,-1.62235514002231,4.73858563361905));
#6011=CARTESIAN_POINT('Ctrl Pts',(4.05607557582361,-1.58249024166121,4.79362334379131));
#6012=CARTESIAN_POINT('Ctrl Pts',(4.05283923950414,-1.54929063553293,4.83945891280168));
#6013=CARTESIAN_POINT('Ctrl Pts',(4.04960290318466,-1.5141467635391,4.8837835390167));
#6014=CARTESIAN_POINT('Ctrl Pts',(4.04636656686519,-1.47722071628238,4.92643119777453));
#6015=CARTESIAN_POINT('Ctrl Pts',(4.04244807472578,-1.43251138708061,4.97806814125327));
#6016=CARTESIAN_POINT('Ctrl Pts',(4.03852958258636,-1.38500289026933,5.02746012816018));
#6017=CARTESIAN_POINT('Ctrl Pts',(4.03461109044695,-1.33494940519814,5.07428832753239));
#6018=CARTESIAN_POINT('Ctrl Pts',(4.03069848988681,-1.28497117715565,5.12104611919694));
#6019=CARTESIAN_POINT('Ctrl Pts',(4.02678588932668,-1.23245591134374,5.16524744040475));
#6020=CARTESIAN_POINT('Ctrl Pts',(4.02287328876654,-1.17769692864366,5.20660771356602));
#6021=CARTESIAN_POINT('Ctrl Pts',(4.018965279537,-1.12300220412392,5.24791945156902));
#6022=CARTESIAN_POINT('Ctrl Pts',(4.01505727030746,-1.06606938237395,5.28639646773815));
#6023=CARTESIAN_POINT('Ctrl Pts',(4.01114926107791,-1.00722602659854,5.32179338471404));
#6024=CARTESIAN_POINT('Ctrl Pts',(4.00724369493527,-0.948419456670685,5.35716817335318));
#6025=CARTESIAN_POINT('Ctrl Pts',(4.00333812879263,-0.887705142448082,5.38946642953741));
#6026=CARTESIAN_POINT('Ctrl Pts',(3.99943256264998,-0.825439595234824,5.4184860736557));
#6027=CARTESIAN_POINT('Ctrl Pts',(3.99552809927701,-0.763191629226074,5.44749752383175));
#6028=CARTESIAN_POINT('Ctrl Pts',(3.99162363590404,-0.699393745279336,5.47323199209042));
#6029=CARTESIAN_POINT('Ctrl Pts',(3.98771917253107,-0.634425395958315,5.4955341862065));
#6030=CARTESIAN_POINT('Ctrl Pts',(3.98381447324754,-0.569453121201594,5.51783772783764));
#6031=CARTESIAN_POINT('Ctrl Pts',(3.97990977396401,-0.503310706622887,5.5367084263743));
#6032=CARTESIAN_POINT('Ctrl Pts',(3.97600507468047,-0.436394118018742,5.55204041274668));
#6033=CARTESIAN_POINT('Ctrl Pts',(3.97209622064834,-0.369406327618353,5.56738871293591));
#6034=CARTESIAN_POINT('Ctrl Pts',(3.96818736661621,-0.301643199518616,5.57919067659121));
#6035=CARTESIAN_POINT('Ctrl Pts',(3.96427851258407,-0.233511292379936,5.58739149826383));
#6036=CARTESIAN_POINT('Ctrl Pts',(3.96036731558006,-0.165338546892934,5.59559723551896));
#6037=CARTESIAN_POINT('Ctrl Pts',(3.95645611857605,-0.0967970731618409,
5.60019750197601));
#6038=CARTESIAN_POINT('Ctrl Pts',(3.95254492157203,-0.0282961421001321,
5.60118957738366));
#6039=CARTESIAN_POINT('Ctrl Pts',(3.94862699211985,0.0403227014490757,5.60218336047727));
#6040=CARTESIAN_POINT('Ctrl Pts',(3.94470906266767,0.108900371926006,5.59955657561392));
#6041=CARTESIAN_POINT('Ctrl Pts',(3.94079113321549,0.177030896039916,5.59335851261956));
#6042=CARTESIAN_POINT('Ctrl Pts',(3.9389737642417,0.208633889969279,5.5904834819379));
#6043=CARTESIAN_POINT('Ctrl Pts',(3.93715639526791,0.240140795167076,5.58684076103467));
#6044=CARTESIAN_POINT('Ctrl Pts',(3.93533902629411,0.271511933329578,5.58243898199916));
#6045=CARTESIAN_POINT('Ctrl Pts',(3.93142052909791,0.339152417295069,5.57294814163727));
#6046=CARTESIAN_POINT('Ctrl Pts',(3.92750203190172,0.4064284310436,5.5598876511501));
#6047=CARTESIAN_POINT('Ctrl Pts',(3.92358353470552,0.472934213080639,5.54329774379605));
#6048=CARTESIAN_POINT('Ctrl Pts',(3.91967092903786,0.539340002520195,5.52673277965561));
#6049=CARTESIAN_POINT('Ctrl Pts',(3.9157583233702,0.604977385279625,5.50664904841392));
#6050=CARTESIAN_POINT('Ctrl Pts',(3.91184571770254,0.669448099006128,5.48313825289464));
#6051=CARTESIAN_POINT('Ctrl Pts',(3.90793770331604,0.733843159012707,5.45965504632291));
#6052=CARTESIAN_POINT('Ctrl Pts',(3.90402968892955,0.797073809110116,5.43275293001398));
#6053=CARTESIAN_POINT('Ctrl Pts',(3.90012167454305,0.858756100670228,5.40257364989516));
#6054=CARTESIAN_POINT('Ctrl Pts',(3.89621610321588,0.920399832111779,5.37241323607637));
#6055=CARTESIAN_POINT('Ctrl Pts',(3.89231053188872,0.980496684386062,5.33897993808273));
#6056=CARTESIAN_POINT('Ctrl Pts',(3.88840496056155,1.03868333862023,5.30246332548369));
#6057=CARTESIAN_POINT('Ctrl Pts',(3.88450049198455,1.09685356367234,5.26595702346334));
#6058=CARTESIAN_POINT('Ctrl Pts',(3.88059602340755,1.15311424506722,5.22636939640863));
#6059=CARTESIAN_POINT('Ctrl Pts',(3.87669155483054,1.20712888640244,5.1839346895644));
#6060=CARTESIAN_POINT('Ctrl Pts',(3.87278685033151,1.26114679149643,5.14149741866265));
#6061=CARTESIAN_POINT('Ctrl Pts',(3.86888214583249,1.31291800198357,5.09621303225256));
#6062=CARTESIAN_POINT('Ctrl Pts',(3.86497744133346,1.36213854850416,5.04835648585572));
#6063=CARTESIAN_POINT('Ctrl Pts',(3.86106858210453,1.41141146725322,5.00044901856996));
#6064=CARTESIAN_POINT('Ctrl Pts',(3.85715972287561,1.45812795256836,4.94996427289987));
#6065=CARTESIAN_POINT('Ctrl Pts',(3.85325086364668,1.50202115528847,4.89721383485885));
#6066=CARTESIAN_POINT('Ctrl Pts',(3.84933966144904,1.54594066757743,4.84443177822555));
#6067=CARTESIAN_POINT('Ctrl Pts',(3.8454284592514,1.58703323512623,4.78938172056141));
#6068=CARTESIAN_POINT('Ctrl Pts',(3.84151725705375,1.62507426724836,4.73240581657807));
#6069=CARTESIAN_POINT('Ctrl Pts',(3.83759932246746,1.66318077975223,4.67533183944228));
#6070=CARTESIAN_POINT('Ctrl Pts',(3.83368138788116,1.6982250226033,4.61632582249884));
#6071=CARTESIAN_POINT('Ctrl Pts',(3.82976345329487,1.73002786493561,4.55575540235487));
#6072=CARTESIAN_POINT('Ctrl Pts',(3.82794613077092,1.74477952053959,4.52765998973685));
#6073=CARTESIAN_POINT('Ctrl Pts',(3.82612880824698,1.75883445140535,4.49922828152488));
#6074=CARTESIAN_POINT('Ctrl Pts',(3.82431148572303,1.77217835395763,4.47049827811835));
#6075=CARTESIAN_POINT('Ctrl Pts',(3.82039300905922,1.80095022580008,4.40855118484431));
#6076=CARTESIAN_POINT('Ctrl Pts',(3.8164745323954,1.8265270178764,4.34497116695154));
#6077=CARTESIAN_POINT('Ctrl Pts',(3.81255605573159,1.84872211032279,4.28012075887377));
#6078=CARTESIAN_POINT('Ctrl Pts',(3.80864347063613,1.87088383166211,4.21536785567986));
#6079=CARTESIAN_POINT('Ctrl Pts',(3.80473088554067,1.88967378643479,4.14934881470658));
#6080=CARTESIAN_POINT('Ctrl Pts',(3.80081830044521,1.90495264280254,4.08244783130918));
#6081=CARTESIAN_POINT('Ctrl Pts',(3.79691030659027,1.92021357012777,4.01562535317073));
#6082=CARTESIAN_POINT('Ctrl Pts',(3.79300231273533,1.93197147273745,3.9479234651545));
#6083=CARTESIAN_POINT('Ctrl Pts',(3.7890943188804,1.94013681071575,3.87974152702515));
#6084=CARTESIAN_POINT('Ctrl Pts',(3.78518876804767,1.94829704425869,3.81160221178502));
#6085=CARTESIAN_POINT('Ctrl Pts',(3.78128321721494,1.95286910989961,3.74298392892463));
#6086=CARTESIAN_POINT('Ctrl Pts',(3.77737766638221,1.95381482691184,3.6742946939236));
#6087=CARTESIAN_POINT('Ctrl Pts',(3.77347321823199,1.95476027691292,3.60562485245269));
#6088=CARTESIAN_POINT('Ctrl Pts',(3.76956877008177,1.95208140407651,3.53688459010406));
#6089=CARTESIAN_POINT('Ctrl Pts',(3.76566432193155,1.94579210753576,3.4684836685776));
#6090=CARTESIAN_POINT('Ctrl Pts',(3.76175963776104,1.93950243081285,3.40007861227866));
#6091=CARTESIAN_POINT('Ctrl Pts',(3.75785495359054,1.92960194468172,3.33201342699205));
#6092=CARTESIAN_POINT('Ctrl Pts',(3.75395026942003,1.91615639730594,3.26469267698481));
#6093=CARTESIAN_POINT('Ctrl Pts',(3.75004143023388,1.90269654238124,3.19730029025668));
#6094=CARTESIAN_POINT('Ctrl Pts',(3.74613259104772,1.88568419438441,3.1306544028623));
#6095=CARTESIAN_POINT('Ctrl Pts',(3.74222375186156,1.86523601993753,3.06514830906286));
#6096=CARTESIAN_POINT('Ctrl Pts',(3.73831256957263,1.84477558809861,2.99960294848809));
#6097=CARTESIAN_POINT('Ctrl Pts',(3.73440138728369,1.82087540201003,2.93519920237402));
#6098=CARTESIAN_POINT('Ctrl Pts',(3.73049020499476,1.79370074809955,2.87231148803781));
#6099=CARTESIAN_POINT('Ctrl Pts',(3.72657228990375,1.76647931509443,2.80931551729655));
#6100=CARTESIAN_POINT('Ctrl Pts',(3.72265437481273,1.73597238288057,2.74784122711538));
#6101=CARTESIAN_POINT('Ctrl Pts',(3.71873645972171,1.70239132559535,2.68823870693032));
#6102=CARTESIAN_POINT('Ctrl Pts',(3.71691895486513,1.68681320986613,2.66058934052384));
#6103=CARTESIAN_POINT('Ctrl Pts',(3.71510145000855,1.67057415673778,2.63334236908991));
#6104=CARTESIAN_POINT('Ctrl Pts',(3.71328394515196,1.65369831032235,2.60653045294036));
#6105=CARTESIAN_POINT('Ctrl Pts',(3.709365444375,1.61731435401475,2.5487245472872));
#6106=CARTESIAN_POINT('Ctrl Pts',(3.70544694359804,1.57782384186816,2.49271435131038));
#6107=CARTESIAN_POINT('Ctrl Pts',(3.70152844282107,1.53542980063071,2.43885347711512));
#6108=CARTESIAN_POINT('Ctrl Pts',(3.69761583371803,1.49309950108459,2.38507358560323));
#6109=CARTESIAN_POINT('Ctrl Pts',(3.69370322461499,1.44787463843252,2.3334369855227));
#6110=CARTESIAN_POINT('Ctrl Pts',(3.68979061551194,1.40000211194106,2.28426935056335));
#6111=CARTESIAN_POINT('Ctrl Pts',(3.68588259791834,1.35218576462613,2.23515941461106));
#6112=CARTESIAN_POINT('Ctrl Pts',(3.68197458032474,1.30172826565825,2.18851304019558));
#6113=CARTESIAN_POINT('Ctrl Pts',(3.67806656273114,1.24891629228578,2.1446223315768));
#6114=CARTESIAN_POINT('Ctrl Pts',(3.67416098833998,1.19613733574069,2.10075906241648));
#6115=CARTESIAN_POINT('Ctrl Pts',(3.67025541394882,1.1410072020901,2.05964835518222));
#6116=CARTESIAN_POINT('Ctrl Pts',(3.66634983955766,1.08384773311687,2.0215438935331));
#6117=CARTESIAN_POINT('Ctrl Pts',(3.66244536806308,1.02670440542709,1.9834501922169));
#6118=CARTESIAN_POINT('Ctrl Pts',(3.65854089656851,0.967533289053315,1.94836132382126));
#6119=CARTESIAN_POINT('Ctrl Pts',(3.65463642507394,0.906685980489135,1.91648819329829));
#6120=CARTESIAN_POINT('Ctrl Pts',(3.65073171780722,0.845834997650355,1.88461313811117));
#6121=CARTESIAN_POINT('Ctrl Pts',(3.6468270105405,0.783308058479606,1.85595443221992));
#6122=CARTESIAN_POINT('Ctrl Pts',(3.64292230327378,0.719480558858603,1.83067662408667));
#6123=CARTESIAN_POINT('Ctrl Pts',(3.63901344151935,0.655585148752814,1.80537192114766));
#6124=CARTESIAN_POINT('Ctrl Pts',(3.63510457976491,0.590386874765151,1.78345547613772));
#6125=CARTESIAN_POINT('Ctrl Pts',(3.63119571801047,0.52427932807126,1.76504296387319));
#6126=CARTESIAN_POINT('Ctrl Pts',(3.62728451342184,0.458132158840093,1.74661941579672));
#6127=CARTESIAN_POINT('Ctrl Pts',(3.62337330883321,0.391075112365833,1.7317040869153));
#6128=CARTESIAN_POINT('Ctrl Pts',(3.61946210424458,0.323512339794136,1.72036157650415));
#6129=CARTESIAN_POINT('Ctrl Pts',(3.61554416749687,0.255833274831545,1.70899954280222));
#6130=CARTESIAN_POINT('Ctrl Pts',(3.61162623074917,0.187647234771641,1.70122265691404));
#6131=CARTESIAN_POINT('Ctrl Pts',(3.60770829400146,0.119362978637942,1.69704360771271));
#6132=CARTESIAN_POINT('Ctrl Pts',(3.60589099752793,0.0876899972041078,1.69510519679254));
#6133=CARTESIAN_POINT('Ctrl Pts',(3.60407370105441,0.0559958742510644,1.69394011591223));
#6134=CARTESIAN_POINT('Ctrl Pts',(3.60225640458088,0.0243211323379382,1.69354583481151));
#6135=CARTESIAN_POINT('Ctrl Pts',(3.59833787824393,-0.0439771955413948,
1.69269567035028));
#6136=CARTESIAN_POINT('Ctrl Pts',(3.59441935190697,-0.112455204635342,1.69542926853146));
#6137=CARTESIAN_POINT('Ctrl Pts',(3.59050082557002,-0.180705710999077,1.70176823336301));
#6138=CARTESIAN_POINT('Ctrl Pts',(3.58658819053925,-0.248853606177836,1.70809766788149));
#6139=CARTESIAN_POINT('Ctrl Pts',(3.58267555550849,-0.316774191731215,1.71802166608975));
#6140=CARTESIAN_POINT('Ctrl Pts',(3.57876292047773,-0.384059911532484,1.73150982030695));
#6141=CARTESIAN_POINT('Ctrl Pts',(3.57485487654503,-0.451266678061753,1.74498214748221));
#6142=CARTESIAN_POINT('Ctrl Pts',(3.57094683261233,-0.517839578446989,1.76201022850709));
#6143=CARTESIAN_POINT('Ctrl Pts',(3.56703878867963,-0.583377636205339,1.78251202330899));
#6144=CARTESIAN_POINT('Ctrl Pts',(3.56313318771024,-0.648874725368399,1.80300100220267));
#6145=CARTESIAN_POINT('Ctrl Pts',(3.55922758674084,-0.713337786867189,1.82695924084957));
#6146=CARTESIAN_POINT('Ctrl Pts',(3.55532198577145,-0.776379002835167,1.85425430534159));
#6147=CARTESIAN_POINT('Ctrl Pts',(3.55141748750173,-0.839402419870669,1.88154166339898));
#6148=CARTESIAN_POINT('Ctrl Pts',(3.547512989232,-0.901004337255898,1.91216378171569));
#6149=CARTESIAN_POINT('Ctrl Pts',(3.54360849096228,-0.960816693256813,1.94594000754769));
#6150=CARTESIAN_POINT('Ctrl Pts',(3.53970375676551,-1.0206326633847,1.97971827428858));
#6151=CARTESIAN_POINT('Ctrl Pts',(3.53579902256873,-1.0786584305169,2.01665078287648));
#6152=CARTESIAN_POINT('Ctrl Pts',(3.53189428837196,-1.13455192769951,2.05651171856492));
#6153=CARTESIAN_POINT('Ctrl Pts',(3.52798539964158,-1.19050489408061,2.09641506523167));
#6154=CARTESIAN_POINT('Ctrl Pts',(3.52407651091119,-1.24432066185106,2.13925277096336));
#6155=CARTESIAN_POINT('Ctrl Pts',(3.5201676221808,-1.29568831620729,2.18475719703583));
#6156=CARTESIAN_POINT('Ctrl Pts',(3.51625639055101,-1.34708675917252,2.23028889743101));
#6157=CARTESIAN_POINT('Ctrl Pts',(3.51234515892122,-1.3960338180056,2.27849015414664));
#6158=CARTESIAN_POINT('Ctrl Pts',(3.50843392729142,-1.44225572602493,2.32905671916633));
#6159=CARTESIAN_POINT('Ctrl Pts',(3.50451596368841,-1.48855719073542,2.37971031885788));
#6160=CARTESIAN_POINT('Ctrl Pts',(3.50059800008541,-1.53212383128964,2.43273697234076));
#6161=CARTESIAN_POINT('Ctrl Pts',(3.4966800364824,-1.57272296308931,2.48780036629318));
#6162=CARTESIAN_POINT('Ctrl Pts',(3.49486297899153,-1.59155186606905,2.51333744692786));
#6163=CARTESIAN_POINT('Ctrl Pts',(3.49304592150067,-1.60974311680241,2.5393122153768));
#6164=CARTESIAN_POINT('Ctrl Pts',(3.4912288640098,-1.62727683669187,2.56568928813259));
#6165=CARTESIAN_POINT('Ctrl Pts',(3.48724042291459,-1.66576335091086,2.62358696141989));
#6166=CARTESIAN_POINT('Ctrl Pts',(3.48325198181939,-1.70122719124068,2.68364762603425));
#6167=CARTESIAN_POINT('Ctrl Pts',(3.47926354072418,-1.73342304991812,2.7455294395725));
#6168=CARTESIAN_POINT('Ctrl Pts',(3.47528172814961,-1.76556540124562,2.80730840970205));
#6169=CARTESIAN_POINT('Ctrl Pts',(3.47129991557503,-1.79445034260521,2.87090210568594));
#6170=CARTESIAN_POINT('Ctrl Pts',(3.46731810300046,-1.81987604930015,2.93594020750271));
#6171=CARTESIAN_POINT('Ctrl Pts',(3.46334277468661,-1.84526035100472,3.00087239674792));
#6172=CARTESIAN_POINT('Ctrl Pts',(3.45936744637276,-1.8671964512743,3.06724388003304));
#6173=CARTESIAN_POINT('Ctrl Pts',(3.45539211805891,-1.8855294599695,3.13466193022225));
#6174=CARTESIAN_POINT('Ctrl Pts',(3.45142059332048,-1.90384492772825,3.20201547513826));
#6175=CARTESIAN_POINT('Ctrl Pts',(3.44744906858206,-1.91856402806981,3.27041314777312));
#6176=CARTESIAN_POINT('Ctrl Pts',(3.44347754384363,-1.92958115826756,3.33944552177032));
#6177=CARTESIAN_POINT('Ctrl Pts',(3.4395087631665,-1.94059067635599,3.40843019895639));
#6178=CARTESIAN_POINT('Ctrl Pts',(3.43553998248937,-1.94790323385196,3.47804824402521));
#6179=CARTESIAN_POINT('Ctrl Pts',(3.43157120181223,-1.95146428769482,3.54787997762178));
#6180=CARTESIAN_POINT('Ctrl Pts',(3.4296706985829,-1.95316954552557,3.581319828802));
#6181=CARTESIAN_POINT('Ctrl Pts',(3.42777019535356,-1.9540153051049,3.61480856012914));
#6182=CARTESIAN_POINT('Ctrl Pts',(3.42586969212423,-1.95399979033479,3.64829965974897));
#6183=CARTESIAN_POINT('Ctrl Pts',(3.32413030787577,-1.95399983251336,3.64820350335859));
#6184=CARTESIAN_POINT('Ctrl Pts',(3.32811085978269,-1.95402888143147,3.57804389856121));
#6185=CARTESIAN_POINT('Ctrl Pts',(3.33209141168961,-1.95027489940237,3.50790303752685));
#6186=CARTESIAN_POINT('Ctrl Pts',(3.33607196359653,-1.94277019996061,3.43820567760661));
#6187=CARTESIAN_POINT('Ctrl Pts',(3.34005484693765,-1.93526110496934,3.36846749550572));
#6188=CARTESIAN_POINT('Ctrl Pts',(3.34403773027878,-1.92399697641733,3.29917379235574));
#6189=CARTESIAN_POINT('Ctrl Pts',(3.34802061361991,-1.90906168828384,3.23074177079247));
#6190=CARTESIAN_POINT('Ctrl Pts',(3.35201014553545,-1.89410146887164,3.16219551656176));
#6191=CARTESIAN_POINT('Ctrl Pts',(3.355999677451,-1.87545795844438,3.09451426921831));
#6192=CARTESIAN_POINT('Ctrl Pts',(3.35998920936655,-1.85326551711363,3.02810219231269));
#6193=CARTESIAN_POINT('Ctrl Pts',(3.36398253485343,-1.83105197340516,2.96162696540429));
#6194=CARTESIAN_POINT('Ctrl Pts',(3.36797586034032,-1.80528295013365,2.89642374333976));
#6195=CARTESIAN_POINT('Ctrl Pts',(3.37196918582721,-1.77614075125022,2.83287618626172));
#6196=CARTESIAN_POINT('Ctrl Pts',(3.37597065791847,-1.74693910067274,2.76919898866013));
#6197=CARTESIAN_POINT('Ctrl Pts',(3.37997213000974,-1.71435075203511,2.70718460986591));
#6198=CARTESIAN_POINT('Ctrl Pts',(3.38397360210101,-1.67860342342431,2.64719121550563));
#6199=CARTESIAN_POINT('Ctrl Pts',(3.38538917625688,-1.66595732884491,2.6259677515797));
#6200=CARTESIAN_POINT('Ctrl Pts',(3.38680475041276,-1.65291627738981,2.60499692950161));
#6201=CARTESIAN_POINT('Ctrl Pts',(3.38822032456863,-1.63949157496413,2.58429363787237));
#6202=CARTESIAN_POINT('Ctrl Pts',(3.39213901376762,-1.60232839550313,2.52698136994608));
#6203=CARTESIAN_POINT('Ctrl Pts',(3.3960577029666,-1.56208293473802,2.47150688257569));
#6204=CARTESIAN_POINT('Ctrl Pts',(3.39997639216559,-1.51896302007941,2.4182210290853));
#6205=CARTESIAN_POINT('Ctrl Pts',(3.40388919137145,-1.47590791688919,2.36501526699669));
#6206=CARTESIAN_POINT('Ctrl Pts',(3.4078019905773,-1.42998724131859,2.31399198913342));
#6207=CARTESIAN_POINT('Ctrl Pts',(3.41171478978316,-1.38145230970952,2.26547351685494));
#6208=CARTESIAN_POINT('Ctrl Pts',(3.41562299901092,-1.33297431285769,2.21701196002581));
#6209=CARTESIAN_POINT('Ctrl Pts',(3.41953120823868,-1.28188849665403,2.17104971919554));
#6210=CARTESIAN_POINT('Ctrl Pts',(3.42343941746644,-1.22848549620142,2.12787500950003));
#6211=CARTESIAN_POINT('Ctrl Pts',(3.42734518432627,-1.17511586903248,2.08472728109437));
#6212=CARTESIAN_POINT('Ctrl Pts',(3.43125095118611,-1.1194323117201,2.04436393660728));
#6213=CARTESIAN_POINT('Ctrl Pts',(3.43515671804595,-1.06176009971729,2.0070342972701));
#6214=CARTESIAN_POINT('Ctrl Pts',(3.4390613825441,-1.0041041650908,1.96971519383168));
#6215=CARTESIAN_POINT('Ctrl Pts',(3.44296604704225,-0.944461102619715,1.93542836280052));
#6216=CARTESIAN_POINT('Ctrl Pts',(3.4468707115404,-0.88318536029021,1.90437994758444));
#6217=CARTESIAN_POINT('Ctrl Pts',(3.45077561204667,-0.821905914294886,1.8733296557211));
#6218=CARTESIAN_POINT('Ctrl Pts',(3.45468051255293,-0.75899403229621,1.84551838823046));
#6219=CARTESIAN_POINT('Ctrl Pts',(3.45858541305919,-0.694827332237743,1.82110561424807));
#6220=CARTESIAN_POINT('Ctrl Pts',(3.46249446707374,-0.630592380268807,1.7966668732382));
#6221=CARTESIAN_POINT('Ctrl Pts',(3.46640352108827,-0.565100407054626,1.7756340149785));
#6222=CARTESIAN_POINT('Ctrl Pts',(3.47031257510282,-0.49874656330373,1.75811739342356));
#6223=CARTESIAN_POINT('Ctrl Pts',(3.47422397167028,-0.432352956124042,1.74059027479876));
#6224=CARTESIAN_POINT('Ctrl Pts',(3.47813536823775,-0.365096931932403,1.72658368679383));
#6225=CARTESIAN_POINT('Ctrl Pts',(3.48204676480522,-0.297383510812253,1.71615676994196));
#6226=CARTESIAN_POINT('Ctrl Pts',(3.48596489107774,-0.229553586201834,1.70571191318709));
#6227=CARTESIAN_POINT('Ctrl Pts',(3.48988301735025,-0.161265182991503,1.69885906877368));
#6228=CARTESIAN_POINT('Ctrl Pts',(3.49380114362277,-0.0929272280146145,
1.69560540942184));
#6229=CARTESIAN_POINT('Ctrl Pts',(3.49561671746175,-0.061260917478458,1.69409773499042));
#6230=CARTESIAN_POINT('Ctrl Pts',(3.49743229130073,-0.0295839467283565,
1.69336213986674));
#6231=CARTESIAN_POINT('Ctrl Pts',(3.49924786513971,0.00206331676382339,
1.69339555765881));
#6232=CARTESIAN_POINT('Ctrl Pts',(3.50316643928061,0.0703679737754331,1.69346768366824));
#6233=CARTESIAN_POINT('Ctrl Pts',(3.50708501342151,0.138803851921841,1.69712578460811));
#6234=CARTESIAN_POINT('Ctrl Pts',(3.51100358756241,0.206963501706501,1.70438594824043));
#6235=CARTESIAN_POINT('Ctrl Pts',(3.51491627231299,0.275020711479269,1.71163520026668));
#6236=CARTESIAN_POINT('Ctrl Pts',(3.51882895706357,0.342802031772585,1.72247571894332));
#6237=CARTESIAN_POINT('Ctrl Pts',(3.52274164181415,0.409900345716121,1.73687158001956));
#6238=CARTESIAN_POINT('Ctrl Pts',(3.52664973806483,0.476919971846337,1.75125055872182));
#6239=CARTESIAN_POINT('Ctrl Pts',(3.53055783431551,0.543257703856662,1.76917649652727));
#6240=CARTESIAN_POINT('Ctrl Pts',(3.53446593056618,0.608513703120316,1.7905619305695));
#6241=CARTESIAN_POINT('Ctrl Pts',(3.538371585438,0.673728937109304,1.8119340051796));
#6242=CARTESIAN_POINT('Ctrl Pts',(3.54227724030981,0.737863312606935,1.83676113616042));
#6243=CARTESIAN_POINT('Ctrl Pts',(3.54618289518163,0.800530830918063,1.86490564959534));
#6244=CARTESIAN_POINT('Ctrl Pts',(3.55008744885813,0.863180680187841,1.89304222771409));
#6245=CARTESIAN_POINT('Ctrl Pts',(3.55399200253463,0.92436404494093,1.92449413008874));
#6246=CARTESIAN_POINT('Ctrl Pts',(3.55789655621114,0.983715333682244,1.95907573585257));
#6247=CARTESIAN_POINT('Ctrl Pts',(3.5618013472406,1.04307023031451,1.99365944378916));
#6248=CARTESIAN_POINT('Ctrl Pts',(3.56570613827006,1.10059240624667,2.03137298304466));
#6249=CARTESIAN_POINT('Ctrl Pts',(3.56961092929951,1.1559428736939,2.07198592674415));
#6250=CARTESIAN_POINT('Ctrl Pts',(3.57351987663855,1.2113522568875,2.11264209938101));
#6251=CARTESIAN_POINT('Ctrl Pts',(3.57742882397759,1.26458492120601,2.15620354395477));
#6252=CARTESIAN_POINT('Ctrl Pts',(3.58133777131662,1.31533359401786,2.20239843491629));
#6253=CARTESIAN_POINT('Ctrl Pts',(3.58524906265562,1.36611269826724,2.24862102664042));
#6254=CARTESIAN_POINT('Ctrl Pts',(3.58916035399461,1.41440450085385,2.29747985777418));
#6255=CARTESIAN_POINT('Ctrl Pts',(3.5930716453336,1.4599393691669,2.34866699942962));
#6256=CARTESIAN_POINT('Ctrl Pts',(3.59698966972396,1.50555262300048,2.39994225665214));
#6257=CARTESIAN_POINT('Ctrl Pts',(3.60090769411433,1.54839916383622,2.45355343977741));
#6258=CARTESIAN_POINT('Ctrl Pts',(3.60482571850469,1.58825087105815,2.50916111321865));
#6259=CARTESIAN_POINT('Ctrl Pts',(3.60664228090672,1.60672781397207,2.53494319081015));
#6260=CARTESIAN_POINT('Ctrl Pts',(3.60845884330875,1.6245616033113,2.56115406024023));
#6261=CARTESIAN_POINT('Ctrl Pts',(3.61027540571078,1.64173285670969,2.58775810273207));
#6262=CARTESIAN_POINT('Ctrl Pts',(3.61419379700105,1.67877187594958,2.64514399174387));
#6263=CARTESIAN_POINT('Ctrl Pts',(3.61811218829132,1.71287172113914,2.70458778327021));
#6264=CARTESIAN_POINT('Ctrl Pts',(3.62203057958159,1.74379755342962,2.76575616792886));
#6265=CARTESIAN_POINT('Ctrl Pts',(3.62594307766091,1.77467687365945,2.82683255611058));
#6266=CARTESIAN_POINT('Ctrl Pts',(3.62985557574024,1.80239143499202,2.88962795431));
#6267=CARTESIAN_POINT('Ctrl Pts',(3.63376807381956,1.82675024602289,2.95378107549555));
#6268=CARTESIAN_POINT('Ctrl Pts',(3.63767597865819,1.8510804600091,3.01785888144223));
#6269=CARTESIAN_POINT('Ctrl Pts',(3.64158388349681,1.87206257414127,3.08329078713651));
#6270=CARTESIAN_POINT('Ctrl Pts',(3.64549178833543,1.88955282088803,3.14969361729596));
#6271=CARTESIAN_POINT('Ctrl Pts',(3.6493972489622,1.90703212830279,3.21605491558825));
#6272=CARTESIAN_POINT('Ctrl Pts',(3.65330270958897,1.92102377574857,3.2833854591959));
#6273=CARTESIAN_POINT('Ctrl Pts',(3.65720817021574,1.93143366978041,3.35128641496791));
#6274=CARTESIAN_POINT('Ctrl Pts',(3.66111252710871,1.94184062184128,3.41916818104976));
#6275=CARTESIAN_POINT('Ctrl Pts',(3.66501688400169,1.94866775551528,3.48761955338122));
#6276=CARTESIAN_POINT('Ctrl Pts',(3.66892124089467,1.9518723184559,3.55623278529371));
#6277=CARTESIAN_POINT('Ctrl Pts',(3.67282583289382,1.95507707436365,3.62485014884565));
#6278=CARTESIAN_POINT('Ctrl Pts',(3.67673042489298,1.95465880608775,3.69362889995242));
#6279=CARTESIAN_POINT('Ctrl Pts',(3.68063501689214,1.9506268316063,3.76215928788278));
#6280=CARTESIAN_POINT('Ctrl Pts',(3.68454376315515,1.94659056733328,3.83076258824888));
#6281=CARTESIAN_POINT('Ctrl Pts',(3.68845250941816,1.9389329528984,3.89911650621338));
#6282=CARTESIAN_POINT('Ctrl Pts',(3.69236125568117,1.92771529253682,3.9668154302129));
#6283=CARTESIAN_POINT('Ctrl Pts',(3.69627234448219,1.9164909093557,4.03455492663443));
#6284=CARTESIAN_POINT('Ctrl Pts',(3.70018343328321,1.9017023399558,4.10163816753919));
#6285=CARTESIAN_POINT('Ctrl Pts',(3.70409452208423,1.88346164729882,4.16767153212047));
#6286=CARTESIAN_POINT('Ctrl Pts',(3.70801234379548,1.86518955342533,4.23381857264685));
#6287=CARTESIAN_POINT('Ctrl Pts',(3.71193016550673,1.84345363127498,4.29891166351238));
#6288=CARTESIAN_POINT('Ctrl Pts',(3.71584798721798,1.81841494640197,4.36257492292585));
#6289=CARTESIAN_POINT('Ctrl Pts',(3.71766630690595,1.80679411803847,4.39212199436581));
#6290=CARTESIAN_POINT('Ctrl Pts',(3.71948462659391,1.79446252923629,4.42136139692663));
#6291=CARTESIAN_POINT('Ctrl Pts',(3.72130294628187,1.78143961641532,4.45025740370065));
#6292=CARTESIAN_POINT('Ctrl Pts',(3.72522147186894,1.75337490510792,4.51252903979293));
#6293=CARTESIAN_POINT('Ctrl Pts',(3.72913999745602,1.72198563863023,4.57345050024927));
#6294=CARTESIAN_POINT('Ctrl Pts',(3.73305852304309,1.6874241453808,4.63264355028591));
#6295=CARTESIAN_POINT('Ctrl Pts',(3.73697115741272,1.65291461281587,4.69174760788883));
#6296=CARTESIAN_POINT('Ctrl Pts',(3.74088379178235,1.61524256473294,4.74912799103301));
#6297=CARTESIAN_POINT('Ctrl Pts',(3.74479642615199,1.57460763543134,4.804428086828));
#6298=CARTESIAN_POINT('Ctrl Pts',(3.74870446955744,1.5340203858993,4.85966329520053));
#6299=CARTESIAN_POINT('Ctrl Pts',(3.75261251296288,1.49047744950318,4.91282266960529));
#6300=CARTESIAN_POINT('Ctrl Pts',(3.75652055636833,1.44422248756346,4.9635773607483));
#6301=CARTESIAN_POINT('Ctrl Pts',(3.76042615689386,1.39799643915049,5.01430032562759));
#6302=CARTESIAN_POINT('Ctrl Pts',(3.7643317574194,1.34906205859251,5.06262122638954));
#6303=CARTESIAN_POINT('Ctrl Pts',(3.76823735794493,1.29770313383148,5.10824441829378));
#6304=CARTESIAN_POINT('Ctrl Pts',(3.77214185585457,1.24635870854784,5.15385473001327));
#6305=CARTESIAN_POINT('Ctrl Pts',(3.77604635376421,1.19259146538888,5.196768518388));
#6306=CARTESIAN_POINT('Ctrl Pts',(3.77995085167385,1.13672056180759,5.23672840561858));
#6307=CARTESIAN_POINT('Ctrl Pts',(3.78385558559481,1.08084628105307,5.27669070826492));
#6308=CARTESIAN_POINT('Ctrl Pts',(3.78776031951578,1.0228684889009,5.31369847130271));
#6309=CARTESIAN_POINT('Ctrl Pts',(3.79166505343674,0.963136307333333,5.34753694863554));
#6310=CARTESIAN_POINT('Ctrl Pts',(3.79557394202005,0.90334057033524,5.3814114303288));
#6311=CARTESIAN_POINT('Ctrl Pts',(3.79948283060335,0.841787147330355,5.41210965379722));
#6312=CARTESIAN_POINT('Ctrl Pts',(3.80339171918666,0.778849921474264,5.43946277050327));
#6313=CARTESIAN_POINT('Ctrl Pts',(3.80730295074269,0.715874971288073,5.46683228256184));
#6314=CARTESIAN_POINT('Ctrl Pts',(3.81121418229871,0.651515028264088,5.49085252547173));
#6315=CARTESIAN_POINT('Ctrl Pts',(3.81512541385474,0.586161478091734,5.51140378199486));
#6316=CARTESIAN_POINT('Ctrl Pts',(3.81904337749726,0.520695440139974,5.53199041173343));
#6317=CARTESIAN_POINT('Ctrl Pts',(3.82296134113978,0.454232857736643,5.54909601583925));
#6318=CARTESIAN_POINT('Ctrl Pts',(3.8268793047823,0.38717683906159,5.56265165605116));
#6319=CARTESIAN_POINT('Ctrl Pts',(3.82869636547251,0.356077812451394,5.56893844766209));
#6320=CARTESIAN_POINT('Ctrl Pts',(3.83051342616273,0.324851235324714,5.57446241188905));
#6321=CARTESIAN_POINT('Ctrl Pts',(3.83233048685294,0.293537575865702,5.57922046757959));
#6322=CARTESIAN_POINT('Ctrl Pts',(3.83624898600517,0.226009535275453,5.58948123503227));
#6323=CARTESIAN_POINT('Ctrl Pts',(3.84016748515741,0.157809303592916,5.59621731169598));
#6324=CARTESIAN_POINT('Ctrl Pts',(3.84408598430965,0.089337189589276,5.59935114468739));
#6325=CARTESIAN_POINT('Ctrl Pts',(3.84799859215053,0.0209680207508368,5.60248026608256));
#6326=CARTESIAN_POINT('Ctrl Pts',(3.85191119999142,-0.0476717318334287,
5.60201787010987));
#6327=CARTESIAN_POINT('Ctrl Pts',(3.8558238078323,-0.116174217615536,5.59793786722721));
#6328=CARTESIAN_POINT('Ctrl Pts',(3.85973182470374,-0.184596324061974,5.5938626517317));
#6329=CARTESIAN_POINT('Ctrl Pts',(3.86363984157518,-0.252880995006901,5.5861782887664));
#6330=CARTESIAN_POINT('Ctrl Pts',(3.86754785844663,-0.320619775905069,5.57491073521875));
#6331=CARTESIAN_POINT('Ctrl Pts',(3.8714534324511,-0.388316213887179,5.56365022491971));
#6332=CARTESIAN_POINT('Ctrl Pts',(3.87535900645557,-0.455466954708045,5.54881104769211));
#6333=CARTESIAN_POINT('Ctrl Pts',(3.87926458046004,-0.521669626871883,5.53047088744464));
#6334=CARTESIAN_POINT('Ctrl Pts',(3.88316905190291,-0.587853609715083,5.51213590470926));
#6335=CARTESIAN_POINT('Ctrl Pts',(3.88707352334577,-0.653089581536215,5.49030203224688));
#6336=CARTESIAN_POINT('Ctrl Pts',(3.89097799478863,-0.716988088420454,5.46509743661043));
#6337=CARTESIAN_POINT('Ctrl Pts',(3.89488270233848,-0.780890459306206,5.43989131682888));
#6338=CARTESIAN_POINT('Ctrl Pts',(3.89878740988832,-0.843454748171191,5.41131425203775));
#6339=CARTESIAN_POINT('Ctrl Pts',(3.90269211743816,-0.904311019378601,5.3795427241299));
#6340=CARTESIAN_POINT('Ctrl Pts',(3.90660097997775,-0.965232047595143,5.34773738821702));
#6341=CARTESIAN_POINT('Ctrl Pts',(3.91050984251733,-1.02444099427484,5.31273103349862));
#6342=CARTESIAN_POINT('Ctrl Pts',(3.91441870505691,-1.08159301051947,5.27474586229668));
#6343=CARTESIAN_POINT('Ctrl Pts',(3.91832991071858,-1.13877928587395,5.2367379213267));
#6344=CARTESIAN_POINT('Ctrl Pts',(3.92224111638024,-1.19390578221183,5.19574790362305));
#6345=CARTESIAN_POINT('Ctrl Pts',(3.9261523220419,-1.24665939534115,5.15203939384194));
#6346=CARTESIAN_POINT('Ctrl Pts',(3.93007026029319,-1.29950381638485,5.10825564601781));
#6347=CARTESIAN_POINT('Ctrl Pts',(3.93398819854449,-1.34996684078181,5.06174439981745));
#6348=CARTESIAN_POINT('Ctrl Pts',(3.93790613679579,-1.39777163204783,5.01280666415819));
#6349=CARTESIAN_POINT('Ctrl Pts',(3.93972343367186,-1.41994541127995,4.99010737988375));
#6350=CARTESIAN_POINT('Ctrl Pts',(3.94154073054794,-1.44154784196988,4.9668865155006));
#6351=CARTESIAN_POINT('Ctrl Pts',(3.94335802742402,-1.46255434627852,4.94317638827728));
#6352=CARTESIAN_POINT('Ctrl Pts',(3.94723899460202,-1.50741523544837,4.89254171941756));
#6353=CARTESIAN_POINT('Ctrl Pts',(3.95111996178003,-1.54974101147079,4.83946434287412));
#6354=CARTESIAN_POINT('Ctrl Pts',(3.95500092895803,-1.58925110793402,4.78423083114816));
#6355=CARTESIAN_POINT('Ctrl Pts',(3.95887649205015,-1.62870618822607,4.72907422979721));
#6356=CARTESIAN_POINT('Ctrl Pts',(3.96275205514227,-1.66535307107133,4.67176784819088));
#6357=CARTESIAN_POINT('Ctrl Pts',(3.96662761823439,-1.69894984269427,4.61263300461006));
#6358=CARTESIAN_POINT('Ctrl Pts',(3.97049917545996,-1.73251188796124,4.55355928409343));
#6359=CARTESIAN_POINT('Ctrl Pts',(3.97437073268553,-1.76302982718918,4.49266128331292));
#6360=CARTESIAN_POINT('Ctrl Pts',(3.97824228991111,-1.79030481181491,4.43028953200083));
#6361=CARTESIAN_POINT('Ctrl Pts',(3.98211211898432,-1.81756762166798,4.36794562165374));
#6362=CARTESIAN_POINT('Ctrl Pts',(3.98598194805753,-1.84159013640098,4.30412971952778));
#6363=CARTESIAN_POINT('Ctrl Pts',(3.98985177713074,-1.86222007239048,4.23921572676147));
#6364=CARTESIAN_POINT('Ctrl Pts',(3.99372037176401,-1.88284342761977,4.17432244096296));
#6365=CARTESIAN_POINT('Ctrl Pts',(3.99758896639727,-1.90007620415422,4.10833223942717));
#6366=CARTESIAN_POINT('Ctrl Pts',(4.00145756103053,-1.91381554134512,4.04163560478018));
#6367=CARTESIAN_POINT('Ctrl Pts',(4.00532869478215,-1.92756389623018,3.97489519437857));
#6368=CARTESIAN_POINT('Ctrl Pts',(4.00919982853377,-1.93781412805715,3.90744791692283));
#6369=CARTESIAN_POINT('Ctrl Pts',(4.01307096228539,-1.94451449325918,3.83969471660667));
#6370=CARTESIAN_POINT('Ctrl Pts',(4.01675741081552,-1.95089519540876,3.77517390649201));
#6371=CARTESIAN_POINT('Ctrl Pts',(4.02044385934564,-1.95405702262766,3.71037610742807));
#6372=CARTESIAN_POINT('Ctrl Pts',(4.02413030787577,-1.95399922086809,3.64564951931539));
#6373=CARTESIAN_POINT('Origin',(0.,0.,3.64739446828387));
#6374=CARTESIAN_POINT('',(4.82586969212423,-1.95430222507481,3.64764326884653));
#6375=CARTESIAN_POINT('',(4.72413035081973,-1.95427619993066,3.64777710414201));
#6376=CARTESIAN_POINT('',(0.,-1.954,3.64739446828387));
#6377=CARTESIAN_POINT('Ctrl Pts',(4.82586969212423,-1.95715633972901,3.64764363220145));
#6378=CARTESIAN_POINT('Ctrl Pts',(4.8250995783704,-1.95718052860821,3.66109012482263));
#6379=CARTESIAN_POINT('Ctrl Pts',(4.78732028442627,-1.95096916696084,4.32070869776121));
#6380=CARTESIAN_POINT('Ctrl Pts',(4.71253181029161,-1.21359828804363,5.61146159126675));
#6381=CARTESIAN_POINT('Ctrl Pts',(4.60150426972061,0.989869636257431,5.73318883630089));
#6382=CARTESIAN_POINT('Ctrl Pts',(4.49047672914949,2.28894570144034,3.94923537617159));
#6383=CARTESIAN_POINT('Ctrl Pts',(4.37944918857844,1.49673214248603,1.88950560619213));
#6384=CARTESIAN_POINT('Ctrl Pts',(4.26842164800734,-0.662966995866537,1.43586675992707));
#6385=CARTESIAN_POINT('Ctrl Pts',(4.18389531480082,-1.8460276791096,2.62877633203429));
#6386=CARTESIAN_POINT('Ctrl Pts',(4.13637816178465,-1.95459509422112,3.46119040754887));
#6387=CARTESIAN_POINT('Ctrl Pts',(4.12587018895884,-1.95303263999471,3.6456699100979));
#6388=CARTESIAN_POINT('Ctrl Pts',(4.02413030792419,-1.95399922086733,3.64564951846532));
#6389=CARTESIAN_POINT('Ctrl Pts',(4.02917285126934,-1.95392015614755,3.55711264524746));
#6390=CARTESIAN_POINT('Ctrl Pts',(4.03421539461449,-1.94781926961924,3.46884243996873));
#6391=CARTESIAN_POINT('Ctrl Pts',(4.03925793795964,-1.93583046129939,3.38154408723206));
#6392=CARTESIAN_POINT('Ctrl Pts',(4.0443004813048,-1.92384165297954,3.29424573449538));
#6393=CARTESIAN_POINT('Ctrl Pts',(4.04934302464995,-1.90596512136721,3.20791897386854));
#6394=CARTESIAN_POINT('Ctrl Pts',(4.05438556799511,-1.88238740014386,3.12324403588909));
#6395=CARTESIAN_POINT('Ctrl Pts',(4.0583040649868,-1.86406544961994,3.05744420690733));
#6396=CARTESIAN_POINT('Ctrl Pts',(4.06222256197849,-1.84225301252198,2.99247609015028));
#6397=CARTESIAN_POINT('Ctrl Pts',(4.06614105897018,-1.81704344396077,2.92873660618314));
#6398=CARTESIAN_POINT('Ctrl Pts',(4.07005366446439,-1.79187177822557,2.86509295513616));
#6399=CARTESIAN_POINT('Ctrl Pts',(4.0739662699586,-1.76331329734956,2.80267472432131));
#6400=CARTESIAN_POINT('Ctrl Pts',(4.07787887545281,-1.73151138885174,2.74186461771199));
#6401=CARTESIAN_POINT('Ctrl Pts',(4.08178688971242,-1.69974679820328,2.68112586853074));
#6402=CARTESIAN_POINT('Ctrl Pts',(4.08569490397203,-1.66474656556231,2.62199192953893));
#6403=CARTESIAN_POINT('Ctrl Pts',(4.08960291823164,-1.62670179878594,2.56482472095736));
#6404=CARTESIAN_POINT('Ctrl Pts',(4.09350848946089,-1.5886808150652,2.50769324950909));
#6405=CARTESIAN_POINT('Ctrl Pts',(4.09741406069013,-1.54761934451823,2.45252647804732));
#6406=CARTESIAN_POINT('Ctrl Pts',(4.10131963191938,-1.503753182883,2.39965957457879));
#6407=CARTESIAN_POINT('Ctrl Pts',(4.10522410042749,-1.45989940666873,2.34680759785172));
#6408=CARTESIAN_POINT('Ctrl Pts',(4.10912856893559,-1.41324282530704,2.2962545782837));
#6409=CARTESIAN_POINT('Ctrl Pts',(4.1130330374437,-1.36405998580495,2.24830320781306));
#6410=CARTESIAN_POINT('Ctrl Pts',(4.11693774190294,-1.31487417413215,2.20034893959068));
#6411=CARTESIAN_POINT('Ctrl Pts',(4.12084244636218,-1.2631621551327,2.15499697405001));
#6412=CARTESIAN_POINT('Ctrl Pts',(4.12474715082143,-1.20923654449766,2.11251239481654));
#6413=CARTESIAN_POINT('Ctrl Pts',(4.12865601005464,-1.15525355468686,2.06998261015824));
#6414=CARTESIAN_POINT('Ctrl Pts',(4.13256486928786,-1.09905265975336,2.03032660554053));
#6415=CARTESIAN_POINT('Ctrl Pts',(4.13647372852107,-1.04097789456905,1.99376784083178));
#6416=CARTESIAN_POINT('Ctrl Pts',(4.14038493074819,-0.982868319018695,1.957187162578));
#6417=CARTESIAN_POINT('Ctrl Pts',(4.1442961329753,-0.922883067278713,1.92370765872149));
#6418=CARTESIAN_POINT('Ctrl Pts',(4.14820733520242,-0.861390907329552,1.89350687075375));
#6419=CARTESIAN_POINT('Ctrl Pts',(4.15212526985654,-0.799792899752562,1.86325409759363));
#6420=CARTESIAN_POINT('Ctrl Pts',(4.15604320451065,-0.736683259058302,1.8362914971923));
#6421=CARTESIAN_POINT('Ctrl Pts',(4.15996113916476,-0.672450022015205,1.81274818959913));
#6422=CARTESIAN_POINT('Ctrl Pts',(4.16177846229857,-0.642655612985202,1.801827691604));
#6423=CARTESIAN_POINT('Ctrl Pts',(4.16359578543237,-0.612619657991507,1.79164216046196));
#6424=CARTESIAN_POINT('Ctrl Pts',(4.16541310856617,-0.58238171102534,1.78220076717313));
#6425=CARTESIAN_POINT('Ctrl Pts',(4.16933160051186,-0.51718298580306,1.7618433398834));
#6426=CARTESIAN_POINT('Ctrl Pts',(4.17325009245754,-0.450786632722358,1.74486834658914));
#6427=CARTESIAN_POINT('Ctrl Pts',(4.17716858440322,-0.383576620845942,1.73141300283583));
#6428=CARTESIAN_POINT('Ctrl Pts',(4.1810811848136,-0.31646766064036,1.71797788947573));
#6429=CARTESIAN_POINT('Ctrl Pts',(4.18499378522397,-0.248547947918793,1.7080520188436));
#6430=CARTESIAN_POINT('Ctrl Pts',(4.18890638563434,-0.18021669174885,1.70172287625836));
#6431=CARTESIAN_POINT('Ctrl Pts',(4.19281439477959,-0.111965619313588,1.69540116064458));
#6432=CARTESIAN_POINT('Ctrl Pts',(4.19672240392484,-0.0433044499019896,
1.69266783597897));
#6433=CARTESIAN_POINT('Ctrl Pts',(4.20063041307009,0.0253591372019198,1.69355903146726));
#6434=CARTESIAN_POINT('Ctrl Pts',(4.20453597916911,0.0939798000670118,1.6944496698351));
#6435=CARTESIAN_POINT('Ctrl Pts',(4.20844154526813,0.162602386999144,1.69896032725903));
#6436=CARTESIAN_POINT('Ctrl Pts',(4.21234711136715,0.230817406905028,1.707075081));
#6437=CARTESIAN_POINT('Ctrl Pts',(4.21625157473709,0.299013166431403,1.71518754355589));
#6438=CARTESIAN_POINT('Ctrl Pts',(4.22015603810705,0.36680109928512,1.72690202420201));
#6439=CARTESIAN_POINT('Ctrl Pts',(4.224060501477,0.433776846712702,1.7421507444375));
#6440=CARTESIAN_POINT('Ctrl Pts',(4.22796520079809,0.500756641560616,1.75740038617044));
#6441=CARTESIAN_POINT('Ctrl Pts',(4.23186990011919,0.566923674618865,1.77618457983965));
#6442=CARTESIAN_POINT('Ctrl Pts',(4.23577459944029,0.631885572091681,1.79838483505251));
#6443=CARTESIAN_POINT('Ctrl Pts',(4.2396834535708,0.696916592506178,1.82060871252713));
#6444=CARTESIAN_POINT('Ctrl Pts',(4.24359230770132,0.760739452005175,1.8462557462092));
#6445=CARTESIAN_POINT('Ctrl Pts',(4.24750116183184,0.822979658705006,1.87515845652985));
#6446=CARTESIAN_POINT('Ctrl Pts',(4.25141235896911,0.885257172815203,1.90407849142784));
#6447=CARTESIAN_POINT('Ctrl Pts',(4.25532355610639,0.945949711592333,1.93625785640229));
#6448=CARTESIAN_POINT('Ctrl Pts',(4.25923475324367,1.00470790265021,1.9714833637344));
#6449=CARTESIAN_POINT('Ctrl Pts',(4.26315268288125,1.06356723653613,2.00676950614337));
#6450=CARTESIAN_POINT('Ctrl Pts',(4.26707061251884,1.12048516969906,2.04511198123528));
#6451=CARTESIAN_POINT('Ctrl Pts',(4.27098854215643,1.17514251896321,2.08625512148462));
#6452=CARTESIAN_POINT('Ctrl Pts',(4.27280591115004,1.20049585121115,2.10533975911356));
#6453=CARTESIAN_POINT('Ctrl Pts',(4.27462328014365,1.22536326940056,2.12502645043353));
#6454=CARTESIAN_POINT('Ctrl Pts',(4.27644064913727,1.24971558638332,2.14528696442451));
#6455=CARTESIAN_POINT('Ctrl Pts',(4.2803591387095,1.30222242483608,2.18897133071489));
#6456=CARTESIAN_POINT('Ctrl Pts',(4.28427762828174,1.35253983626061,2.23549850288804));
#6457=CARTESIAN_POINT('Ctrl Pts',(4.28819611785398,1.40034404905103,2.28462062633967));
#6458=CARTESIAN_POINT('Ctrl Pts',(4.29210871583145,1.44807638643019,2.33366889285235));
#6459=CARTESIAN_POINT('Ctrl Pts',(4.29602131380893,1.49330268437295,2.3853040176659));
#6460=CARTESIAN_POINT('Ctrl Pts',(4.29993391178641,1.53573264762285,2.43923833804849));
#6461=CARTESIAN_POINT('Ctrl Pts',(4.30384191842259,1.57811282031326,2.49310936778028));
#6462=CARTESIAN_POINT('Ctrl Pts',(4.30774992505877,1.61770287270592,2.54927384999249));
#6463=CARTESIAN_POINT('Ctrl Pts',(4.31165793169496,1.65425102822597,2.60740911472676));
#6464=CARTESIAN_POINT('Ctrl Pts',(4.31556349523904,1.69077633565022,2.66550803617422));
#6465=CARTESIAN_POINT('Ctrl Pts',(4.31946905878312,1.72426325734888,2.72557488075033));
#6466=CARTESIAN_POINT('Ctrl Pts',(4.3233746223272,1.75450273635886,2.78725718382907));
#6467=CARTESIAN_POINT('Ctrl Pts',(4.3272790831002,1.78473367697923,2.84892207035328));
#6468=CARTESIAN_POINT('Ctrl Pts',(4.33118354387319,1.81171877886262,2.91220106849717));
#6469=CARTESIAN_POINT('Ctrl Pts',(4.33508800464619,1.83529531184884,2.97671785596937));
#6470=CARTESIAN_POINT('Ctrl Pts',(4.33899270133211,1.85887326936183,3.04123854163518));
#6471=CARTESIAN_POINT('Ctrl Pts',(4.34289739801803,1.87904208272451,3.10699670233859));
#6472=CARTESIAN_POINT('Ctrl Pts',(4.34680209470395,1.89568811035569,3.17359853303739));
#6473=CARTESIAN_POINT('Ctrl Pts',(4.35071094615929,1.91235185009415,3.24027123102042));
#6474=CARTESIAN_POINT('Ctrl Pts',(4.35461979761464,1.92548520407722,3.30778891251322));
#6475=CARTESIAN_POINT('Ctrl Pts',(4.35852864906998,1.93502537597306,3.37574617666339));
#6476=CARTESIAN_POINT('Ctrl Pts',(4.36243984350534,1.94457126628318,3.4437441746488));
#6477=CARTESIAN_POINT('Ctrl Pts',(4.36635103794069,1.950519645517,3.51218178970461));
#6478=CARTESIAN_POINT('Ctrl Pts',(4.37026223237604,1.95285973907249,3.580649884161));
#6479=CARTESIAN_POINT('Ctrl Pts',(4.37418015929856,1.95520386071968,3.6492358353426));
#6480=CARTESIAN_POINT('Ctrl Pts',(4.37809808622109,1.95392730970642,3.71785187923872));
#6481=CARTESIAN_POINT('Ctrl Pts',(4.38201601314362,1.94907137633538,3.78609115155389));
#6482=CARTESIAN_POINT('Ctrl Pts',(4.38383340533186,1.94681887506375,3.81774501414223));
#6483=CARTESIAN_POINT('Ctrl Pts',(4.3856507975201,1.9437969214201,3.84931791374553));
#6484=CARTESIAN_POINT('Ctrl Pts',(4.38746818970834,1.94001336524288,3.88077000830249));
#6485=CARTESIAN_POINT('Ctrl Pts',(4.39138668198172,1.93185561275431,3.94858409394712));
#6486=CARTESIAN_POINT('Ctrl Pts',(4.39530517425511,1.92012173726112,4.0161040377949));
#6487=CARTESIAN_POINT('Ctrl Pts',(4.39922366652849,1.90484397768049,4.08292336594093));
#6488=CARTESIAN_POINT('Ctrl Pts',(4.40313626725048,1.8895891885945,4.14964222955149));
#6489=CARTESIAN_POINT('Ctrl Pts',(4.40704886797247,1.87080119907181,4.21566209253637));
#6490=CARTESIAN_POINT('Ctrl Pts',(4.41096146869446,1.84856385522711,4.28058296561141));
#6491=CARTESIAN_POINT('Ctrl Pts',(4.41486947812581,1.82635260607386,4.34542765646954));
#6492=CARTESIAN_POINT('Ctrl Pts',(4.41877748755716,1.80070020003049,4.4091754556096));
#6493=CARTESIAN_POINT('Ctrl Pts',(4.42268549698851,1.77174079835075,4.47143969972415));
#6494=CARTESIAN_POINT('Ctrl Pts',(4.42659106335757,1.74279950042006,4.53366501982144));
#6495=CARTESIAN_POINT('Ctrl Pts',(4.43049662972664,1.71055551477644,4.59440817974511));
#6496=CARTESIAN_POINT('Ctrl Pts',(4.4344021960957,1.67519122308988,4.65330220067418));
#6497=CARTESIAN_POINT('Ctrl Pts',(4.43830665971918,1.63983691659182,4.71217959274199));
#6498=CARTESIAN_POINT('Ctrl Pts',(4.44221112334267,1.6013643061073,4.7692084609066));
#6499=CARTESIAN_POINT('Ctrl Pts',(4.44611558696615,1.56000096824241,4.82404776432428));
#6500=CARTESIAN_POINT('Ctrl Pts',(4.45002028652378,1.51863513092433,4.8788903815043));
#6501=CARTESIAN_POINT('Ctrl Pts',(4.45392498608142,1.4743785176148,4.93154278020563));
#6502=CARTESIAN_POINT('Ctrl Pts',(4.45782968563905,1.42750004749021,4.98169563909031));
#6503=CARTESIAN_POINT('Ctrl Pts',(4.46173853997862,1.38057169649312,5.03190186294942));
#6504=CARTESIAN_POINT('Ctrl Pts',(4.46564739431819,1.33101625765964,5.07960287931854));
#6505=CARTESIAN_POINT('Ctrl Pts',(4.46955624865776,1.27914000413551,5.12452575893484));
#6506=CARTESIAN_POINT('Ctrl Pts',(4.47346744598867,1.22723265566573,5.16947556560168));
#6507=CARTESIAN_POINT('Ctrl Pts',(4.47737864331959,1.17300211219345,5.21164361948917));
#6508=CARTESIAN_POINT('Ctrl Pts',(4.48128984065051,1.11678604131846,5.25079864001233));
#6509=CARTESIAN_POINT('Ctrl Pts',(4.48520777045583,1.06047320384596,5.29002105937809));
#6510=CARTESIAN_POINT('Ctrl Pts',(4.48912570026114,1.00216843533822,5.32621983500999));
#6511=CARTESIAN_POINT('Ctrl Pts',(4.49304363006646,0.942235775033994,5.35920863584006));
#6512=CARTESIAN_POINT('Ctrl Pts',(4.49486099680411,0.914435475194978,5.37451078578218));
#6513=CARTESIAN_POINT('Ctrl Pts',(4.49667836354177,0.886285215289973,5.38912293121047));
#6514=CARTESIAN_POINT('Ctrl Pts',(4.49849573027942,0.857822709676756,5.40303002236758));
#6515=CARTESIAN_POINT('Ctrl Pts',(4.50241422181614,0.796453650230121,5.43301561518745));
#6516=CARTESIAN_POINT('Ctrl Pts',(4.50633271335287,0.73338909294653,5.45983885890346));
#6517=CARTESIAN_POINT('Ctrl Pts',(4.5102512048896,0.668987832150729,5.48330603489983));
#6518=CARTESIAN_POINT('Ctrl Pts',(4.51416380486715,0.604683400411566,5.50673792735539));
#6519=CARTESIAN_POINT('Ctrl Pts',(4.5180764048447,0.539046712223277,5.52682359956585));
#6520=CARTESIAN_POINT('Ctrl Pts',(4.52198900482225,0.472459149121607,5.54341618556753));
#6521=CARTESIAN_POINT('Ctrl Pts',(4.52589701350137,0.405949724182698,5.55998930075327));
#6522=CARTESIAN_POINT('Ctrl Pts',(4.52980502218049,0.338492115304126,5.57307735214722));
#6523=CARTESIAN_POINT('Ctrl Pts',(4.53371303085961,0.270483845284602,5.58258295766677));
#6524=CARTESIAN_POINT('Ctrl Pts',(4.53761859647206,0.202518090200798,5.59208262081772));
#6525=CARTESIAN_POINT('Ctrl Pts',(4.54152416208451,0.134002842795795,5.59800421276478));
#6526=CARTESIAN_POINT('Ctrl Pts',(4.54542972769696,0.0653452906021997,5.60030153033166));
#6527=CARTESIAN_POINT('Ctrl Pts',(4.54933419056062,-0.00329287591447554,
5.60259819924366));
#6528=CARTESIAN_POINT('Ctrl Pts',(4.55323865342427,-0.0720727761918079,
5.60127260884809));
#6529=CARTESIAN_POINT('Ctrl Pts',(4.55714311628792,-0.140584451882745,5.59633059137483));
#6530=CARTESIAN_POINT('Ctrl Pts',(4.56104781508368,-0.209100267478244,5.59138827527393));
#6531=CARTESIAN_POINT('Ctrl Pts',(4.56495251387943,-0.277347336006443,5.5828291361928));
#6532=CARTESIAN_POINT('Ctrl Pts',(4.56885721267518,-0.344919875101811,5.57071094763919));
#6533=CARTESIAN_POINT('Ctrl Pts',(4.57276606625502,-0.4125643145727,5.55857986476018));
#6534=CARTESIAN_POINT('Ctrl Pts',(4.57667491983485,-0.479532307292798,5.54288226179697));
#6535=CARTESIAN_POINT('Ctrl Pts',(4.58058377341469,-0.5454283365702,5.52372704266035));
#6536=CARTESIAN_POINT('Ctrl Pts',(4.584494969986,-0.611363864342917,5.50456034176464));
#6537=CARTESIAN_POINT('Ctrl Pts',(4.58840616655731,-0.676225685518619,5.48193206200187));
#6538=CARTESIAN_POINT('Ctrl Pts',(4.59231736312862,-0.739636199691905,5.45600008922651));
#6539=CARTESIAN_POINT('Ctrl Pts',(4.59623529218249,-0.803155864651535,5.43002347881879));
#6540=CARTESIAN_POINT('Ctrl Pts',(4.60015322123637,-0.865218792240787,5.40073203547598));
#6541=CARTESIAN_POINT('Ctrl Pts',(4.60407115029025,-0.925470798061731,5.3683302026839));
#6542=CARTESIAN_POINT('Ctrl Pts',(4.60588852381033,-0.953419338835413,5.3533002641351));
#6543=CARTESIAN_POINT('Ctrl Pts',(4.60770589733041,-0.980978626059195,5.33760169347744));
#6544=CARTESIAN_POINT('Ctrl Pts',(4.60952327085049,-1.00811553775735,5.32125798199465));
#6545=CARTESIAN_POINT('Ctrl Pts',(4.6134417617717,-1.06662620765759,5.28601883915662));
#6546=CARTESIAN_POINT('Ctrl Pts',(4.6173602526929,-1.12340266514513,5.24763841256609));
#6547=CARTESIAN_POINT('Ctrl Pts',(4.62127874361411,-1.17808737194236,5.20631272915258));
#6548=CARTESIAN_POINT('Ctrl Pts',(4.625191342969,-1.23268985867503,5.16504918011919));
#6549=CARTESIAN_POINT('Ctrl Pts',(4.62910394232389,-1.2852064473077,5.12084945702431));
#6550=CARTESIAN_POINT('Ctrl Pts',(4.63301654167879,-1.33530666907631,5.07395400069755));
#6551=CARTESIAN_POINT('Ctrl Pts',(4.63692454972767,-1.3853480998908,5.0271135746386));
#6552=CARTESIAN_POINT('Ctrl Pts',(4.64083255777656,-1.43297843794731,4.97758403233602));
#6553=CARTESIAN_POINT('Ctrl Pts',(4.64474056582544,-1.47789999451356,4.92564624560195));
#6554=CARTESIAN_POINT('Ctrl Pts',(4.64864613080331,-1.52279346860109,4.87374092750659));
#6555=CARTESIAN_POINT('Ctrl Pts',(4.65255169578118,-1.5649811993835,4.81943072256506));
#6556=CARTESIAN_POINT('Ctrl Pts',(4.65645726075905,-1.60420321923422,4.76303241645459));
#6557=CARTESIAN_POINT('Ctrl Pts',(4.66036172298472,-1.64341416458768,4.70665003463585));
#6558=CARTESIAN_POINT('Ctrl Pts',(4.66426618521039,-1.67966078073795,4.64818112563719));
#6559=CARTESIAN_POINT('Ctrl Pts',(4.66817064743606,-1.71272528491323,4.58797306596664));
#6560=CARTESIAN_POINT('Ctrl Pts',(4.67207534559136,-1.74579178703235,4.52776136818554));
#6561=CARTESIAN_POINT('Ctrl Pts',(4.67598004374666,-1.77567556097404,4.46581074337476));
#6562=CARTESIAN_POINT('Ctrl Pts',(4.67988474190196,-1.80220470312604,4.4024932750836));
#6563=CARTESIAN_POINT('Ctrl Pts',(4.68379359484192,-1.8287620735478,4.33910843399292));
#6564=CARTESIAN_POINT('Ctrl Pts',(4.68770244778188,-1.851957498273,4.27435430137858));
#6565=CARTESIAN_POINT('Ctrl Pts',(4.69161130072184,-1.87166757980071,4.20862211436249));
#6566=CARTESIAN_POINT('Ctrl Pts',(4.69552249665267,-1.89138947567441,4.14285052706291));
#6567=CARTESIAN_POINT('Ctrl Pts',(4.6994336925835,-1.90762175436053,4.07610019650578));
#6568=CARTESIAN_POINT('Ctrl Pts',(4.70334488851433,-1.92029187621531,4.00877392279321));
#6569=CARTESIAN_POINT('Ctrl Pts',(4.70726281693344,-1.93298380762613,3.94133175784014));
#6570=CARTESIAN_POINT('Ctrl Pts',(4.71118074535254,-1.94210127926278,3.8733121582267));
#6571=CARTESIAN_POINT('Ctrl Pts',(4.71509867377164,-1.94762356115874,3.805123552537));
#6572=CARTESIAN_POINT('Ctrl Pts',(4.71691605298829,-1.95018513944007,3.77349343030501));
#6573=CARTESIAN_POINT('Ctrl Pts',(4.71873343220494,-1.95197388355601,3.74182694727269));
#6574=CARTESIAN_POINT('Ctrl Pts',(4.72055081142158,-1.95299152617943,3.71016467356758));
#6575=CARTESIAN_POINT('Ctrl Pts',(4.72174397690631,-1.95365963993518,3.68937741474617));
#6576=CARTESIAN_POINT('Ctrl Pts',(4.72293714239104,-1.95399588157958,3.66857943228897));
#6577=CARTESIAN_POINT('Ctrl Pts',(4.72413030787577,-1.95399996239942,3.64777779982395));
#6578=CARTESIAN_POINT('Origin',(0.,0.,3.64739446828387));
#6579=CARTESIAN_POINT('',(5.5258696920781,-1.95399938884984,3.64893990493634));
#6580=CARTESIAN_POINT('',(5.42413030787577,-1.95399943981962,3.64887405762318));
#6581=CARTESIAN_POINT('',(0.,-1.954,3.64739446828387));
#6582=CARTESIAN_POINT('Ctrl Pts',(5.5258696920781,-1.95399938884984,3.64893990493634));
#6583=CARTESIAN_POINT('Ctrl Pts',(5.5212902068915,-1.9539356881594,3.72948096754407));
#6584=CARTESIAN_POINT('Ctrl Pts',(5.5167107217049,-1.9488883727995,3.80981306186029));
#6585=CARTESIAN_POINT('Ctrl Pts',(5.5121312365183,-1.93895808420072,3.88938113674448));
#6586=CARTESIAN_POINT('Ctrl Pts',(5.50750036886044,-1.92891637635988,3.96984197667854));
#6587=CARTESIAN_POINT('Ctrl Pts',(5.50286950120259,-1.91388160449041,4.04952144814043));
#6588=CARTESIAN_POINT('Ctrl Pts',(5.49823863354473,-1.89400709304308,4.12786624841512));
#6589=CARTESIAN_POINT('Ctrl Pts',(5.49540062045956,-1.8818270594692,4.17587961972306));
#6590=CARTESIAN_POINT('Ctrl Pts',(5.49256260737439,-1.86783026256677,4.22339212396149));
#6591=CARTESIAN_POINT('Ctrl Pts',(5.48972459428922,-1.85206076918552,4.27028041871455));
#6592=CARTESIAN_POINT('Ctrl Pts',(5.48580620372998,-1.83028813032352,4.33501819334261));
#6593=CARTESIAN_POINT('Ctrl Pts',(5.48188781317074,-1.80507401469032,4.3987411113528));
#6594=CARTESIAN_POINT('Ctrl Pts',(5.4779694226115,-1.77653259424169,4.46105775343129));
#6595=CARTESIAN_POINT('Ctrl Pts',(5.4740569252752,-1.74803409982388,4.52328067185987));
#6596=CARTESIAN_POINT('Ctrl Pts',(5.4701444279389,-1.71621843543999,4.58410106841765));
#6597=CARTESIAN_POINT('Ctrl Pts',(5.46623193060261,-1.681248985294,4.64314436130314));
#6598=CARTESIAN_POINT('Ctrl Pts',(5.46232402652118,-1.64632058913045,4.70211833761949));
#6599=CARTESIAN_POINT('Ctrl Pts',(5.45841612243974,-1.6082460099648,4.75931893258282));
#6600=CARTESIAN_POINT('Ctrl Pts',(5.45450821835831,-1.56723518853569,4.81439483838471));
#6601=CARTESIAN_POINT('Ctrl Pts',(5.45060275849708,-1.5262500175515,4.86943629665693));
#6602=CARTESIAN_POINT('Ctrl Pts',(5.44669729863585,-1.48233254040954,4.92235530833337));
#6603=CARTESIAN_POINT('Ctrl Pts',(5.44279183877463,-1.43573591095844,4.97282963983483));
#6604=CARTESIAN_POINT('Ctrl Pts',(5.43888748265438,-1.38915245040719,5.02328970654023));
#6605=CARTESIAN_POINT('Ctrl Pts',(5.43498312653414,-1.33989167411582,5.07130610346443));
#6606=CARTESIAN_POINT('Ctrl Pts',(5.4310787704139,-1.28824571546202,5.11659117961757));
#6607=CARTESIAN_POINT('Ctrl Pts',(5.42717417919354,-1.23659664695582,5.16187898260368));
#6608=CARTESIAN_POINT('Ctrl Pts',(5.42326958797317,-1.182562482418,5.20443481600184));
#6609=CARTESIAN_POINT('Ctrl Pts',(5.41936499675281,-1.12646938739021,5.24401048952151));
#6610=CARTESIAN_POINT('Ctrl Pts',(5.41545625127246,-1.07031661254271,5.28362826927653));
#6611=CARTESIAN_POINT('Ctrl Pts',(5.41154750579211,-1.0121009381428,5.32025927739807));
#6612=CARTESIAN_POINT('Ctrl Pts',(5.40763876031176,-0.952177706508478,5.35369854881238));
#6613=CARTESIAN_POINT('Ctrl Pts',(5.40372767229675,-0.892218562521245,5.38715786058306));
#6614=CARTESIAN_POINT('Ctrl Pts',(5.39981658428174,-0.830550266193544,5.41742141207729));
#6615=CARTESIAN_POINT('Ctrl Pts',(5.39590549626673,-0.767550432645577,5.44433139910409));
#6616=CARTESIAN_POINT('Ctrl Pts',(5.39198767533847,-0.704442145283215,5.4712877115031));
#6617=CARTESIAN_POINT('Ctrl Pts',(5.38806985441022,-0.639998207400958,5.49487876839444));
#6618=CARTESIAN_POINT('Ctrl Pts',(5.38415203348196,-0.574612917818897,5.51499613745095));
#6619=CARTESIAN_POINT('Ctrl Pts',(5.38233370689402,-0.544266505186804,5.52433294679083));
#6620=CARTESIAN_POINT('Ctrl Pts',(5.38051538030607,-0.513717484252054,5.53292222715614));
#6621=CARTESIAN_POINT('Ctrl Pts',(5.37869705371813,-0.483005906313095,5.54075689911075));
#6622=CARTESIAN_POINT('Ctrl Pts',(5.3747785277876,-0.41682191311884,5.55764075562746));
#6623=CARTESIAN_POINT('Ctrl Pts',(5.37086000185706,-0.349620703532015,5.57108354879798));
#6624=CARTESIAN_POINT('Ctrl Pts',(5.36694147592653,-0.28179296869672,5.58096854826971));
#6625=CARTESIAN_POINT('Ctrl Pts',(5.36302884120956,-0.214067207837933,5.59083868637675));
#6626=CARTESIAN_POINT('Ctrl Pts',(5.35911620649258,-0.145717273873157,5.59716157616642));
#6627=CARTESIAN_POINT('Ctrl Pts',(5.35520357177561,-0.0771464480078521,
5.59987095356091));
#6628=CARTESIAN_POINT('Ctrl Pts',(5.35129552801878,-0.0086560809513348,
5.60257715185882));
#6629=CARTESIAN_POINT('Ctrl Pts',(5.34738748426195,0.0600541741938194,5.60167823916572));
#6630=CARTESIAN_POINT('Ctrl Pts',(5.34347944050512,0.128575292284431,5.59715968343516));
#6631=CARTESIAN_POINT('Ctrl Pts',(5.33957383962591,0.19705357853482,5.59264395220693));
#6632=CARTESIAN_POINT('Ctrl Pts',(5.3356682387467,0.265342472664014,5.58451309856252));
#6633=CARTESIAN_POINT('Ctrl Pts',(5.33176263786749,0.333033891361192,5.57280466541196));
#6634=CARTESIAN_POINT('Ctrl Pts',(5.32785813960241,0.40070619967885,5.56109953774096));
#6635=CARTESIAN_POINT('Ctrl Pts',(5.32395364133733,0.467780883087807,5.54581891941337));
#6636=CARTESIAN_POINT('Ctrl Pts',(5.32004914307226,0.533857724051826,5.52705186538319));
#6637=CARTESIAN_POINT('Ctrl Pts',(5.31614440879464,0.599938559117517,5.50828367695372));
#6638=CARTESIAN_POINT('Ctrl Pts',(5.31223967451703,0.665020959650779,5.48602877125562));
#6639=CARTESIAN_POINT('Ctrl Pts',(5.30833494023941,0.728719356347928,5.46042621088626));
#6640=CARTESIAN_POINT('Ctrl Pts',(5.30442605130004,0.792485528538487,5.43479640923217));
#6641=CARTESIAN_POINT('Ctrl Pts',(5.30051716236068,0.854864300948419,5.40581202823348));
#6642=CARTESIAN_POINT('Ctrl Pts',(5.29660827342131,0.915490550093816,5.37366010621128));
#6643=CARTESIAN_POINT('Ctrl Pts',(5.29269704150905,0.976153138378216,5.34148891245151));
#6644=CARTESIAN_POINT('Ctrl Pts',(5.28878580959679,1.03506069105752,5.30614665209333));
#6645=CARTESIAN_POINT('Ctrl Pts',(5.28487457768453,1.09187558439379,5.26786468035342));
#6646=CARTESIAN_POINT('Ctrl Pts',(5.28095661368922,1.14878826855117,5.22951681699196));
#6647=CARTESIAN_POINT('Ctrl Pts',(5.27703864969391,1.2036007120853,5.18821943943023));
#6648=CARTESIAN_POINT('Ctrl Pts',(5.2731206856986,1.25600768300813,5.14424472807092));
#6649=CARTESIAN_POINT('Ctrl Pts',(5.27130362818142,1.28031277631217,5.12385031404954));
#6650=CARTESIAN_POINT('Ctrl Pts',(5.26948657066424,1.30410099538047,5.10288056396185));
#6651=CARTESIAN_POINT('Ctrl Pts',(5.26766951314706,1.32734469991678,5.08136519588009));
#6652=CARTESIAN_POINT('Ctrl Pts',(5.2637510139676,1.37746993607034,5.03496713121943));
#6653=CARTESIAN_POINT('Ctrl Pts',(5.25983251478814,1.42525856221545,4.98584591761485));
#6654=CARTESIAN_POINT('Ctrl Pts',(5.25591401560868,1.47040035663306,4.93426617564765));
#6655=CARTESIAN_POINT('Ctrl Pts',(5.25200140773905,1.51547428213322,4.88276398179955));
#6656=CARTESIAN_POINT('Ctrl Pts',(5.24808879986942,1.55790895241809,4.82881096259536));
#6657=CARTESIAN_POINT('Ctrl Pts',(5.2441761919998,1.59742967920941,4.77270972188214));
#6658=CARTESIAN_POINT('Ctrl Pts',(5.24026817509748,1.63690403325633,4.71667430912065));
#6659=CARTESIAN_POINT('Ctrl Pts',(5.23636015819516,1.67347095248099,4.6584960811169));
#6660=CARTESIAN_POINT('Ctrl Pts',(5.23245214129284,1.70689606355718,4.59851056435891));
#6661=CARTESIAN_POINT('Ctrl Pts',(5.22854656725618,1.74030028090181,4.53856254399939));
#6662=CARTESIAN_POINT('Ctrl Pts',(5.22464099321952,1.77056634709305,4.47680990453244));
#6663=CARTESIAN_POINT('Ctrl Pts',(5.22073541918286,1.79750412333855,4.41361566779541));
#6664=CARTESIAN_POINT('Ctrl Pts',(5.21683094770655,1.82443429493397,4.3504392710632));
#6665=CARTESIAN_POINT('Ctrl Pts',(5.21292647623023,1.84803784911861,4.28582253714588));
#6666=CARTESIAN_POINT('Ctrl Pts',(5.20902200475392,1.86817217000137,4.2201498639218));
#6667=CARTESIAN_POINT('Ctrl Pts',(5.20511729716942,1.88830770843128,4.15447321939041));
#6668=CARTESIAN_POINT('Ctrl Pts',(5.20121258958492,1.90497345537369,4.08774097969503));
#6669=CARTESIAN_POINT('Ctrl Pts',(5.19730788200041,1.91807673883901,4.02035240683018));
#6670=CARTESIAN_POINT('Ctrl Pts',(5.19339901942455,1.93119396548149,3.95289212592267));
#6671=CARTESIAN_POINT('Ctrl Pts',(5.18949015684869,1.94074106941273,3.88477460170885));
#6672=CARTESIAN_POINT('Ctrl Pts',(5.18558129427282,1.94667676563991,3.81640798880139));
#6673=CARTESIAN_POINT('Ctrl Pts',(5.18167008857389,1.95261601995246,3.74800039430797));
#6674=CARTESIAN_POINT('Ctrl Pts',(5.17775888287496,1.95493954153139,3.67934390549881));
#6675=CARTESIAN_POINT('Ctrl Pts',(5.17384767717603,1.95365819189621,3.610847659438));
#6676=CARTESIAN_POINT('Ctrl Pts',(5.16992973888634,1.95237463659778,3.54223350671916));
#6677=CARTESIAN_POINT('Ctrl Pts',(5.16601180059666,1.94747386063337,3.47378063748742));
#6678=CARTESIAN_POINT('Ctrl Pts',(5.16209386230698,1.93901859753385,3.40589316721522));
#6679=CARTESIAN_POINT('Ctrl Pts',(5.16027656572998,1.93509670812358,3.37440424160557));
#6680=CARTESIAN_POINT('Ctrl Pts',(5.15845926915297,1.93041080123306,3.34303681436164));
#6681=CARTESIAN_POINT('Ctrl Pts',(5.15664197257597,1.92497081948355,3.31183025067891));
#6682=CARTESIAN_POINT('Ctrl Pts',(5.1527234949001,1.91324106259501,3.24454226660472));
#6683=CARTESIAN_POINT('Ctrl Pts',(5.14880501722423,1.89795575006274,3.17773696910643));
#6684=CARTESIAN_POINT('Ctrl Pts',(5.14488653954836,1.87916855139227,3.11181855820361));
#6685=CARTESIAN_POINT('Ctrl Pts',(5.1409739536715,1.86040960103854,3.04599926181934));
#6686=CARTESIAN_POINT('Ctrl Pts',(5.13706136779464,1.83815934832929,2.98106467459703));
#6687=CARTESIAN_POINT('Ctrl Pts',(5.13314878191778,1.81252265527333,2.91740979438932));
#6688=CARTESIAN_POINT('Ctrl Pts',(5.1292407876249,1.78691604795422,2.85382961585905));
#6689=CARTESIAN_POINT('Ctrl Pts',(5.12533279333202,1.75793107587759,2.79152661575932));
#6690=CARTESIAN_POINT('Ctrl Pts',(5.12142479903914,1.72572214182346,2.73087982616392));
#6691=CARTESIAN_POINT('Ctrl Pts',(5.11751924798183,1.69353334444492,2.6702709522824));
#6692=CARTESIAN_POINT('Ctrl Pts',(5.11361369692452,1.65812481356218,2.61131666823854));
#6693=CARTESIAN_POINT('Ctrl Pts',(5.10970814586721,1.61969806496519,2.55437380134843));
#6694=CARTESIAN_POINT('Ctrl Pts',(5.10580369770541,1.58128216776612,2.49744701465582));
#6695=CARTESIAN_POINT('Ctrl Pts',(5.10189924954361,1.53985001983801,2.44253092495091));
#6696=CARTESIAN_POINT('Ctrl Pts',(5.09799480138181,1.49564689828914,2.38995406984024));
#6697=CARTESIAN_POINT('Ctrl Pts',(5.09409011741262,1.45144110711252,2.33737403937394));
#6698=CARTESIAN_POINT('Ctrl Pts',(5.09018543344342,1.40446432849761,2.28713389874035));
#6699=CARTESIAN_POINT('Ctrl Pts',(5.08628074947422,1.35500144837195,2.23952832588612));
#6700=CARTESIAN_POINT('Ctrl Pts',(5.08237191080845,1.30548593831249,2.1918720993267));
#6701=CARTESIAN_POINT('Ctrl Pts',(5.07846307214267,1.25347940263475,2.14685637657938));
#6702=CARTESIAN_POINT('Ctrl Pts',(5.0745542334769,1.19930210612833,2.10473752060038));
#6703=CARTESIAN_POINT('Ctrl Pts',(5.07064305189136,1.14509233627887,2.06259341898996));
#6704=CARTESIAN_POINT('Ctrl Pts',(5.06673187030582,1.08870961977553,2.0233499207839));
#6705=CARTESIAN_POINT('Ctrl Pts',(5.06282068872027,1.03050337127767,1.98722013955048));
#6706=CARTESIAN_POINT('Ctrl Pts',(5.05890277460612,0.972196929213073,1.95102816616862));
#6707=CARTESIAN_POINT('Ctrl Pts',(5.05498486049197,0.912061121091883,1.91796084372818));
#6708=CARTESIAN_POINT('Ctrl Pts',(5.05106694637782,0.85046932120423,1.8881850055733));
#6709=CARTESIAN_POINT('Ctrl Pts',(5.04924944158685,0.821897129951701,1.87437211255804));
#6710=CARTESIAN_POINT('Ctrl Pts',(5.04743193679588,0.793011879616,1.86126686004469));
#6711=CARTESIAN_POINT('Ctrl Pts',(5.0456144320049,0.763852036129499,1.84888228681252));
#6712=CARTESIAN_POINT('Ctrl Pts',(5.04169593494842,0.700984107837442,1.82218144178747));
#6713=CARTESIAN_POINT('Ctrl Pts',(5.03777743789193,0.636590155551074,1.79872813327964));
#6714=CARTESIAN_POINT('Ctrl Pts',(5.03385894083545,0.571038710239964,1.77869684924341));
#6715=CARTESIAN_POINT('Ctrl Pts',(5.02994633527566,0.505585822135272,1.75869568242865));
#6716=CARTESIAN_POINT('Ctrl Pts',(5.02603372971586,0.438979361448329,1.74210647146395));
#6717=CARTESIAN_POINT('Ctrl Pts',(5.02212112415607,0.371607938864396,1.72905572349114));
#6718=CARTESIAN_POINT('Ctrl Pts',(5.01821310983003,0.304315573048273,1.71602028987436));
#6719=CARTESIAN_POINT('Ctrl Pts',(5.01430509550399,0.236260508593107,1.70651516594548));
#6720=CARTESIAN_POINT('Ctrl Pts',(5.01039708117795,0.167844859934864,1.70061659112545));
#6721=CARTESIAN_POINT('Ctrl Pts',(5.00649150988179,0.0994719801766054,1.69472170370094));
#6722=CARTESIAN_POINT('Ctrl Pts',(5.00258593858563,0.0307394522219118,1.69242893512387));
#6723=CARTESIAN_POINT('Ctrl Pts',(4.99868036728947,-0.0379436627796898,
1.69376290669022));
#6724=CARTESIAN_POINT('Ctrl Pts',(4.99477589871406,-0.106607385407976,1.6950965016156));
#6725=CARTESIAN_POINT('Ctrl Pts',(4.99087143013866,-0.175221231337169,1.70005479430132));
#6726=CARTESIAN_POINT('Ctrl Pts',(4.98696696156326,-0.243376122230716,1.70861029692081));
#6727=CARTESIAN_POINT('Ctrl Pts',(4.98306225703643,-0.31153513180085,1.71716631655894));
#6728=CARTESIAN_POINT('Ctrl Pts',(4.97915755250961,-0.379234643660647,1.72931991390672));
#6729=CARTESIAN_POINT('Ctrl Pts',(4.97525284798278,-0.446072494380595,1.74499195310548));
#6730=CARTESIAN_POINT('Ctrl Pts',(4.97134398868202,-0.512981463454875,1.76068066802951));
#6731=CARTESIAN_POINT('Ctrl Pts',(4.96743512938126,-0.579026461982407,1.77989518365212));
#6732=CARTESIAN_POINT('Ctrl Pts',(4.9635262700805,-0.643818279759126,1.80250584762191));
#6733=CARTESIAN_POINT('Ctrl Pts',(4.95961506778575,-0.708648934144592,1.82513006456089));
#6734=CARTESIAN_POINT('Ctrl Pts',(4.95570386549101,-0.772224457656741,1.85115429490041));
#6735=CARTESIAN_POINT('Ctrl Pts',(4.95179266319626,-0.834176119683401,1.88040091952656));
#6736=CARTESIAN_POINT('Ctrl Pts',(4.94787472847511,-0.896234420276364,1.90969788692024));
#6737=CARTESIAN_POINT('Ctrl Pts',(4.94395679375397,-0.956662847974479,1.94222808592322));
#6738=CARTESIAN_POINT('Ctrl Pts',(4.94003885903282,-1.01511851568075,1.97776864220124));
#6739=CARTESIAN_POINT('Ctrl Pts',(4.93822153649982,-1.04223300575396,1.99425402502569));
#6740=CARTESIAN_POINT('Ctrl Pts',(4.93640421396682,-1.06892347732316,2.01138649999384));
#6741=CARTESIAN_POINT('Ctrl Pts',(4.93458689143382,-1.09515809873353,2.02914086060109));
#6742=CARTESIAN_POINT('Ctrl Pts',(4.93068215939183,-1.15152628047912,2.06728820070679));
#6743=CARTESIAN_POINT('Ctrl Pts',(4.92677742734985,-1.20601427441912,2.10846238665924));
#6744=CARTESIAN_POINT('Ctrl Pts',(4.92287269530787,-1.25827678983217,2.15245115157596));
#6745=CARTESIAN_POINT('Ctrl Pts',(4.91883090350855,-1.31237376855875,2.19798396340297));
#6746=CARTESIAN_POINT('Ctrl Pts',(4.91478911170923,-1.36408562775221,2.24653241326184));
#6747=CARTESIAN_POINT('Ctrl Pts',(4.91074731990991,-1.41306090869161,2.2978112480534));
#6748=CARTESIAN_POINT('Ctrl Pts',(4.90685312352861,-1.46024774346118,2.34721751705428));
#6749=CARTESIAN_POINT('Ctrl Pts',(4.90295892714731,-1.50489402519348,2.39915781793863));
#6750=CARTESIAN_POINT('Ctrl Pts',(4.89906473076601,-1.54671985078526,2.45333680502517));
#6751=CARTESIAN_POINT('Ctrl Pts',(4.8951728750249,-1.58852053660526,2.50748322736611));
#6752=CARTESIAN_POINT('Ctrl Pts',(4.89128101928378,-1.62750382633117,2.56386527560233));
#6753=CARTESIAN_POINT('Ctrl Pts',(4.88738916354267,-1.66342951017403,2.6221538796013));
#6754=CARTESIAN_POINT('Ctrl Pts',(4.88349828789472,-1.69934614678601,2.68042780467419));
#6755=CARTESIAN_POINT('Ctrl Pts',(4.87960741224678,-1.7322064461976,2.74060691051924));
#6756=CARTESIAN_POINT('Ctrl Pts',(4.87571653659884,-1.7618140741168,2.80233401586407));
#6757=CARTESIAN_POINT('Ctrl Pts',(4.87182528202397,-1.79142458548136,2.86406713272511));
#6758=CARTESIAN_POINT('Ctrl Pts',(4.86793402744911,-1.81778158504715,2.92734810008857));
#6759=CARTESIAN_POINT('Ctrl Pts',(4.86404277287425,-1.84073598285885,2.9917977619097));
#6760=CARTESIAN_POINT('Ctrl Pts',(4.86014733215933,-1.86371507458922,3.05631675749073));
#6761=CARTESIAN_POINT('Ctrl Pts',(4.85625189144442,-1.88328409647481,3.12200648773817));
#6762=CARTESIAN_POINT('Ctrl Pts',(4.85235645072951,-1.89934352177914,3.18847161390025));
#6763=CARTESIAN_POINT('Ctrl Pts',(4.84845849903485,-1.91541329890106,3.25497958311862));
#6764=CARTESIAN_POINT('Ctrl Pts',(4.84456054734019,-1.92796888898619,3.32226345550716));
#6765=CARTESIAN_POINT('Ctrl Pts',(4.84066259564552,-1.93696221203219,3.389919442001));
#6766=CARTESIAN_POINT('Ctrl Pts',(4.83675820641697,-1.94597038770502,3.45768716351374));
#6767=CARTESIAN_POINT('Ctrl Pts',(4.83285381718841,-1.95140452392265,3.52582773192013));
#6768=CARTESIAN_POINT('Ctrl Pts',(4.82894942795985,-1.95326856711039,3.59393509362883));
#6769=CARTESIAN_POINT('Ctrl Pts',(4.82792284934798,-1.95375867881702,3.61184251954066));
#6770=CARTESIAN_POINT('Ctrl Pts',(4.8268962707361,-1.95400226243369,3.62974767089812));
#6771=CARTESIAN_POINT('Ctrl Pts',(4.82586969212423,-1.95399998416516,3.64764323036849));
#6772=CARTESIAN_POINT('Ctrl Pts',(4.72413079030316,-1.95710318190607,3.64776998461592));
#6773=CARTESIAN_POINT('Ctrl Pts',(4.75994664419966,-1.9554136014585,3.022364796511));
#6774=CARTESIAN_POINT('Ctrl Pts',(4.8327716782865,-1.29210840943672,1.74764265246943));
#6775=CARTESIAN_POINT('Ctrl Pts',(4.94260589256374,0.878268351030341,1.51220654580568));
#6776=CARTESIAN_POINT('Ctrl Pts',(5.05363343313481,2.26979830067418,3.22502187308483));
#6777=CARTESIAN_POINT('Ctrl Pts',(5.16466097370589,1.5875322833648,5.32373643149222));
#6778=CARTESIAN_POINT('Ctrl Pts',(5.27568851427697,-0.545177970067405,5.8908661531987));
#6779=CARTESIAN_POINT('Ctrl Pts',(5.36217802636002,-1.81852615233383,4.735922224886));
#6780=CARTESIAN_POINT('Ctrl Pts',(5.41165835825273,-1.95368429139157,3.8680854635217));
#6781=CARTESIAN_POINT('Ctrl Pts',(5.42412950995508,-1.95213885961564,3.64888667332463));
#6782=CARTESIAN_POINT('Origin',(0.,0.,3.64739446828387));
#6783=CARTESIAN_POINT('',(6.22586985342116,-1.95353597714873,3.64632535240864));
#6784=CARTESIAN_POINT('',(6.12413030792735,-1.95399955699052,3.64607868681971));
#6785=CARTESIAN_POINT('',(0.,-1.954,3.64739446828387));
#6786=CARTESIAN_POINT('Ctrl Pts',(6.22586969212423,-1.95399970893239,3.64632793551611));
#6787=CARTESIAN_POINT('Ctrl Pts',(6.22192922025797,-1.95403757522788,3.71570295389058));
#6788=CARTESIAN_POINT('Ctrl Pts',(6.21798874839172,-1.95037645685081,3.78509205096179));
#6789=CARTESIAN_POINT('Ctrl Pts',(6.21404827652546,-1.94303829200873,3.85407827458662));
#6790=CARTESIAN_POINT('Ctrl Pts',(6.21010723418459,-1.93569906479724,3.92307448556594));
#6791=CARTESIAN_POINT('Ctrl Pts',(6.20616619184372,-1.92468178589053,3.9916672306491));
#6792=CARTESIAN_POINT('Ctrl Pts',(6.20222514950284,-1.91006015343086,4.05944569116239));
#6793=CARTESIAN_POINT('Ctrl Pts',(6.19827911405417,-1.89541999607833,4.12731002366864));
#6794=CARTESIAN_POINT('Ctrl Pts',(6.19433307860549,-1.87716646696284,4.19435754146509));
#6795=CARTESIAN_POINT('Ctrl Pts',(6.19038704315681,-1.8554240829409,4.26018927280079));
#6796=CARTESIAN_POINT('Ctrl Pts',(6.1864385391419,-1.83366809728873,4.32606218724066));
#6797=CARTESIAN_POINT('Ctrl Pts',(6.182490035127,-1.80841908414581,4.39071735315625));
#6798=CARTESIAN_POINT('Ctrl Pts',(6.17854153111209,-1.77984999050235,4.45377527863887));
#6799=CARTESIAN_POINT('Ctrl Pts',(6.17458487851165,-1.75122193840214,4.51696333768535));
#6800=CARTESIAN_POINT('Ctrl Pts',(6.1706282259112,-1.71926033568415,4.57854714271377));
#6801=CARTESIAN_POINT('Ctrl Pts',(6.16667157331076,-1.68418427929637,4.6381715942668));
#6802=CARTESIAN_POINT('Ctrl Pts',(6.16307766144574,-1.65232394988149,4.69232975408553));
#6803=CARTESIAN_POINT('Ctrl Pts',(6.15948374958071,-1.61789476739727,4.74487148430732));
#6804=CARTESIAN_POINT('Ctrl Pts',(6.15588983771569,-1.58109015814158,4.79555382648631));
#6805=CARTESIAN_POINT('Ctrl Pts',(6.15197641278596,-1.54101347268034,4.85074203054616));
#6806=CARTESIAN_POINT('Ctrl Pts',(6.14806298785624,-1.49796252247789,4.90394126259883));
#6807=CARTESIAN_POINT('Ctrl Pts',(6.14414956292652,-1.45216195437606,4.95481240385869));
#6808=CARTESIAN_POINT('Ctrl Pts',(6.1402421044734,-1.40643121462739,5.00560598608019));
#6809=CARTESIAN_POINT('Ctrl Pts',(6.13633464602028,-1.35795950337581,5.0540781577686));
#6810=CARTESIAN_POINT('Ctrl Pts',(6.13242718756716,-1.30701347514826,5.09992046659883));
#6811=CARTESIAN_POINT('Ctrl Pts',(6.12852440627108,-1.25612842839426,5.14570790301524));
#6812=CARTESIAN_POINT('Ctrl Pts',(6.12462162497499,-1.20277531117033,5.18887139966881));
#6813=CARTESIAN_POINT('Ctrl Pts',(6.12071884367891,-1.14725832432906,5.22913854911922));
#6814=CARTESIAN_POINT('Ctrl Pts',(6.11681855583622,-1.09177680681312,5.26937997223424));
#6815=CARTESIAN_POINT('Ctrl Pts',(6.11291826799353,-1.03413456015337,5.30672842959029));
#6816=CARTESIAN_POINT('Ctrl Pts',(6.10901798015085,-0.974668408497115,5.34095211226228));
#6817=CARTESIAN_POINT('Ctrl Pts',(6.10511883754132,-0.915219717759566,5.37516574590766));
#6818=CARTESIAN_POINT('Ctrl Pts',(6.1012196949318,-0.853948612355486,5.40625618021191));
#6819=CARTESIAN_POINT('Ctrl Pts',(6.09732055232227,-0.791218844617588,5.4340362174664));
#6820=CARTESIAN_POINT('Ctrl Pts',(6.09342120841215,-0.728485838336974,5.46181768891777));
#6821=CARTESIAN_POINT('Ctrl Pts',(6.08952186450202,-0.664294472261642,5.48628822667262));
#6822=CARTESIAN_POINT('Ctrl Pts',(6.0856225205919,-0.599029234794682,5.50730843830004));
#6823=CARTESIAN_POINT('Ctrl Pts',(6.08171903797274,-0.533694725718389,5.52835096048579));
#6824=CARTESIAN_POINT('Ctrl Pts',(6.07781555535358,-0.467284540994088,5.54593569663872));
#6825=CARTESIAN_POINT('Ctrl Pts',(6.07391207273442,-0.400198132893067,5.55997321291869));
#6826=CARTESIAN_POINT('Ctrl Pts',(6.07000626427478,-0.333071752208878,5.57401909327423));
#6827=CARTESIAN_POINT('Ctrl Pts',(6.06610045581514,-0.265268833825991,5.58451347230018));
#6828=CARTESIAN_POINT('Ctrl Pts',(6.0621946473555,-0.19719600918756,5.59141857666332));
#6829=CARTESIAN_POINT('Ctrl Pts',(6.0582820765205,-0.129005325725104,5.59833563627416));
#6830=CARTESIAN_POINT('Ctrl Pts',(6.0543695056855,-0.0605442957425206,5.60165099501344));
#6831=CARTESIAN_POINT('Ctrl Pts',(6.0504569348505,0.00777927282227454,5.60137898278606));
#6832=CARTESIAN_POINT('Ctrl Pts',(6.0485920556152,0.0403448696309175,5.60124933147086));
#6833=CARTESIAN_POINT('Ctrl Pts',(6.04672717637991,0.0728792977294585,5.60030545174069));
#6834=CARTESIAN_POINT('Ctrl Pts',(6.04486229714461,0.105338970147309,5.59855302190485));
#6835=CARTESIAN_POINT('Ctrl Pts',(6.0409427454772,0.173561813075101,5.59486981327929));
#6836=CARTESIAN_POINT('Ctrl Pts',(6.03702319380979,0.241725674141686,5.58759689429554));
#6837=CARTESIAN_POINT('Ctrl Pts',(6.03310364214238,0.309422647204876,5.57673985607651));
#6838=CARTESIAN_POINT('Ctrl Pts',(6.02918997732355,0.377017944907487,5.56589912424794));
#6839=CARTESIAN_POINT('Ctrl Pts',(6.02527631250471,0.444147264941309,5.55148503414074));
#6840=CARTESIAN_POINT('Ctrl Pts',(6.02136264768587,0.510405798910706,5.53355509782694));
#6841=CARTESIAN_POINT('Ctrl Pts',(6.01745357256907,0.576586629003434,5.51564618862432));
#6842=CARTESIAN_POINT('Ctrl Pts',(6.01354449745227,0.641898229039043,5.494229749871));
#6843=CARTESIAN_POINT('Ctrl Pts',(6.00963542233547,0.705945795963414,5.46941437299446));
#6844=CARTESIAN_POINT('Ctrl Pts',(6.00572878995174,0.769953340349117,5.44461450294243));
#6845=CARTESIAN_POINT('Ctrl Pts',(6.00182215756802,0.832697961298201,5.4164200853168));
#6846=CARTESIAN_POINT('Ctrl Pts',(5.99791552518429,0.893801338935865,5.38498911794082));
#6847=CARTESIAN_POINT('Ctrl Pts',(5.9940099968832,0.954887447690414,5.35356703350589));
#6848=CARTESIAN_POINT('Ctrl Pts',(5.9901044685821,1.01433279715154,5.31891043993515));
#6849=CARTESIAN_POINT('Ctrl Pts',(5.98619894028101,1.07178198514831,5.28122413391966));
#6850=CARTESIAN_POINT('Ctrl Pts',(5.98229317904975,1.12923459948019,5.24353558024988));
#6851=CARTESIAN_POINT('Ctrl Pts',(5.97838741781849,1.18469040646371,5.20281722710309));
#6852=CARTESIAN_POINT('Ctrl Pts',(5.97448165658724,1.23782293994471,5.15931720749597));
#6853=CARTESIAN_POINT('Ctrl Pts',(5.97057175247585,1.29101183163716,5.11577104698155));
#6854=CARTESIAN_POINT('Ctrl Pts',(5.96666184836446,1.34187215084874,5.06943764360154));
#6855=CARTESIAN_POINT('Ctrl Pts',(5.96275194425307,1.39011129021969,5.02060479478297));
#6856=CARTESIAN_POINT('Ctrl Pts',(5.95883970243907,1.4383792714135,4.97174274916706));
#6857=CARTESIAN_POINT('Ctrl Pts',(5.95492746062508,1.48402262717616,4.92037865129621));
#6858=CARTESIAN_POINT('Ctrl Pts',(5.95101521881108,1.52678824140369,4.86683436672554));
#6859=CARTESIAN_POINT('Ctrl Pts',(5.94709626367075,1.56962724054399,4.81319820126589));
#6860=CARTESIAN_POINT('Ctrl Pts',(5.94317730853042,1.60957835661113,4.75737478184438));
#6861=CARTESIAN_POINT('Ctrl Pts',(5.93925835339009,1.64643158878359,4.69971524801576));
#6862=CARTESIAN_POINT('Ctrl Pts',(5.93745048778457,1.66343247001623,4.67311614588104));
#6863=CARTESIAN_POINT('Ctrl Pts',(5.93564262217905,1.67977473443783,4.64612664650916));
#6864=CARTESIAN_POINT('Ctrl Pts',(5.93383475657353,1.69544115163435,4.61878280532771));
#6865=CARTESIAN_POINT('Ctrl Pts',(5.9299154907718,1.72940432509505,4.55950418345275));
#6866=CARTESIAN_POINT('Ctrl Pts',(5.92599622497008,1.76032172067738,4.49832553361446));
#6867=CARTESIAN_POINT('Ctrl Pts',(5.92207695916835,1.78797652885593,4.43559236999402));
#6868=CARTESIAN_POINT('Ctrl Pts',(5.91816356697678,1.81558989213881,4.37295322146871));
#6869=CARTESIAN_POINT('Ctrl Pts',(5.91425017478521,1.83995017544407,4.30876462905164));
#6870=CARTESIAN_POINT('Ctrl Pts',(5.91033678259365,1.86088584978546,4.24339770155383));
#6871=CARTESIAN_POINT('Ctrl Pts',(5.90642795900979,1.88179708321256,4.17810708530575));
#6872=CARTESIAN_POINT('Ctrl Pts',(5.90251913542593,1.89929149862642,4.11164133195098));
#6873=CARTESIAN_POINT('Ctrl Pts',(5.89861031184207,1.91324589168177,4.04439088887583));
#6874=CARTESIAN_POINT('Ctrl Pts',(5.89470391770692,1.92719161167183,3.97718224392699));
#6875=CARTESIAN_POINT('Ctrl Pts',(5.89079752357176,1.93760157433054,3.90919035696604));
#6876=CARTESIAN_POINT('Ctrl Pts',(5.88689112943661,1.94440301405621,3.84081866255422));
#6877=CARTESIAN_POINT('Ctrl Pts',(5.8829858256886,1.9512025553041,3.77246605265203));
#6878=CARTESIAN_POINT('Ctrl Pts',(5.87908052194059,1.95439552460934,3.70373433466594));
#6879=CARTESIAN_POINT('Ctrl Pts',(5.87517521819257,1.95396089951249,3.63503311009168));
#6880=CARTESIAN_POINT('Ctrl Pts',(5.87126966739349,1.95352624692107,3.56632753945049));
#6881=CARTESIAN_POINT('Ctrl Pts',(5.8673641165944,1.94946355000497,3.49765295755854));
#6882=CARTESIAN_POINT('Ctrl Pts',(5.86345856579531,1.94180388956307,3.42941819783743));
#6883=CARTESIAN_POINT('Ctrl Pts',(5.85954884918067,1.93413605902323,3.36111065621248));
#6884=CARTESIAN_POINT('Ctrl Pts',(5.85563913256604,1.92286366321745,3.29324436238415));
#6885=CARTESIAN_POINT('Ctrl Pts',(5.85172941595141,1.90806947589925,3.22622125552985));
#6886=CARTESIAN_POINT('Ctrl Pts',(5.84781734878636,1.8932663942067,3.15915785389015));
#6887=CARTESIAN_POINT('Ctrl Pts',(5.8439052816213,1.87493743823196,3.09293912189533));
#6888=CARTESIAN_POINT('Ctrl Pts',(5.83999321445625,1.85321543256454,3.02795233175729));
#6889=CARTESIAN_POINT('Ctrl Pts',(5.83607441223039,1.83145603003688,2.96285365959759));
#6890=CARTESIAN_POINT('Ctrl Pts',(5.83215561000453,1.80629209935244,2.89899161930871));
#6891=CARTESIAN_POINT('Ctrl Pts',(5.82823680777867,1.77790445793083,2.83673317127403));
#6892=CARTESIAN_POINT('Ctrl Pts',(5.82642694385327,1.76479387842842,2.80797966123306));
#6893=CARTESIAN_POINT('Ctrl Pts',(5.82461707992786,1.75099633135706,2.77956783987747));
#6894=CARTESIAN_POINT('Ctrl Pts',(5.82280721600245,1.73653280861797,2.75153186464793));
#6895=CARTESIAN_POINT('Ctrl Pts',(5.81888944803674,1.70522397635551,2.69084307799401));
#6896=CARTESIAN_POINT('Ctrl Pts',(5.81497168007103,1.67066771919405,2.63167709240386));
#6897=CARTESIAN_POINT('Ctrl Pts',(5.81105391210533,1.63303593841818,2.57440349728987));
#6898=CARTESIAN_POINT('Ctrl Pts',(5.80714204705379,1.59546085757295,2.51721619649423));
#6899=CARTESIAN_POINT('Ctrl Pts',(5.80323018200225,1.55481971769912,2.46191603529415));
#6900=CARTESIAN_POINT('Ctrl Pts',(5.79931831695071,1.51133052729582,2.408848531605));
#6901=CARTESIAN_POINT('Ctrl Pts',(5.7954110563828,1.46789252609836,2.35584349133134));
#6902=CARTESIAN_POINT('Ctrl Pts',(5.79150379581489,1.42161344246653,2.30506626812452));
#6903=CARTESIAN_POINT('Ctrl Pts',(5.78759653524698,1.37275379361172,2.25683234377284));
#6904=CARTESIAN_POINT('Ctrl Pts',(5.78369172549626,1.32392479182156,2.20862867400204));
#6905=CARTESIAN_POINT('Ctrl Pts',(5.77978691574554,1.27251878501437,2.16296548343143));
#6906=CARTESIAN_POINT('Ctrl Pts',(5.77588210599482,1.21883461745178,2.12012298773394));
#6907=CARTESIAN_POINT('Ctrl Pts',(5.77197840559194,1.1651657014428,2.07729266349499));
#6908=CARTESIAN_POINT('Ctrl Pts',(5.76807470518906,1.10922029387594,2.03728175003941));
#6909=CARTESIAN_POINT('Ctrl Pts',(5.76417100478618,1.05133054742943,2.00033038937202));
#6910=CARTESIAN_POINT('Ctrl Pts',(5.76026707390628,0.993437383134513,1.96337684707219));
#6911=CARTESIAN_POINT('Ctrl Pts',(5.75636314302638,0.933600068134951,1.9294834787164));
#6912=CARTESIAN_POINT('Ctrl Pts',(5.75245921214648,0.872178434039021,1.89884627644092));
#6913=CARTESIAN_POINT('Ctrl Pts',(5.74855112949317,0.810691478933375,1.86817649194883));
#6914=CARTESIAN_POINT('Ctrl Pts',(5.74464304683987,0.747617283319029,1.84077000432081));
#6915=CARTESIAN_POINT('Ctrl Pts',(5.74073496418656,0.683337987343999,1.81677566715332));
#6916=CARTESIAN_POINT('Ctrl Pts',(5.73682454138663,0.619020201144718,1.79276696225818));
#6917=CARTESIAN_POINT('Ctrl Pts',(5.73291411858669,0.553496347862577,1.77217462161367));
#6918=CARTESIAN_POINT('Ctrl Pts',(5.72900369578676,0.487163454161308,1.75509751248396));
#6919=CARTESIAN_POINT('Ctrl Pts',(5.72508653679808,0.420716293815509,1.73799098591367));
#6920=CARTESIAN_POINT('Ctrl Pts',(5.7211693778094,0.353457793522223,1.72441187359348));
#6921=CARTESIAN_POINT('Ctrl Pts',(5.71725221882072,0.285794006257841,1.71440771561662));
#6922=CARTESIAN_POINT('Ctrl Pts',(5.71542803769094,0.254283668215885,1.70974888092201));
#6923=CARTESIAN_POINT('Ctrl Pts',(5.71360385656115,0.222685489647637,1.70586459717762));
#6924=CARTESIAN_POINT('Ctrl Pts',(5.71177967543137,0.191040535300942,1.70275580933668));
#6925=CARTESIAN_POINT('Ctrl Pts',(5.70786098451082,0.123061104281254,1.69607753683001));
#6926=CARTESIAN_POINT('Ctrl Pts',(5.70394229359028,0.0545967376770631,1.69295492978579));
#6927=CARTESIAN_POINT('Ctrl Pts',(5.70002360266973,-0.0139486777057676,
1.69344425540989));
#6928=CARTESIAN_POINT('Ctrl Pts',(5.69611080172421,-0.0823910661356112,
1.69393284555479));
#6929=CARTESIAN_POINT('Ctrl Pts',(5.6921980007787,-0.150913773809251,1.69802259030234));
#6930=CARTESIAN_POINT('Ctrl Pts',(5.68828519983318,-0.219108106246357,1.70571796644915));
#6931=CARTESIAN_POINT('Ctrl Pts',(5.68437698884756,-0.287222442472266,1.71340431543909));
#6932=CARTESIAN_POINT('Ctrl Pts',(5.68046877786194,-0.355008682184551,1.72468784075306));
#6933=CARTESIAN_POINT('Ctrl Pts',(5.67656056687632,-0.422060281410876,1.7395210136608));
#6934=CARTESIAN_POINT('Ctrl Pts',(5.67265479824836,-0.489069978092083,1.75434491687618));
#6935=CARTESIAN_POINT('Ctrl Pts',(5.6687490296204,-0.55534546597675,1.77271396128292));
#6936=CARTESIAN_POINT('Ctrl Pts',(5.66484326099244,-0.620489011696215,1.7945292852864));
#6937=CARTESIAN_POINT('Ctrl Pts',(5.66093859471864,-0.685614171467829,1.81633845218859));
#6938=CARTESIAN_POINT('Ctrl Pts',(5.65703392844483,-0.749607557261707,1.84159181166358));
#6939=CARTESIAN_POINT('Ctrl Pts',(5.65312926217103,-0.81208700473629,1.87014077318617));
#6940=CARTESIAN_POINT('Ctrl Pts',(5.64922435988424,-0.874570228707953,1.89869146031732));
#6941=CARTESIAN_POINT('Ctrl Pts',(5.64531945759746,-0.935538886526247,1.93053793828032));
#6942=CARTESIAN_POINT('Ctrl Pts',(5.64141455531067,-0.994632859047944,1.96548440062207));
#6943=CARTESIAN_POINT('Ctrl Pts',(5.63750549952043,-1.05378968769269,2.00046803425293));
#6944=CARTESIAN_POINT('Ctrl Pts',(5.6335964437302,-1.1110674275645,2.03855798189316));
#6945=CARTESIAN_POINT('Ctrl Pts',(5.62968738793996,-1.16613342782463,2.07951410661402));
#6946=CARTESIAN_POINT('Ctrl Pts',(5.62577598959698,-1.22123242710478,2.12049477482766));
#6947=CARTESIAN_POINT('Ctrl Pts',(5.621864591254,-1.2741166703757,2.16434472458644));
#6948=CARTESIAN_POINT('Ctrl Pts',(5.61795319291102,-1.32448739361131,2.21078417172996));
#6949=CARTESIAN_POINT('Ctrl Pts',(5.61403506488184,-1.37494478129035,2.25730351943042));
#6950=CARTESIAN_POINT('Ctrl Pts',(5.61011693685267,-1.42287967463459,2.30642090478235));
#6951=CARTESIAN_POINT('Ctrl Pts',(5.6061988088235,-1.46803150387178,2.3578210878049));
#6952=CARTESIAN_POINT('Ctrl Pts',(5.60438325083577,-1.48895367987577,2.38163858742791));
#6953=CARTESIAN_POINT('Ctrl Pts',(5.60256769284803,-1.50927887683695,2.40594579641597));
#6954=CARTESIAN_POINT('Ctrl Pts',(5.60075213486029,-1.52898432404688,2.43070924324869));
#6955=CARTESIAN_POINT('Ctrl Pts',(5.59684165166294,-1.57142737501594,2.48404658824237));
#6956=CARTESIAN_POINT('Ctrl Pts',(5.59293116846558,-1.6111640527522,2.53971800749396));
#6957=CARTESIAN_POINT('Ctrl Pts',(5.58902068526823,-1.64792721276267,2.59741737261166));
#6958=CARTESIAN_POINT('Ctrl Pts',(5.58511589987983,-1.68463680664033,2.65503266628787));
#6959=CARTESIAN_POINT('Ctrl Pts',(5.58121111449144,-1.71838121312398,2.71466963328178));
#6960=CARTESIAN_POINT('Ctrl Pts',(5.57730632910304,-1.7489338680892,2.77598966852054));
#6961=CARTESIAN_POINT('Ctrl Pts',(5.57340588306939,-1.77945257014912,2.8372415593263));
#6962=CARTESIAN_POINT('Ctrl Pts',(5.56950543703574,-1.80678633979231,2.9001723678975));
#6963=CARTESIAN_POINT('Ctrl Pts',(5.5656049910021,-1.83075322221421,2.96441669459553));
#6964=CARTESIAN_POINT('Ctrl Pts',(5.56170723775053,-1.85470355842809,3.02861666842466));
#6965=CARTESIAN_POINT('Ctrl Pts',(5.55780948449896,-1.87529144678611,3.09412790017198));
#6966=CARTESIAN_POINT('Ctrl Pts',(5.5539117312474,-1.89238272508188,3.16056429069452));
#6967=CARTESIAN_POINT('Ctrl Pts',(5.55001553362784,-1.90946718207883,3.22697416579414));
#6968=CARTESIAN_POINT('Ctrl Pts',(5.54611933600829,-1.92305768028661,3.29430798817087));
#6969=CARTESIAN_POINT('Ctrl Pts',(5.54222313838873,-1.93307022193267,3.36216558286517));
#6970=CARTESIAN_POINT('Ctrl Pts',(5.53832611196746,-1.94308489345316,3.4300376122716));
#6971=CARTESIAN_POINT('Ctrl Pts',(5.53442908554619,-1.94952001575366,3.49843314824966));
#6972=CARTESIAN_POINT('Ctrl Pts',(5.53053205912492,-1.9523431543508,3.56694443621705));
#6973=CARTESIAN_POINT('Ctrl Pts',(5.52897793679136,-1.95346901347268,3.59426653035276));
#6974=CARTESIAN_POINT('Ctrl Pts',(5.52742381445779,-1.95402100669827,3.62160699243968));
#6975=CARTESIAN_POINT('Ctrl Pts',(5.52586969212423,-1.95399938885048,3.64893990412505));
#6976=CARTESIAN_POINT('Ctrl Pts',(5.42413030787577,-1.95399943981962,3.64887405762318));
#6977=CARTESIAN_POINT('Ctrl Pts',(5.42803486416928,-1.9540514551376,3.58018073880961));
#6978=CARTESIAN_POINT('Ctrl Pts',(5.4319394204628,-1.95047675797587,3.51144725141454));
#6979=CARTESIAN_POINT('Ctrl Pts',(5.43584397675631,-1.94328925495971,3.4430837452218));
#6980=CARTESIAN_POINT('Ctrl Pts',(5.43974798134642,-1.93610276751858,3.37472989861042));
#6981=CARTESIAN_POINT('Ctrl Pts',(5.44365198593652,-1.92530453973603,3.30674641766514));
#6982=CARTESIAN_POINT('Ctrl Pts',(5.44755599052663,-1.91096035466862,3.23953846074591));
#6983=CARTESIAN_POINT('Ctrl Pts',(5.45146077678909,-1.89661329756235,3.17231704723347));
#6984=CARTESIAN_POINT('Ctrl Pts',(5.45536556305155,-1.87871897897925,3.10587194559481));
#6985=CARTESIAN_POINT('Ctrl Pts',(5.45927034931401,-1.85739392663885,3.04059647777541));
#6986=CARTESIAN_POINT('Ctrl Pts',(5.46317986564956,-1.8360430421403,2.97524193834664));
#6987=CARTESIAN_POINT('Ctrl Pts',(5.46708938198511,-1.81125328691819,2.91106032641271));
#6988=CARTESIAN_POINT('Ctrl Pts',(5.47099889832066,-1.78319022584853,2.8484272484067));
#6989=CARTESIAN_POINT('Ctrl Pts',(5.4749112282153,-1.75510696865389,2.78574909529402));
#6990=CARTESIAN_POINT('Ctrl Pts',(5.47882355810994,-1.7237459439217,2.72462212920013));
#6991=CARTESIAN_POINT('Ctrl Pts',(5.48273588800458,-1.68931847990927,2.66539697672035));
#6992=CARTESIAN_POINT('Ctrl Pts',(5.48665507658779,-1.65483066125905,2.60606799688273));
#6993=CARTESIAN_POINT('Ctrl Pts',(5.49057426517099,-1.61726594887423,2.54864789067703));
#6994=CARTESIAN_POINT('Ctrl Pts',(5.49449345375419,-1.57687814704107,2.4934571608948));
#6995=CARTESIAN_POINT('Ctrl Pts',(5.49557683430917,-1.56571375465847,2.47820079795344));
#6996=CARTESIAN_POINT('Ctrl Pts',(5.49666021486415,-1.55433386759309,2.4631145830252));
#6997=CARTESIAN_POINT('Ctrl Pts',(5.49774359541912,-1.54274435158162,2.44820479785512));
#6998=CARTESIAN_POINT('Ctrl Pts',(5.5016621214048,-1.50082572987125,2.39427695102282));
#6999=CARTESIAN_POINT('Ctrl Pts',(5.50558064739048,-1.4559931807208,2.3424430626892));
#7000=CARTESIAN_POINT('Ctrl Pts',(5.50949917337616,-1.40848368839704,2.29303495193695));
#7001=CARTESIAN_POINT('Ctrl Pts',(5.51341180805355,-1.36104562422436,2.24370112381384));
#7002=CARTESIAN_POINT('Ctrl Pts',(5.51732444273093,-1.31093894257672,2.19678618675945));
#7003=CARTESIAN_POINT('Ctrl Pts',(5.52123707740832,-1.25844152415246,2.15258982208797));
#7004=CARTESIAN_POINT('Ctrl Pts',(5.52514512098626,-1.20600570638572,2.10844531758802));
#7005=CARTESIAN_POINT('Ctrl Pts',(5.5290531645642,-1.15118509767119,2.06701336528421));
#7006=CARTESIAN_POINT('Ctrl Pts',(5.53296120814214,-1.09429384419977,2.02855631005233));
#7007=CARTESIAN_POINT('Ctrl Pts',(5.53686680875612,-1.03743815411925,1.99012329477747));
#7008=CARTESIAN_POINT('Ctrl Pts',(5.54077240937011,-0.978514793457697,1.95466176237219));
#7009=CARTESIAN_POINT('Ctrl Pts',(5.5446780099841,-0.917869103633582,1.92239234985187));
#7010=CARTESIAN_POINT('Ctrl Pts',(5.54858250789829,-0.857240536397237,1.89013204821561));
#7011=CARTESIAN_POINT('Ctrl Pts',(5.55248700581249,-0.794891039285522,1.86106230817238));
#7012=CARTESIAN_POINT('Ctrl Pts',(5.55639150372669,-0.731191334976379,1.83535825682024));
#7013=CARTESIAN_POINT('Ctrl Pts',(5.56029623756837,-0.667487781642105,1.8096526523127));
#7014=CARTESIAN_POINT('Ctrl Pts',(5.56420097141004,-0.602434316123581,1.78731332188342));
#7015=CARTESIAN_POINT('Ctrl Pts',(5.56810570525172,-0.536420762695307,1.7684669110456));
#7016=CARTESIAN_POINT('Ctrl Pts',(5.57201459363006,-0.470336972539247,1.74960044811));
#7017=CARTESIAN_POINT('Ctrl Pts',(5.5759234820084,-0.403291529645279,1.73423445667239));
#7018=CARTESIAN_POINT('Ctrl Pts',(5.57983237038674,-0.335687534543338,1.72244514969072));
#7019=CARTESIAN_POINT('Ctrl Pts',(5.58374360166571,-0.26804301911242,1.71064877646102));
#7020=CARTESIAN_POINT('Ctrl Pts',(5.58765483294468,-0.199839773474244,1.70243341304379));
#7021=CARTESIAN_POINT('Ctrl Pts',(5.59156606422366,-0.131486358979629,1.69782340330515));
#7022=CARTESIAN_POINT('Ctrl Pts',(5.59548402748142,-0.0630152951557196,
1.69320545885603));
#7023=CARTESIAN_POINT('Ctrl Pts',(5.59940199073919,0.00560596196072642,
1.69220526025078));
#7024=CARTESIAN_POINT('Ctrl Pts',(5.60331995399695,0.0739693956149147,1.69479503969838));
#7025=CARTESIAN_POINT('Ctrl Pts',(5.60513701466137,0.10567477364043,1.69599611945697));
#7026=CARTESIAN_POINT('Ctrl Pts',(5.60695407532578,0.137324779937523,1.69796863240155));
#7027=CARTESIAN_POINT('Ctrl Pts',(5.6087711359902,0.168879356249839,1.70070605895056));
#7028=CARTESIAN_POINT('Ctrl Pts',(5.6126895205751,0.236924946485997,1.70660915850138));
#7029=CARTESIAN_POINT('Ctrl Pts',(5.61660790515999,0.304795263666359,1.71609598339351));
#7030=CARTESIAN_POINT('Ctrl Pts',(5.62052628974489,0.372083006075865,1.72914781141475));
#7031=CARTESIAN_POINT('Ctrl Pts',(5.62443878264703,0.43926957464105,1.74218001470839));
#7032=CARTESIAN_POINT('Ctrl Pts',(5.62835127554917,0.505874827988566,1.75876648978475));
#7033=CARTESIAN_POINT('Ctrl Pts',(5.6322637684513,0.571496231559635,1.77883672036353));
#7034=CARTESIAN_POINT('Ctrl Pts',(5.63617167038825,0.637040634203925,1.79888340029768));
#7035=CARTESIAN_POINT('Ctrl Pts',(5.6400795723252,0.701603011786189,1.82240557394214));
#7036=CARTESIAN_POINT('Ctrl Pts',(5.64398747426214,0.764792477692673,1.84928199514302));
#7037=CARTESIAN_POINT('Ctrl Pts',(5.64789293340082,0.827942444368987,1.87614161610779));
#7038=CARTESIAN_POINT('Ctrl Pts',(5.6517983925395,0.889720750222788,1.90635113331972));
#7039=CARTESIAN_POINT('Ctrl Pts',(5.65570385167817,0.949754581589691,1.93974045334133));
#7040=CARTESIAN_POINT('Ctrl Pts',(5.65960820849432,1.00977146830488,1.97312034917018));
#7041=CARTESIAN_POINT('Ctrl Pts',(5.66351256531046,1.06804442841491,2.00967802715195));
#7042=CARTESIAN_POINT('Ctrl Pts',(5.66741692212661,1.12422507203647,2.04919736297908));
#7043=CARTESIAN_POINT('Ctrl Pts',(5.67132151545936,1.18040911894727,2.08871909279322));
#7044=CARTESIAN_POINT('Ctrl Pts',(5.67522610879212,1.23450019697237,2.1312025515863));
#7045=CARTESIAN_POINT('Ctrl Pts',(5.67913070212488,1.28618024652914,2.17638924278729));
#7046=CARTESIAN_POINT('Ctrl Pts',(5.68303945183553,1.33791530868184,2.22162403450687));
#7047=CARTESIAN_POINT('Ctrl Pts',(5.68694820154618,1.38723384954996,2.26956747692691));
#7048=CARTESIAN_POINT('Ctrl Pts',(5.69085695125683,1.43385294230903,2.31992253267402));
#7049=CARTESIAN_POINT('Ctrl Pts',(5.69476804471798,1.48049998864158,2.37030778213938));
#7050=CARTESIAN_POINT('Ctrl Pts',(5.69867913817914,1.52444405084874,2.42310714477378));
#7051=CARTESIAN_POINT('Ctrl Pts',(5.70259023164029,1.56544278674034,2.47799082477893));
#7052=CARTESIAN_POINT('Ctrl Pts',(5.70650805982365,1.60651212056052,2.53296901194476));
#7053=CARTESIAN_POINT('Ctrl Pts',(5.710425888007,1.64462573292583,2.59003827089));
#7054=CARTESIAN_POINT('Ctrl Pts',(5.71434371619036,1.67958533188226,2.64884095798712));
#7055=CARTESIAN_POINT('Ctrl Pts',(5.716162036314,1.69581058202645,2.67613212652971));
#7056=CARTESIAN_POINT('Ctrl Pts',(5.71798035643764,1.71135711117411,2.7037963513432));
#7057=CARTESIAN_POINT('Ctrl Pts',(5.71979867656128,1.72620860178437,2.73179637789395));
#7058=CARTESIAN_POINT('Ctrl Pts',(5.7237172632497,1.75821443653913,2.79213808004565));
#7059=CARTESIAN_POINT('Ctrl Pts',(5.72763584993812,1.78711577385686,2.85427932151725));
#7060=CARTESIAN_POINT('Ctrl Pts',(5.73155443662654,1.81270709470793,2.91786791715942));
#7061=CARTESIAN_POINT('Ctrl Pts',(5.73546713106489,1.83825993473059,2.9813608967194));
#7062=CARTESIAN_POINT('Ctrl Pts',(5.73937982550325,1.86051245417103,3.04629645861379));
#7063=CARTESIAN_POINT('Ctrl Pts',(5.7432925199416,1.87930521175744,3.11229828902138));
#7064=CARTESIAN_POINT('Ctrl Pts',(5.74720062162182,1.89807591022535,3.1782226458495));
#7065=CARTESIAN_POINT('Ctrl Pts',(5.75110872330204,1.91339477829522,3.24521031476398));
#7066=CARTESIAN_POINT('Ctrl Pts',(5.75501682498226,1.925151295957,3.31286720829584));
#7067=CARTESIAN_POINT('Ctrl Pts',(5.7589224826383,1.93690046140132,3.38048179098295));
#7068=CARTESIAN_POINT('Ctrl Pts',(5.76282814029434,1.94509161174389,3.4487642846754));
#7069=CARTESIAN_POINT('Ctrl Pts',(5.76673379795039,1.94966505701592,3.5173092444838));
#7070=CARTESIAN_POINT('Ctrl Pts',(5.77063835177014,1.95423720971821,3.58583483177652));
#7071=CARTESIAN_POINT('Ctrl Pts',(5.77454290558989,1.95519365441088,3.65462224750219));
#7072=CARTESIAN_POINT('Ctrl Pts',(5.77844745940964,1.9525266159011,3.72326155072272));
#7073=CARTESIAN_POINT('Ctrl Pts',(5.7823522479429,1.94985941706828,3.79190498004124));
#7074=CARTESIAN_POINT('Ctrl Pts',(5.78625703647617,1.94356832425448,3.86039978791119));
#7075=CARTESIAN_POINT('Ctrl Pts',(5.79016182500943,1.93369761352097,3.92833848310408));
#7076=CARTESIAN_POINT('Ctrl Pts',(5.79407076589633,1.92381640626984,3.99634942433178));
#7077=CARTESIAN_POINT('Ctrl Pts',(5.79797970678323,1.91034805528966,4.06380258514446));
#7078=CARTESIAN_POINT('Ctrl Pts',(5.80188864767013,1.8933882795822,4.13029903726282));
#7079=CARTESIAN_POINT('Ctrl Pts',(5.80579993028798,1.8764183437744,4.19683532544022));
#7080=CARTESIAN_POINT('Ctrl Pts',(5.80971121290583,1.85595296703639,4.26241329480045));
#7081=CARTESIAN_POINT('Ctrl Pts',(5.81362249552368,1.83213741818903,4.32665029701972));
#7082=CARTESIAN_POINT('Ctrl Pts',(5.81754050780242,1.80828089286843,4.39099782391425));
#7083=CARTESIAN_POINT('Ctrl Pts',(5.82145852008116,1.78106288604147,4.45399932770491));
#7084=CARTESIAN_POINT('Ctrl Pts',(5.82537653235989,1.75067597596596,4.51529401729611));
#7085=CARTESIAN_POINT('Ctrl Pts',(5.82719309395072,1.73658727746786,4.54371291211097));
#7086=CARTESIAN_POINT('Ctrl Pts',(5.82900965554154,1.7218180070699,4.5717652764579));
#7087=CARTESIAN_POINT('Ctrl Pts',(5.83082621713236,1.70639051229435,4.59941727239722));
#7088=CARTESIAN_POINT('Ctrl Pts',(5.8347449049416,1.67311031083597,4.65906817547481));
#7089=CARTESIAN_POINT('Ctrl Pts',(5.83866359275085,1.63663272637616,4.7170897663396));
#7090=CARTESIAN_POINT('Ctrl Pts',(5.84258228056009,1.59714186055191,4.7731181809562));
#7091=CARTESIAN_POINT('Ctrl Pts',(5.84649507869295,1.55771034837637,4.82906238645838));
#7092=CARTESIAN_POINT('Ctrl Pts',(5.85040787682581,1.51527482417692,4.88301896247133));
#7093=CARTESIAN_POINT('Ctrl Pts',(5.85432067495868,1.47006467497947,4.93464963000493));
#7094=CARTESIAN_POINT('Ctrl Pts',(5.85822888358509,1.42490755490964,4.98621973748052));
#7095=CARTESIAN_POINT('Ctrl Pts',(5.8621370922115,1.37698259577563,5.03546898652637));
#7096=CARTESIAN_POINT('Ctrl Pts',(5.86604530083791,1.32656067870888,5.08209052170544));
#7097=CARTESIAN_POINT('Ctrl Pts',(5.86995106738939,1.27617026817394,5.12868292505125));
#7098=CARTESIAN_POINT('Ctrl Pts',(5.87385683394088,1.2232863550066,5.17265053860784));
#7099=CARTESIAN_POINT('Ctrl Pts',(5.87776260049236,1.16821696380866,5.21372301794058));
#7100=CARTESIAN_POINT('Ctrl Pts',(5.88166726497468,1.11316311124502,5.25478390807245));
#7101=CARTESIAN_POINT('Ctrl Pts',(5.88557192945699,1.05592539883243,5.29295099187428));
#7102=CARTESIAN_POINT('Ctrl Pts',(5.88947659393931,0.996843822961791,5.32799507301508));
#7103=CARTESIAN_POINT('Ctrl Pts',(5.89338149472209,0.937758671622883,5.36304127493548));
#7104=CARTESIAN_POINT('Ctrl Pts',(5.89728639550488,0.876829859508901,5.39496385033934));
#7105=CARTESIAN_POINT('Ctrl Pts',(5.90119129628766,0.814423597314107,5.42357863782766));
#7106=CARTESIAN_POINT('Ctrl Pts',(5.90510035101687,0.751950948728358,5.4522238650892));
#7107=CARTESIAN_POINT('Ctrl Pts',(5.90900940574608,0.687998161327613,5.47755407684429));
#7108=CARTESIAN_POINT('Ctrl Pts',(5.91291846047529,0.62295219724466,5.49943295599088));
#7109=CARTESIAN_POINT('Ctrl Pts',(5.91682985800875,0.55786724932253,5.5213249477528));
#7110=CARTESIAN_POINT('Ctrl Pts',(5.92074125554221,0.491688294525717,5.53976135825004));
#7111=CARTESIAN_POINT('Ctrl Pts',(5.92465265307567,0.424815539002211,5.55465631654233));
#7112=CARTESIAN_POINT('Ctrl Pts',(5.92857078068969,0.35782771999363,5.56957690359475));
#7113=CARTESIAN_POINT('Ctrl Pts',(5.9324889083037,0.29014420234409,5.58094379549625));
#7114=CARTESIAN_POINT('Ctrl Pts',(5.93640703591772,0.222172536783606,5.58872271561845));
#7115=CARTESIAN_POINT('Ctrl Pts',(5.93822260984629,0.190675965964468,5.59232729565198));
#7116=CARTESIAN_POINT('Ctrl Pts',(5.94003818377486,0.159117552570715,5.59516220427779));
#7117=CARTESIAN_POINT('Ctrl Pts',(5.94185375770344,0.127537778503502,5.59722782399774));
#7118=CARTESIAN_POINT('Ctrl Pts',(5.94577148616542,0.0593934976570033,5.6016851127047));
#7119=CARTESIAN_POINT('Ctrl Pts',(5.94968921462741,-0.00911979872307073,
5.60257459642064));
#7120=CARTESIAN_POINT('Ctrl Pts',(5.9536069430894,-0.0775967852894685,5.59985310777223));
#7121=CARTESIAN_POINT('Ctrl Pts',(5.95751877860343,-0.145970770506587,5.59713571271813));
#7122=CARTESIAN_POINT('Ctrl Pts',(5.96143061411747,-0.214308066664483,5.59081814430949));
#7123=CARTESIAN_POINT('Ctrl Pts',(5.96534244963151,-0.282200215530251,5.58090915360557));
#7124=CARTESIAN_POINT('Ctrl Pts',(5.96924969548283,-0.350012708167429,5.5710117888826));
#7125=CARTESIAN_POINT('Ctrl Pts',(5.97315694133415,-0.417380606242612,5.55753144105242));
#7126=CARTESIAN_POINT('Ctrl Pts',(5.97706418718548,-0.483899283145357,5.54052876985136));
#7127=CARTESIAN_POINT('Ctrl Pts',(5.98096899142348,-0.550376392945782,5.52353672351245));
#7128=CARTESIAN_POINT('Ctrl Pts',(5.98487379566148,-0.616004858668716,5.50302684158917));
#7129=CARTESIAN_POINT('Ctrl Pts',(5.98877859989948,-0.680390524083188,5.47911080405691));
#7130=CARTESIAN_POINT('Ctrl Pts',(5.99268230397228,-0.744758049057379,5.45520150478615));
#7131=CARTESIAN_POINT('Ctrl Pts',(5.99658600804508,-0.807883007867782,5.42788812625633));
#7132=CARTESIAN_POINT('Ctrl Pts',(6.00048971211789,-0.869388420973091,5.39733154528919));
#7133=CARTESIAN_POINT('Ctrl Pts',(6.00439365583889,-0.930897609892601,5.36677308845508));
#7134=CARTESIAN_POINT('Ctrl Pts',(6.00829759955989,-0.990786616270124,5.3329712551077));
#7135=CARTESIAN_POINT('Ctrl Pts',(6.01220154328089,-1.04870203159526,5.29613339513917));
#7136=CARTESIAN_POINT('Ctrl Pts',(6.01610965249554,-1.10667924245652,5.25925622930892));
#7137=CARTESIAN_POINT('Ctrl Pts',(6.0200177617102,-1.16267824386887,5.21933683660942));
#7138=CARTESIAN_POINT('Ctrl Pts',(6.02392587092486,-1.21637452603557,5.17662597868762));
#7139=CARTESIAN_POINT('Ctrl Pts',(6.02783632816032,-1.27010306932417,5.13388945976774));
#7140=CARTESIAN_POINT('Ctrl Pts',(6.03174678539579,-1.32152577164834,5.08835846406956));
#7141=CARTESIAN_POINT('Ctrl Pts',(6.03565724263125,-1.37035328888209,5.04032227102529));
#7142=CARTESIAN_POINT('Ctrl Pts',(6.03957444778363,-1.41926506327798,4.99220318633436));
#7143=CARTESIAN_POINT('Ctrl Pts',(6.043491652936,-1.46557238303484,4.94157063931874));
#7144=CARTESIAN_POINT('Ctrl Pts',(6.04740885808838,-1.50902523794519,4.88874809688632));
#7145=CARTESIAN_POINT('Ctrl Pts',(6.04923300481709,-1.52926017077472,4.86414992951135));
#7146=CARTESIAN_POINT('Ctrl Pts',(6.0510571515458,-1.54887670810727,4.83907727941775));
#7147=CARTESIAN_POINT('Ctrl Pts',(6.05288129827451,-1.56785287850625,4.81356484664188));
#7148=CARTESIAN_POINT('Ctrl Pts',(6.05681837522051,-1.6088093661754,4.75850106841764));
#7149=CARTESIAN_POINT('Ctrl Pts',(6.06075545216651,-1.64694295803685,4.70116771866654));
#7150=CARTESIAN_POINT('Ctrl Pts',(6.06469252911251,-1.68199473772209,4.64188413754907));
#7151=CARTESIAN_POINT('Ctrl Pts',(6.06862362532713,-1.71699327098078,4.58269061288167));
#7152=CARTESIAN_POINT('Ctrl Pts',(6.07255472154176,-1.74891903684483,4.52155314947086));
#7153=CARTESIAN_POINT('Ctrl Pts',(6.07648581775639,-1.7775548481719,4.45882207549266));
#7154=CARTESIAN_POINT('Ctrl Pts',(6.080456191933,-1.80647677722476,4.39546421737978));
#7155=CARTESIAN_POINT('Ctrl Pts',(6.08442656610961,-1.83204232976782,4.33048112322188));
#7156=CARTESIAN_POINT('Ctrl Pts',(6.08839694028623,-1.85407425987925,4.26426126010623));
#7157=CARTESIAN_POINT('Ctrl Pts',(6.09231991040319,-1.87584314099758,4.1988320253299));
#7158=CARTESIAN_POINT('Ctrl Pts',(6.09624288052014,-1.89416217128946,4.13219586906046));
#7159=CARTESIAN_POINT('Ctrl Pts',(6.1001658506371,-1.9089086849858,4.06474759500726));
#7160=CARTESIAN_POINT('Ctrl Pts',(6.10415992684354,-1.92392248772367,3.99607678219701));
#7161=CARTESIAN_POINT('Ctrl Pts',(6.10815400304999,-1.93523279654417,3.92656460262322));
#7162=CARTESIAN_POINT('Ctrl Pts',(6.11214807925643,-1.94276391462491,3.85664162365595));
#7163=CARTESIAN_POINT('Ctrl Pts',(6.11614215546288,-1.95029503270565,3.78671864468868));
#7164=CARTESIAN_POINT('Ctrl Pts',(6.12013623166933,-1.95404689998987,3.71638539512174));
#7165=CARTESIAN_POINT('Ctrl Pts',(6.12413030787577,-1.95399955699113,3.64607868772758));
#7166=CARTESIAN_POINT('Origin',(0.,0.,3.64739446828387));
#7167=CARTESIAN_POINT('',(6.59995882699137,0.834037993952276,5.41445321791391));
#7168=CARTESIAN_POINT('Ctrl Pts',(6.12413030792735,-1.95399955699052,3.6460786868197));
#7169=CARTESIAN_POINT('Ctrl Pts',(6.128579472032,-1.95394681966027,3.56776118292618));
#7170=CARTESIAN_POINT('Ctrl Pts',(6.13302863613666,-1.9491815174852,3.48962762197139));
#7171=CARTESIAN_POINT('Ctrl Pts',(6.13747780024132,-1.93979384649703,3.41220128578861));
#7172=CARTESIAN_POINT('Ctrl Pts',(6.14196527052808,-1.93032535002662,3.33410832835666));
#7173=CARTESIAN_POINT('Ctrl Pts',(6.14645274081484,-1.91615465962242,3.25673503473373));
#7174=CARTESIAN_POINT('Ctrl Pts',(6.1509402111016,-1.89742413111203,3.18059936690237));
#7175=CARTESIAN_POINT('Ctrl Pts',(6.15526308701627,-1.87938061318493,3.10725625292429));
#7176=CARTESIAN_POINT('Ctrl Pts',(6.15958596293093,-1.85710603049991,3.03506166685608));
#7177=CARTESIAN_POINT('Ctrl Pts',(6.1639088388456,-1.83076925289313,2.96445966710507));
#7178=CARTESIAN_POINT('Ctrl Pts',(6.16782834248828,-1.80688998876341,2.90044561704503));
#7179=CARTESIAN_POINT('Ctrl Pts',(6.17174784613096,-1.7796022508274,2.83755952478642));
#7180=CARTESIAN_POINT('Ctrl Pts',(6.17566734977364,-1.74903318078112,2.77618902034024));
#7181=CARTESIAN_POINT('Ctrl Pts',(6.17958097555391,-1.71850995347519,2.7149105498387));
#7182=CARTESIAN_POINT('Ctrl Pts',(6.18349460133418,-1.68471537782724,2.65514359264594));
#7183=CARTESIAN_POINT('Ctrl Pts',(6.18740822711445,-1.64782522231827,2.59725731691185));
#7184=CARTESIAN_POINT('Ctrl Pts',(6.19131727661406,-1.61097820320371,2.5394387287542));
#7185=CARTESIAN_POINT('Ctrl Pts',(6.19522632611367,-1.5710430561003,2.48349686699584));
#7186=CARTESIAN_POINT('Ctrl Pts',(6.19913537561328,-1.52824131094062,2.42977609804857));
#7187=CARTESIAN_POINT('Ctrl Pts',(6.2030419907236,-1.48546622088209,2.37608878410468));
#7188=CARTESIAN_POINT('Ctrl Pts',(6.20694860583392,-1.43982837971601,2.32462020257689));
#7189=CARTESIAN_POINT('Ctrl Pts',(6.21085522094425,-1.39159154689863,2.27568423408706));
#7190=CARTESIAN_POINT('Ctrl Pts',(6.21476074031502,-1.34336824369806,2.22676199130979));
#7191=CARTESIAN_POINT('Ctrl Pts',(6.21866625968579,-1.29254774089066,2.18037130118336));
#7192=CARTESIAN_POINT('Ctrl Pts',(6.22257177905657,-1.23943161720214,2.13679019638481));
#7193=CARTESIAN_POINT('Ctrl Pts',(6.22647753970867,-1.1863122120221,2.09320639916415));
#7194=CARTESIAN_POINT('Ctrl Pts',(6.23038330036077,-1.13089728596084,2.05243284162797));
#7195=CARTESIAN_POINT('Ctrl Pts',(6.23428906101287,-1.07352113506549,2.01470699893534));
#7196=CARTESIAN_POINT('Ctrl Pts',(6.23819897711688,-1.01608394002089,1.97694101862568));
#7197=CARTESIAN_POINT('Ctrl Pts',(6.2421088932209,-0.956681767401127,1.94222949473819));
#7198=CARTESIAN_POINT('Ctrl Pts',(6.24601880932491,-0.895676657146052,1.91076574404726));
#7199=CARTESIAN_POINT('Ctrl Pts',(6.24993107033161,-0.834634960160559,1.87928312353117));
#7200=CARTESIAN_POINT('Ctrl Pts',(6.2538433313383,-0.771988860386667,1.8510523547138));
#7201=CARTESIAN_POINT('Ctrl Pts',(6.257755592345,-0.708121117161733,1.82621889096311));
#7202=CARTESIAN_POINT('Ctrl Pts',(6.26167457751989,-0.644143601749422,1.80134274488956));
#7203=CARTESIAN_POINT('Ctrl Pts',(6.26559356269479,-0.578940718830281,1.77987571125724));
#7204=CARTESIAN_POINT('Ctrl Pts',(6.26951254786969,-0.512910290448902,1.76191335356762));
#7205=CARTESIAN_POINT('Ctrl Pts',(6.27132049171868,-0.482448499574295,1.75362678634447));
#7206=CARTESIAN_POINT('Ctrl Pts',(6.27312843556768,-0.45181072436177,1.74608538440029));
#7207=CARTESIAN_POINT('Ctrl Pts',(6.27493637941667,-0.421036523795824,1.73929482580449));
#7208=CARTESIAN_POINT('Ctrl Pts',(6.27884955238992,-0.354427834596099,1.72459711802713));
#7209=CARTESIAN_POINT('Ctrl Pts',(6.28276272536317,-0.286914720102418,1.71336187894293));
#7210=CARTESIAN_POINT('Ctrl Pts',(6.28667589833642,-0.218890401956766,1.70569341201099));
#7211=CARTESIAN_POINT('Ctrl Pts',(6.29058316674399,-0.150968725339424,1.69803651598762));
#7212=CARTESIAN_POINT('Ctrl Pts',(6.29449043515156,-0.0825378619267242,
1.69393576663677));
#7213=CARTESIAN_POINT('Ctrl Pts',(6.29839770355913,-0.0140020575316097,
1.693444637202));
#7214=CARTESIAN_POINT('Ctrl Pts',(6.30230038694881,0.0544533229314145,1.6929540840873));
#7215=CARTESIAN_POINT('Ctrl Pts',(6.3062030703385,0.123012908974606,1.69606474292709));
#7216=CARTESIAN_POINT('Ctrl Pts',(6.31010575372818,0.191268328644095,1.70277820113559));
#7217=CARTESIAN_POINT('Ctrl Pts',(6.31400600085657,0.259481139672197,1.70948746844857));
#7218=CARTESIAN_POINT('Ctrl Pts',(6.31790624798496,0.327389671181229,1.7197950259574));
#7219=CARTESIAN_POINT('Ctrl Pts',(6.32180649511335,0.394588140713679,1.7336504417202));
#7220=CARTESIAN_POINT('Ctrl Pts',(6.3257056540783,0.461767861968184,1.7475019918416));
#7221=CARTESIAN_POINT('Ctrl Pts',(6.32960481304326,0.528237431631385,1.76489933579883));
#7222=CARTESIAN_POINT('Ctrl Pts',(6.33350397200822,0.593600579199207,1.78574080759014));
#7223=CARTESIAN_POINT('Ctrl Pts',(6.33740338928221,0.65896805690377,1.80658366007418));
#7224=CARTESIAN_POINT('Ctrl Pts',(6.3413028065562,0.723228497863452,1.83087094102834));
#7225=CARTESIAN_POINT('Ctrl Pts',(6.34520222383019,0.786001893430872,1.85845147771008));
#7226=CARTESIAN_POINT('Ctrl Pts',(6.34910586523305,0.848843289649043,1.88606189161013));
#7227=CARTESIAN_POINT('Ctrl Pts',(6.3530095066359,0.910193973351115,1.91697248177239));
#7228=CARTESIAN_POINT('Ctrl Pts',(6.35691314803876,0.969695934475873,1.9509847905642));
#7229=CARTESIAN_POINT('Ctrl Pts',(6.36081916424754,1.02923409401004,1.98501779096777));
#7230=CARTESIAN_POINT('Ctrl Pts',(6.36472518045632,1.08692087827308,2.02215599775593));
#7231=CARTESIAN_POINT('Ctrl Pts',(6.3686311966651,1.14242723508608,2.06215757351591));
#7232=CARTESIAN_POINT('Ctrl Pts',(6.37254404842718,1.19803072837793,2.10222915228889));
#7233=CARTESIAN_POINT('Ctrl Pts',(6.37645690018926,1.25144579487274,2.14517379158577));
#7234=CARTESIAN_POINT('Ctrl Pts',(6.38036975195135,1.30237711460555,2.1907099275024));
#7235=CARTESIAN_POINT('Ctrl Pts',(6.38223447463015,1.32664912712779,2.21241079186211));
#7236=CARTESIAN_POINT('Ctrl Pts',(6.38409919730895,1.35035760118791,2.23469968813216));
#7237=CARTESIAN_POINT('Ctrl Pts',(6.38596391998775,1.37347374173203,2.25754344001767));
#7238=CARTESIAN_POINT('Ctrl Pts',(6.38988983122375,1.42214152323476,2.30563774552445));
#7239=CARTESIAN_POINT('Ctrl Pts',(6.39381574245974,1.46837481356246,2.35638495257544));
#7240=CARTESIAN_POINT('Ctrl Pts',(6.39774165369574,1.5118716955992,2.40950918440414));
#7241=CARTESIAN_POINT('Ctrl Pts',(6.401661650329,1.55530304717378,2.46255338163494));
#7242=CARTESIAN_POINT('Ctrl Pts',(6.40558164696225,1.59600586540517,2.51796711955856));
#7243=CARTESIAN_POINT('Ctrl Pts',(6.40950164359551,1.63371504486074,2.57543777503752));
#7244=CARTESIAN_POINT('Ctrl Pts',(6.4134169792512,1.67137938712486,2.63284009641798));
#7245=CARTESIAN_POINT('Ctrl Pts',(6.41733231490688,1.70605689353566,2.69229406976241));
#7246=CARTESIAN_POINT('Ctrl Pts',(6.42124765056257,1.73752386585782,2.75345553548449));
#7247=CARTESIAN_POINT('Ctrl Pts',(6.42516049537214,1.76897081961895,2.81457809169465));
#7248=CARTESIAN_POINT('Ctrl Pts',(6.42907334018171,1.79721106794486,2.87740555063087));
#7249=CARTESIAN_POINT('Ctrl Pts',(6.43298618499128,1.82206603382117,2.94156774139178));
#7250=CARTESIAN_POINT('Ctrl Pts',(6.4368978684084,1.84691362236174,3.00571088782872));
#7251=CARTESIAN_POINT('Ctrl Pts',(6.44080955182551,1.86837774659701,3.07118752305999));
#7252=CARTESIAN_POINT('Ctrl Pts',(6.44472123524263,1.8863280242434,3.1376076648513));
#7253=CARTESIAN_POINT('Ctrl Pts',(6.44863308502627,1.90427906532715,3.20403063153584));
#7254=CARTESIAN_POINT('Ctrl Pts',(6.45254493480991,1.91871583776211,3.27139671099779));
#7255=CARTESIAN_POINT('Ctrl Pts',(6.45645678459355,1.92955835474801,3.33930267088875));
#7256=CARTESIAN_POINT('Ctrl Pts',(6.46037263616518,1.94041196353361,3.4072780979806));
#7257=CARTESIAN_POINT('Ctrl Pts',(6.46428848773681,1.94766390122192,3.47579402321336));
#7258=CARTESIAN_POINT('Ctrl Pts',(6.46820433930844,1.95128582531456,3.54443997383857));
#7259=CARTESIAN_POINT('Ctrl Pts',(6.47212245625163,1.95490984473785,3.61312563704775));
#7260=CARTESIAN_POINT('Ctrl Pts',(6.47604057319482,1.95489967004011,3.68194098549061));
#7261=CARTESIAN_POINT('Ctrl Pts',(6.47995869013801,1.95127910870616,3.75047618308761));
#7262=CARTESIAN_POINT('Ctrl Pts',(6.4838833491557,1.94765250212592,3.81912581381023));
#7263=CARTESIAN_POINT('Ctrl Pts',(6.48780800817339,1.94040352839184,3.88749387319098));
#7264=CARTESIAN_POINT('Ctrl Pts',(6.49173266719108,1.92960768452088,3.95517715759239));
#7265=CARTESIAN_POINT('Ctrl Pts',(6.49348559831366,1.92478576989576,3.98540758912064));
#7266=CARTESIAN_POINT('Ctrl Pts',(6.49523852943624,1.91925696002775,4.01550157306795));
#7267=CARTESIAN_POINT('Ctrl Pts',(6.49699146055883,1.91303120504268,4.04542412613984));
#7268=CARTESIAN_POINT('Ctrl Pts',(6.5008727175178,1.89924643361079,4.1116772240764));
#7269=CARTESIAN_POINT('Ctrl Pts',(6.50475397447678,1.88198628894892,4.17735458711251));
#7270=CARTESIAN_POINT('Ctrl Pts',(6.50863523143576,1.86131381314335,4.24205982712173));
#7271=CARTESIAN_POINT('Ctrl Pts',(6.51250998753633,1.84067596241917,4.30665668997175));
#7272=CARTESIAN_POINT('Ctrl Pts',(6.5163847436369,1.81663727951453,4.37028418844698));
#7273=CARTESIAN_POINT('Ctrl Pts',(6.52025949973747,1.78931167938922,4.43255668973963));
#7274=CARTESIAN_POINT('Ctrl Pts',(6.52413063354277,1.76201162445679,4.49477097591349));
#7275=CARTESIAN_POINT('Ctrl Pts',(6.52800176734808,1.73143094295279,4.55563231808264));
#7276=CARTESIAN_POINT('Ctrl Pts',(6.53187290115338,1.69773268329177,4.61477223114744));
#7277=CARTESIAN_POINT('Ctrl Pts',(6.53574180537595,1.66405383217141,4.67387808253015));
#7278=CARTESIAN_POINT('Ctrl Pts',(6.53961070959852,1.62726121136194,4.73126403542489));
#7279=CARTESIAN_POINT('Ctrl Pts',(6.5434796138211,1.58756426082805,4.78658528537357));
#7280=CARTESIAN_POINT('Ctrl Pts',(6.54734767812641,1.54787592827793,4.84189452539132));
#7281=CARTESIAN_POINT('Ctrl Pts',(6.55121574243173,1.50528481066992,4.89513954481636));
#7282=CARTESIAN_POINT('Ctrl Pts',(6.55508380673704,1.46004311123211,4.94600530812145));
#7283=CARTESIAN_POINT('Ctrl Pts',(6.55895498853783,1.41476494890696,4.99691206707039));
#7284=CARTESIAN_POINT('Ctrl Pts',(6.56282617033861,1.36683226981965,5.04543536161557));
#7285=CARTESIAN_POINT('Ctrl Pts',(6.56669735213939,1.31653618878333,5.09129490239415));
#7286=CARTESIAN_POINT('Ctrl Pts',(6.57057001435284,1.26622087358051,5.13717198072287));
#7287=CARTESIAN_POINT('Ctrl Pts',(6.57444267656629,1.21354074412186,5.18038295628716));
#7288=CARTESIAN_POINT('Ctrl Pts',(6.57831533877974,1.15882003527172,5.22068786935464));
#7289=CARTESIAN_POINT('Ctrl Pts',(6.58219473815397,1.10400413035407,5.26106289973798));
#7290=CARTESIAN_POINT('Ctrl Pts',(6.58607413752819,1.04714097458828,5.29852149120506));
#7291=CARTESIAN_POINT('Ctrl Pts',(6.58995353690242,0.988583156110744,5.33286750083412));
#7292=CARTESIAN_POINT('Ctrl Pts',(6.59328863359874,0.938241345920918,5.36239456216389));
#7293=CARTESIAN_POINT('Ctrl Pts',(6.59662373029505,0.88664765834881,5.38962186526931));
#7294=CARTESIAN_POINT('Ctrl Pts',(6.59995882699137,0.834037993952276,5.41445321791391));
#7295=CARTESIAN_POINT('',(6.6,1.90834530359594,4.06731613031539));
#7296=CARTESIAN_POINT('Origin',(6.6,0.,3.64739446828387));
#7297=CARTESIAN_POINT('Ctrl Pts',(6.6,1.90834530359594,4.06731613031539));
#7298=CARTESIAN_POINT('Ctrl Pts',(6.56299081980964,2.04784060254395,3.43337598697229));
#7299=CARTESIAN_POINT('Ctrl Pts',(6.48897245942892,1.64305422583221,2.02647090284419));
#7300=CARTESIAN_POINT('Ctrl Pts',(6.37794491885784,-0.472540916100214,1.38598473075093));
#7301=CARTESIAN_POINT('Ctrl Pts',(6.29024427840894,-1.80025717638368,2.51599492455183));
#7302=CARTESIAN_POINT('Ctrl Pts',(6.2395528181504,-1.9529603584434,3.4057264198301));
#7303=CARTESIAN_POINT('Ctrl Pts',(6.22587053808222,-1.95156756343269,3.64631438782879));
#7304=CARTESIAN_POINT('Origin',(1.2059437743963,0.,3.64739446828387));
#7305=CARTESIAN_POINT('',(6.599956144719,-0.42654248155568,2.15151955324975));
#7306=CARTESIAN_POINT('Ctrl Pts',(6.4559437743963,-1.5554997682929,3.6465454448856));
#7307=CARTESIAN_POINT('Ctrl Pts',(6.46061116422838,-1.55546406369716,3.58113088679472));
#7308=CARTESIAN_POINT('Ctrl Pts',(6.46527855406046,-1.55129786300922,3.51586849460407));
#7309=CARTESIAN_POINT('Ctrl Pts',(6.46994594389254,-1.54308295192937,3.45124336972736));
#7310=CARTESIAN_POINT('Ctrl Pts',(6.47464971063311,-1.53480401511366,3.38611456670539));
#7311=CARTESIAN_POINT('Ctrl Pts',(6.47935347737368,-1.52241313274287,3.32163325345467));
#7312=CARTESIAN_POINT('Ctrl Pts',(6.48405724411425,-1.50604397351761,3.25827777649169));
#7313=CARTESIAN_POINT('Ctrl Pts',(6.48836864959578,-1.4910402357253,3.20020705025716));
#7314=CARTESIAN_POINT('Ctrl Pts',(6.49268005507731,-1.47269489336211,3.14308208717692));
#7315=CARTESIAN_POINT('Ctrl Pts',(6.49699146055883,-1.45114591966537,3.0872554053374));
#7316=CARTESIAN_POINT('Ctrl Pts',(6.50128165573217,-1.42970295788867,3.03170336737719));
#7317=CARTESIAN_POINT('Ctrl Pts',(6.50557185090551,-1.40501473944522,2.97725350914402));
#7318=CARTESIAN_POINT('Ctrl Pts',(6.50986204607885,-1.37722024457809,2.92431449488931));
#7319=CARTESIAN_POINT('Ctrl Pts',(6.51396372832576,-1.35064705115635,2.87370164252155));
#7320=CARTESIAN_POINT('Ctrl Pts',(6.51806541057266,-1.32123511808883,2.8244701800106));
#7321=CARTESIAN_POINT('Ctrl Pts',(6.52216709281957,-1.28915582586842,2.77695922851613));
#7322=CARTESIAN_POINT('Ctrl Pts',(6.52626492593395,-1.25710663774667,2.72949286261793));
#7323=CARTESIAN_POINT('Ctrl Pts',(6.53036275904833,-1.22239534318046,2.68374424903125));
#7324=CARTESIAN_POINT('Ctrl Pts',(6.53446059216271,-1.18523844654547,2.64002657380317));
#7325=CARTESIAN_POINT('Ctrl Pts',(6.53855622804132,-1.14810147323584,2.59633233975415));
#7326=CARTESIAN_POINT('Ctrl Pts',(6.54265186391993,-1.10852184009623,2.55466729042924));
#7327=CARTESIAN_POINT('Ctrl Pts',(6.54674749979854,-1.06675701342171,2.51531243754776));
#7328=CARTESIAN_POINT('Ctrl Pts',(6.55084258685509,-1.02499778330378,2.47596285828235));
#7329=CARTESIAN_POINT('Ctrl Pts',(6.55493767391165,-0.981054328890206,2.4389232239911));
#7330=CARTESIAN_POINT('Ctrl Pts',(6.5590327609682,-0.935220039280021,2.40443681489053));
#7331=CARTESIAN_POINT('Ctrl Pts',(6.56313151800817,-0.889344673355695,2.36991949935319));
#7332=CARTESIAN_POINT('Ctrl Pts',(6.56723027504813,-0.841575516606041,2.33796029461034));
#7333=CARTESIAN_POINT('Ctrl Pts',(6.57132903208809,-0.792236695122554,2.30876036259954));
#7334=CARTESIAN_POINT('Ctrl Pts',(6.57542996437529,-0.74287168908268,2.27954493392215));
#7335=CARTESIAN_POINT('Ctrl Pts',(6.57953089666248,-0.691935833065455,2.25309193575008));
#7336=CARTESIAN_POINT('Ctrl Pts',(6.58363182894968,-0.639776841899525,2.22955602806261));
#7337=CARTESIAN_POINT('Ctrl Pts',(6.58773952212041,-0.587531860319731,2.20598131858089));
#7338=CARTESIAN_POINT('Ctrl Pts',(6.59184721529114,-0.534060217488819,2.18533348088132));
#7339=CARTESIAN_POINT('Ctrl Pts',(6.59595490846187,-0.479727038099651,2.16771807835392));
#7340=CARTESIAN_POINT('Ctrl Pts',(6.59728865388091,-0.46208535307097,2.1619984538715));
#7341=CARTESIAN_POINT('Ctrl Pts',(6.59862239929996,-0.444352929777357,2.15659812813977));
#7342=CARTESIAN_POINT('Ctrl Pts',(6.599956144719,-0.42654248155568,2.15151955324975));
#7343=CARTESIAN_POINT('',(6.6,-1.55328677638795,3.5644460487792));
#7344=CARTESIAN_POINT('Origin',(6.6,0.,3.64739446828387));
#7345=CARTESIAN_POINT('Ctrl Pts',(6.59414638614667,-1.55549999987963,3.64737511703584));
#7346=CARTESIAN_POINT('Ctrl Pts',(6.59510874546272,-1.55549982783689,3.63354590681215));
#7347=CARTESIAN_POINT('Ctrl Pts',(6.59607695453386,-1.55531523240308,3.61971776272618));
#7348=CARTESIAN_POINT('Ctrl Pts',(6.59802745792117,-1.5545773647494,3.59207096791355));
#7349=CARTESIAN_POINT('Ctrl Pts',(6.59900966026663,-1.55402412717383,3.5782536322402));
#7350=CARTESIAN_POINT('Ctrl Pts',(6.6,-1.55328677638795,3.5644460487792));
#7351=CARTESIAN_POINT('Ctrl Pts',(2.26863408412604,-0.684651324693825,5.04165517356951));
#7352=CARTESIAN_POINT('Ctrl Pts',(2.30564859368349,-1.14788625211098,4.81419027525137));
#7353=CARTESIAN_POINT('Ctrl Pts',(2.3796722834313,-1.8217797641733,3.86524735393602));
#7354=CARTESIAN_POINT('Ctrl Pts',(2.49070515336946,-1.17126252580745,2.23289142025749));
#7355=CARTESIAN_POINT('Ctrl Pts',(2.60173269394054,0.550929011373164,1.8972621249236));
#7356=CARTESIAN_POINT('Ctrl Pts',(2.71276023451162,1.76895437683424,3.15850697088285));
#7357=CARTESIAN_POINT('Ctrl Pts',(2.8237877750827,1.37119925940374,4.86751886652752));
#7358=CARTESIAN_POINT('Ctrl Pts',(2.93481531565378,-0.279566957660275,5.46119858728686));
#7359=CARTESIAN_POINT('Ctrl Pts',(3.04584285622486,-1.67479408727594,4.3979960058981));
#7360=CARTESIAN_POINT('Ctrl Pts',(3.15687039679593,-1.53990869075139,2.64885471465201));
#7361=CARTESIAN_POINT('Ctrl Pts',(3.26789793736702,0.00194110293598171,
1.81210655462338));
#7362=CARTESIAN_POINT('Ctrl Pts',(3.37892547793808,1.5420014927779,2.65212320530051));
#7363=CARTESIAN_POINT('Ctrl Pts',(3.48995301850917,1.67322430909778,4.40148852237912));
#7364=CARTESIAN_POINT('Ctrl Pts',(3.60098055908024,0.275705577370855,5.46186647902077));
#7365=CARTESIAN_POINT('Ctrl Pts',(3.71200809965133,-1.37370863799142,4.86446239222593));
#7366=CARTESIAN_POINT('Ctrl Pts',(3.8230356402224,-1.76803851820383,3.15508418544703));
#7367=CARTESIAN_POINT('Ctrl Pts',(3.93406318079349,-0.547003778353853,1.89550562214907));
#7368=CARTESIAN_POINT('Ctrl Pts',(4.04509072136456,1.17379929443624,2.23653514832174));
#7369=CARTESIAN_POINT('Ctrl Pts',(4.15611826193565,1.8221637133016,3.86659322783984));
#7370=CARTESIAN_POINT('Ctrl Pts',(4.26714580250671,0.805712675430428,5.29638067585463));
#7371=CARTESIAN_POINT('Ctrl Pts',(4.3781733430778,-0.946875698946845,5.2195760848642));
#7372=CARTESIAN_POINT('Ctrl Pts',(4.48920088364887,-1.83435347884445,3.70635156641869));
#7373=CARTESIAN_POINT('Ctrl Pts',(4.60022842421995,-1.04587869061767,2.13926112118895));
#7374=CARTESIAN_POINT('Ctrl Pts',(4.71125596479103,0.698160489741094,1.95007286504292));
#7375=CARTESIAN_POINT('Ctrl Pts',(4.82228350536211,1.80432722111991,3.31163848029748));
#7376=CARTESIAN_POINT('Ctrl Pts',(4.93331104593319,1.26197456066074,4.97996636915454));
#7377=CARTESIAN_POINT('Ctrl Pts',(5.04433858650427,-0.433377472991919,5.43079391382108));
#7378=CARTESIAN_POINT('Ctrl Pts',(5.15536612707534,-1.73277632833419,4.25222167463752));
#7379=CARTESIAN_POINT('Ctrl Pts',(5.26639366764643,-1.44902630832145,2.521053045387));
#7380=CARTESIAN_POINT('Ctrl Pts',(5.3774212082175,0.158619024761312,1.81895867888319));
#7381=CARTESIAN_POINT('Ctrl Pts',(5.48844874878859,1.6213501498084,2.7874193626174));
#7382=CARTESIAN_POINT('Ctrl Pts',(5.59947628935966,1.60272396252789,4.54157643737503));
#7383=CARTESIAN_POINT('Ctrl Pts',(5.71050382993074,0.119801397977272,5.4788004965795));
#7384=CARTESIAN_POINT('Ctrl Pts',(5.82153137050182,-1.47263207300637,4.74269930283736));
#7385=CARTESIAN_POINT('Ctrl Pts',(5.9325589110729,-1.71949372363033,3.00600192052272));
#7386=CARTESIAN_POINT('Ctrl Pts',(6.04358645164398,-0.395546584890944,1.8550680874704));
#7387=CARTESIAN_POINT('Ctrl Pts',(6.15461399221506,1.29018035693896,2.34215685811287));
#7388=CARTESIAN_POINT('Ctrl Pts',(6.26564153278613,1.79638565259649,4.02087081558556));
#7389=CARTESIAN_POINT('Ctrl Pts',(6.37666907335722,0.662790583736323,5.36010676734267));
#7390=CARTESIAN_POINT('Ctrl Pts',(6.48769661392829,-1.07933315373079,5.13104989888334));
#7391=CARTESIAN_POINT('Ctrl Pts',(6.56171497430901,-1.57859588144958,4.07982280745059));
#7392=CARTESIAN_POINT('Ctrl Pts',(6.59872415449937,-1.55108009138598,3.56456388988623));
#7393=CARTESIAN_POINT('Ctrl Pts',(2.34623717873851,-0.743896982560043,5.1623062111741));
#7394=CARTESIAN_POINT('Ctrl Pts',(2.38325168829595,-1.24721750834176,4.91515785201061));
#7395=CARTESIAN_POINT('Ctrl Pts',(2.45727537804376,-1.9794257610814,3.88409904831387));
#7396=CARTESIAN_POINT('Ctrl Pts',(2.56830824798192,-1.27261662587662,2.11048873057953));
#7397=CARTESIAN_POINT('Ctrl Pts',(2.67933578855301,0.598603134739513,1.74581607012819));
#7398=CARTESIAN_POINT('Ctrl Pts',(2.79036332912407,1.92202917857765,3.11620155152352));
#7399=CARTESIAN_POINT('Ctrl Pts',(2.90139086969516,1.48985469649849,4.97310118273044));
#7400=CARTESIAN_POINT('Ctrl Pts',(3.01241841026624,-0.30375902116303,5.61815441924826));
#7401=CARTESIAN_POINT('Ctrl Pts',(3.12344595083731,-1.81972081700291,4.46294860335526));
#7402=CARTESIAN_POINT('Ctrl Pts',(3.23447349140839,-1.67316323966835,2.56244701707551));
#7403=CARTESIAN_POINT('Ctrl Pts',(3.34550103197947,0.00210907445123311,
1.65329164271569));
#7404=CARTESIAN_POINT('Ctrl Pts',(3.45652857255054,1.6754371403481,2.5659983434854));
#7405=CARTESIAN_POINT('Ctrl Pts',(3.56755611312163,1.81801519954786,4.46674334146218));
#7406=CARTESIAN_POINT('Ctrl Pts',(3.6785836536927,0.29956349996529,5.61888010636462));
#7407=CARTESIAN_POINT('Ctrl Pts',(3.7896111942638,-1.49258122179998,4.96978021930246));
#7408=CARTESIAN_POINT('Ctrl Pts',(3.90063873483486,-1.92103406698283,3.11248257857215));
#7409=CARTESIAN_POINT('Ctrl Pts',(4.01166627540594,-0.594338235376009,1.74390757003961));
#7410=CARTESIAN_POINT('Ctrl Pts',(4.12269381597701,1.27537291139066,2.11444776522171));
#7411=CARTESIAN_POINT('Ctrl Pts',(4.2337213565481,1.97984293488607,3.88556138614897));
#7412=CARTESIAN_POINT('Ctrl Pts',(4.34474889711917,0.875434263318063,5.43907414500631));
#7413=CARTESIAN_POINT('Ctrl Pts',(4.45577643769026,-1.02881269618661,5.35562334103673));
#7414=CARTESIAN_POINT('Ctrl Pts',(4.56680397826132,-1.99308753031499,3.71145336340483));
#7415=CARTESIAN_POINT('Ctrl Pts',(4.67783151883243,-1.13638281854237,2.00875622172268));
#7416=CARTESIAN_POINT('Ctrl Pts',(4.78885905940349,0.758575150487437,1.80319673792884));
#7417=CARTESIAN_POINT('Ctrl Pts',(4.89988659997458,1.96046297864434,3.28258415195061));
#7418=CARTESIAN_POINT('Ctrl Pts',(5.01091414054565,1.37117834127157,5.0952792241416));
#7419=CARTESIAN_POINT('Ctrl Pts',(5.12194168111672,-0.470879384644958,5.58511870598642));
#7420=CARTESIAN_POINT('Ctrl Pts',(5.2329692216878,-1.88272049670789,4.30455982756789));
#7421=CARTESIAN_POINT('Ctrl Pts',(5.34399676225889,-1.57441643582957,2.42358615067044));
#7422=CARTESIAN_POINT('Ctrl Pts',(5.45502430282995,0.172344972748461,1.66073670909787));
#7423=CARTESIAN_POINT('Ctrl Pts',(5.56605184340105,1.76165215871761,2.7130022264108));
#7424=CARTESIAN_POINT('Ctrl Pts',(5.67707938397211,1.74141417185507,4.61895363230649));
#7425=CARTESIAN_POINT('Ctrl Pts',(5.78810692454321,0.130168299172756,5.63727949319146));
#7426=CARTESIAN_POINT('Ctrl Pts',(5.89913446511428,-1.60006490313954,4.83748047559882));
#7427=CARTESIAN_POINT('Ctrl Pts',(6.01016200568536,-1.86828849430995,2.95049962019548));
#7428=CARTESIAN_POINT('Ctrl Pts',(6.12118954625643,-0.429774836255362,1.69997081136455));
#7429=CARTESIAN_POINT('Ctrl Pts',(6.23221708682751,1.40182489957839,2.22920935023958));
#7430=CARTESIAN_POINT('Ctrl Pts',(6.34324462739859,1.95183419396477,4.05318923971664));
#7431=CARTESIAN_POINT('Ctrl Pts',(6.45427216796967,0.720144542963021,5.50831471383087));
#7432=CARTESIAN_POINT('Ctrl Pts',(6.56529970854074,-1.17273223212766,5.25943662488868));
#7433=CARTESIAN_POINT('Ctrl Pts',(6.63931806892146,-1.7151981899943,4.11724258670156));
#7434=CARTESIAN_POINT('Ctrl Pts',(6.67632724911182,-1.68530134694034,3.55739622375953));
#7435=CARTESIAN_POINT('Ctrl Pts',(2.42384027335096,-0.803142640426261,5.28295724877869));
#7436=CARTESIAN_POINT('Ctrl Pts',(2.46085478290841,-1.34654876457254,5.01612542876985));
#7437=CARTESIAN_POINT('Ctrl Pts',(2.53487847265621,-2.1370717579895,3.90295074269172));
#7438=CARTESIAN_POINT('Ctrl Pts',(2.64591134259438,-1.3739707259458,1.98808604090159));
#7439=CARTESIAN_POINT('Ctrl Pts',(2.75693888316546,0.646277258105862,1.59437001533278));
#7440=CARTESIAN_POINT('Ctrl Pts',(2.86796642373654,2.07510398032106,3.07389613216417));
#7441=CARTESIAN_POINT('Ctrl Pts',(2.97899396430762,1.60851013359324,5.07868349893336));
#7442=CARTESIAN_POINT('Ctrl Pts',(3.09002150487869,-0.327951084665789,5.77511025120965));
#7443=CARTESIAN_POINT('Ctrl Pts',(3.20104904544978,-1.96464754672989,4.52790120081243));
#7444=CARTESIAN_POINT('Ctrl Pts',(3.31207658602085,-1.80641778858531,2.47603931949901));
#7445=CARTESIAN_POINT('Ctrl Pts',(3.42310412659193,0.00227704596648382,
1.494476730808));
#7446=CARTESIAN_POINT('Ctrl Pts',(3.53413166716301,1.8088727879183,2.47987348167028));
#7447=CARTESIAN_POINT('Ctrl Pts',(3.64515920773409,1.96280608999794,4.53199816054524));
#7448=CARTESIAN_POINT('Ctrl Pts',(3.75618674830517,0.323421422559726,5.77589373370847));
#7449=CARTESIAN_POINT('Ctrl Pts',(3.86721428887625,-1.61145380560854,5.07509804637899));
#7450=CARTESIAN_POINT('Ctrl Pts',(3.97824182944732,-2.07402961576183,3.06988097169728));
#7451=CARTESIAN_POINT('Ctrl Pts',(4.08926937001841,-0.641672692398164,1.59230951793014));
#7452=CARTESIAN_POINT('Ctrl Pts',(4.20029691058948,1.37694652834506,1.99236038212167));
#7453=CARTESIAN_POINT('Ctrl Pts',(4.31132445116056,2.13752215647056,3.90452954445811));
#7454=CARTESIAN_POINT('Ctrl Pts',(4.42235199173164,0.9451558512057,5.58176761415798));
#7455=CARTESIAN_POINT('Ctrl Pts',(4.53337953230272,-1.11074969342638,5.49167059720925));
#7456=CARTESIAN_POINT('Ctrl Pts',(4.64440707287379,-2.15182158178555,3.71655516039097));
#7457=CARTESIAN_POINT('Ctrl Pts',(4.75543461344488,-1.22688694646707,1.8782513222564));
#7458=CARTESIAN_POINT('Ctrl Pts',(4.86646215401595,0.818989811233778,1.65632061081476));
#7459=CARTESIAN_POINT('Ctrl Pts',(4.97748969458703,2.11659873616878,3.25352982360373));
#7460=CARTESIAN_POINT('Ctrl Pts',(5.08851723515811,1.48038212188239,5.21059207912866));
#7461=CARTESIAN_POINT('Ctrl Pts',(5.19954477572919,-0.508381296297998,5.73944349815176));
#7462=CARTESIAN_POINT('Ctrl Pts',(5.31057231630027,-2.0326646650816,4.35689798049827));
#7463=CARTESIAN_POINT('Ctrl Pts',(5.42159985687135,-1.69980656333768,2.32611925595385));
#7464=CARTESIAN_POINT('Ctrl Pts',(5.53262739744242,0.186070920735613,1.50251473931255));
#7465=CARTESIAN_POINT('Ctrl Pts',(5.64365493801351,1.90195416762681,2.63858509020417));
#7466=CARTESIAN_POINT('Ctrl Pts',(5.75468247858458,1.88010438118225,4.69633082723795));
#7467=CARTESIAN_POINT('Ctrl Pts',(5.86571001915567,0.140535200368236,5.79575848980343));
#7468=CARTESIAN_POINT('Ctrl Pts',(5.97673755972673,-1.72749773327271,4.9322616483603));
#7469=CARTESIAN_POINT('Ctrl Pts',(6.08776510029783,-2.01708326498956,2.89499731986824));
#7470=CARTESIAN_POINT('Ctrl Pts',(6.19879264086889,-0.464003087619777,1.54487353525871));
#7471=CARTESIAN_POINT('Ctrl Pts',(6.30982018143998,1.51346944221782,2.1162618423663));
#7472=CARTESIAN_POINT('Ctrl Pts',(6.42084772201105,2.10728273533306,4.08550766384771));
#7473=CARTESIAN_POINT('Ctrl Pts',(6.53187526258214,0.777498502189718,5.65652266031908));
#7474=CARTESIAN_POINT('Ctrl Pts',(6.64290280315321,-1.26613131052453,5.38782335089402));
#7475=CARTESIAN_POINT('Ctrl Pts',(6.71692116353393,-1.85180049853903,4.15466236595253));
#7476=CARTESIAN_POINT('Ctrl Pts',(6.75393034372429,-1.81952260249468,3.55022855763283));
#7477=CARTESIAN_POINT('Ctrl Pts',(2.50144336796343,-0.862388298292479,5.40360828638327));
#7478=CARTESIAN_POINT('Ctrl Pts',(2.53845787752087,-1.44588002080332,5.11709300552908));
#7479=CARTESIAN_POINT('Ctrl Pts',(2.61248156726868,-2.29471775489761,3.92180243706957));
#7480=CARTESIAN_POINT('Ctrl Pts',(2.72351443720684,-1.47532482601497,1.86568335122363));
#7481=CARTESIAN_POINT('Ctrl Pts',(2.83454197777792,0.69395138147221,1.44292396053739));
#7482=CARTESIAN_POINT('Ctrl Pts',(2.945569518349,2.22817878206446,3.03159071280484));
#7483=CARTESIAN_POINT('Ctrl Pts',(3.05659705892007,1.72716557068799,5.18426581513628));
#7484=CARTESIAN_POINT('Ctrl Pts',(3.16762459949115,-0.352143148168544,5.93206608317104));
#7485=CARTESIAN_POINT('Ctrl Pts',(3.27865214006223,-2.10957427645686,4.5928537982696));
#7486=CARTESIAN_POINT('Ctrl Pts',(3.38967968063331,-1.93967233750227,2.38963162192252));
#7487=CARTESIAN_POINT('Ctrl Pts',(3.50070722120439,0.00244501748173489,
1.33566181890031));
#7488=CARTESIAN_POINT('Ctrl Pts',(3.61173476177546,1.94230843548851,2.39374861985516));
#7489=CARTESIAN_POINT('Ctrl Pts',(3.72276230234655,2.10759698044802,4.59725297962832));
#7490=CARTESIAN_POINT('Ctrl Pts',(3.83378984291762,0.34727934515416,5.93290736105231));
#7491=CARTESIAN_POINT('Ctrl Pts',(3.9448173834887,-1.73032638941711,5.18041587345552));
#7492=CARTESIAN_POINT('Ctrl Pts',(4.05584492405978,-2.22702516454082,3.0272793648224));
#7493=CARTESIAN_POINT('Ctrl Pts',(4.16687246463086,-0.689007149420319,1.44071146582068));
#7494=CARTESIAN_POINT('Ctrl Pts',(4.27790000520194,1.47852014529947,1.87027299902164));
#7495=CARTESIAN_POINT('Ctrl Pts',(4.38892754577301,2.29520137805504,3.92349770276724));
#7496=CARTESIAN_POINT('Ctrl Pts',(4.4999550863441,1.01487743909333,5.72446108330965));
#7497=CARTESIAN_POINT('Ctrl Pts',(4.61098262691517,-1.19268669066615,5.62771785338177));
#7498=CARTESIAN_POINT('Ctrl Pts',(4.72201016748625,-2.31055563325609,3.72165695737712));
#7499=CARTESIAN_POINT('Ctrl Pts',(4.83303770805733,-1.31739107439176,1.74774642279012));
#7500=CARTESIAN_POINT('Ctrl Pts',(4.94406524862841,0.879404471980121,1.50944448370068));
#7501=CARTESIAN_POINT('Ctrl Pts',(5.05509278919948,2.2727344936932,3.22447549525686));
#7502=CARTESIAN_POINT('Ctrl Pts',(5.16612032977057,1.58958590249323,5.32590493411573));
#7503=CARTESIAN_POINT('Ctrl Pts',(5.27714787034164,-0.545883207951038,5.89376829031711));
#7504=CARTESIAN_POINT('Ctrl Pts',(5.38817541091273,-2.1826088334553,4.40923613342865));
#7505=CARTESIAN_POINT('Ctrl Pts',(5.4992029514838,-1.82519669084581,2.22865236123728));
#7506=CARTESIAN_POINT('Ctrl Pts',(5.61023049205488,0.199796868722764,1.34429276952724));
#7507=CARTESIAN_POINT('Ctrl Pts',(5.72125803262597,2.042256176536,2.56416795399757));
#7508=CARTESIAN_POINT('Ctrl Pts',(5.83228557319703,2.01879459050943,4.77370802216941));
#7509=CARTESIAN_POINT('Ctrl Pts',(5.94331311376813,0.150902101563718,5.95423748641541));
#7510=CARTESIAN_POINT('Ctrl Pts',(6.05434065433919,-1.85493056340588,5.02704282112175));
#7511=CARTESIAN_POINT('Ctrl Pts',(6.16536819491027,-2.16587803566918,2.83949501954101));
#7512=CARTESIAN_POINT('Ctrl Pts',(6.27639573548135,-0.498231338984194,1.38977625915286));
#7513=CARTESIAN_POINT('Ctrl Pts',(6.38742327605243,1.62511398485724,2.00331433449301));
#7514=CARTESIAN_POINT('Ctrl Pts',(6.49845081662351,2.26273127670134,4.1178260879788));
#7515=CARTESIAN_POINT('Ctrl Pts',(6.60947835719459,0.834852461416416,5.80473060680729));
#7516=CARTESIAN_POINT('Ctrl Pts',(6.72050589776567,-1.3595303889214,5.51621007689934));
#7517=CARTESIAN_POINT('Ctrl Pts',(6.79452425814639,-1.98840280708376,4.1920821452035));
#7518=CARTESIAN_POINT('Ctrl Pts',(6.83153343833676,-1.95374385804904,3.54306089150614));
#7519=CARTESIAN_POINT('Ctrl Pts',(6.6,0.83475068776765,5.41764852956582));
#7520=CARTESIAN_POINT('Ctrl Pts',(6.6,0.7907192463387,5.43356975418934));
#7521=CARTESIAN_POINT('Ctrl Pts',(6.6,0.746172855022355,5.44776191297247));
#7522=CARTESIAN_POINT('Ctrl Pts',(6.6,0.701168580024064,5.46015373566206));
#7523=CARTESIAN_POINT('Ctrl Pts',(6.59999999999999,0.632780325132891,5.47898428295328));
#7524=CARTESIAN_POINT('Ctrl Pts',(6.6,0.563334570934092,5.4936600771938));
#7525=CARTESIAN_POINT('Ctrl Pts',(6.6,0.493183000021699,5.50428783505599));
#7526=CARTESIAN_POINT('Ctrl Pts',(6.6,0.422101207198843,5.51505651881754));
#7527=CARTESIAN_POINT('Ctrl Pts',(6.6,0.350293636793038,5.52166884246508));
#7528=CARTESIAN_POINT('Ctrl Pts',(6.6,0.27813252516632,5.52418340588879));
#7529=CARTESIAN_POINT('Ctrl Pts',(6.6,0.245886653870964,5.5253070622003));
#7530=CARTESIAN_POINT('Ctrl Pts',(6.6,0.213570373230081,5.52561179547265));
#7531=CARTESIAN_POINT('Ctrl Pts',(6.6,0.181218209310509,5.52509972733514));
#7532=CARTESIAN_POINT('Ctrl Pts',(6.6,0.160635756760572,5.52477394949324));
#7533=CARTESIAN_POINT('Ctrl Pts',(6.6,0.140038799819156,5.52411753323207));
#7534=CARTESIAN_POINT('Ctrl Pts',(6.6,0.119436477971668,5.52313064631116));
#7535=CARTESIAN_POINT('Ctrl Pts',(6.6,0.107012385202456,5.5225355107362));
#7536=CARTESIAN_POINT('Ctrl Pts',(6.6,0.0945852684045237,5.52182002860968));
#7537=CARTESIAN_POINT('Ctrl Pts',(6.6,0.0821742362622182,5.52098560168444));
#7538=CARTESIAN_POINT('Ctrl Pts',(6.6,0.0118828483352063,5.51625972344755));
#7539=CARTESIAN_POINT('Ctrl Pts',(6.6,-0.0580208766357301,5.50771766688684));
#7540=CARTESIAN_POINT('Ctrl Pts',(6.6,-0.127194914653041,5.49545172311728));
#7541=CARTESIAN_POINT('Ctrl Pts',(6.6,-0.195407928455584,5.48335618820801));
#7542=CARTESIAN_POINT('Ctrl Pts',(6.6,-0.262912350188068,5.46763903161646));
#7543=CARTESIAN_POINT('Ctrl Pts',(6.6,-0.329361205530838,5.44834294016328));
#7544=CARTESIAN_POINT('Ctrl Pts',(6.6,-0.39443868562668,5.42944508254039));
#7545=CARTESIAN_POINT('Ctrl Pts',(6.6,-0.458504499770776,5.40711402878201));
#7546=CARTESIAN_POINT('Ctrl Pts',(6.6,-0.521201674010066,5.38135263368021));
#7547=CARTESIAN_POINT('Ctrl Pts',(6.6,-0.536341223469168,5.37513200380317));
#7548=CARTESIAN_POINT('Ctrl Pts',(6.6,-0.551400795462264,5.36871120070083));
#7549=CARTESIAN_POINT('Ctrl Pts',(6.6,-0.566375007959067,5.36208997493157));
#7550=CARTESIAN_POINT('Ctrl Pts',(6.6,-0.580397210895579,5.35588970420315));
#7551=CARTESIAN_POINT('Ctrl Pts',(6.6,-0.594348562079377,5.34951165292965));
#7552=CARTESIAN_POINT('Ctrl Pts',(6.6,-0.608198751037917,5.34296812914935));
#7553=CARTESIAN_POINT('Ctrl Pts',(6.6,-0.668835467720879,5.31432030356649));
#7554=CARTESIAN_POINT('Ctrl Pts',(6.6,-0.727626283845795,5.2824663680222));
#7555=CARTESIAN_POINT('Ctrl Pts',(6.6,-0.784252300272617,5.24745318929936));
#7556=CARTESIAN_POINT('Ctrl Pts',(6.6,-0.839181587060244,5.21348913784788));
#7557=CARTESIAN_POINT('Ctrl Pts',(6.6,-0.892074481393698,5.17655181647775));
#7558=CARTESIAN_POINT('Ctrl Pts',(6.6,-0.942605638289231,5.13664980579598));
#7559=CARTESIAN_POINT('Ctrl Pts',(6.6,-0.97196789287341,5.11346385344422));
#7560=CARTESIAN_POINT('Ctrl Pts',(6.6,-1.0005320279455,5.08927628731349));
#7561=CARTESIAN_POINT('Ctrl Pts',(6.6,-1.02822743693251,5.06408422531173));
#7562=CARTESIAN_POINT('Ctrl Pts',(6.6,-1.05360839269705,5.0409974165347));
#7563=CARTESIAN_POINT('Ctrl Pts',(6.6,-1.0782596465578,5.01706684049449));
#7564=CARTESIAN_POINT('Ctrl Pts',(6.6,-1.10215906011825,4.99233467734655));
#7565=CARTESIAN_POINT('Ctrl Pts',(6.6,-1.11213104593841,4.98201522831115));
#7566=CARTESIAN_POINT('Ctrl Pts',(6.6,-1.12197209812286,4.97155621624695));
#7567=CARTESIAN_POINT('Ctrl Pts',(6.6,-1.13168042863728,4.96096067320925));
#7568=CARTESIAN_POINT('Ctrl Pts',(6.6,-1.13846377682764,4.95355741704859));
#7569=CARTESIAN_POINT('Ctrl Pts',(6.6,-1.14518055031752,4.94608936896101));
#7570=CARTESIAN_POINT('Ctrl Pts',(6.6,-1.15182470155627,4.93856413467273));
#7571=CARTESIAN_POINT('Ctrl Pts',(6.6,-1.19473914758542,4.88995879004454));
#7572=CARTESIAN_POINT('Ctrl Pts',(6.6,-1.23469798302823,4.83889366788672));
#7573=CARTESIAN_POINT('Ctrl Pts',(6.6,-1.27161691617958,4.78569376443529));
#7574=CARTESIAN_POINT('Ctrl Pts',(6.6,-1.30884832150702,4.73204359094136));
#7575=CARTESIAN_POINT('Ctrl Pts',(6.6,-1.34298845602856,4.67622123916325));
#7576=CARTESIAN_POINT('Ctrl Pts',(6.6,-1.37390225462564,4.61854045629316));
#7577=CARTESIAN_POINT('Ctrl Pts',(6.6,-1.39543358791776,4.57836602879194));
#7578=CARTESIAN_POINT('Ctrl Pts',(6.6,-1.41539879072854,4.53728964557128));
#7579=CARTESIAN_POINT('Ctrl Pts',(6.6,-1.43373730300016,4.49541608744732));
#7580=CARTESIAN_POINT('Ctrl Pts',(6.6,-1.44483372953756,4.47007887062731));
#7581=CARTESIAN_POINT('Ctrl Pts',(6.6,-1.45533433096051,4.44444978199303));
#7582=CARTESIAN_POINT('Ctrl Pts',(6.6,-1.46522340819265,4.4185523449034));
#7583=CARTESIAN_POINT('Ctrl Pts',(6.6,-1.47150797518841,4.40209437065686));
#7584=CARTESIAN_POINT('Ctrl Pts',(6.6,-1.47754607716869,4.38552568952892));
#7585=CARTESIAN_POINT('Ctrl Pts',(6.6,-1.48332362301664,4.36888265218315));
#7586=CARTESIAN_POINT('Ctrl Pts',(6.6,-1.50409466260666,4.30904873710829));
#7587=CARTESIAN_POINT('Ctrl Pts',(6.6,-1.52153669760017,4.24816653118245));
#7588=CARTESIAN_POINT('Ctrl Pts',(6.6,-1.53551151713138,4.1865281437664));
#7589=CARTESIAN_POINT('Ctrl Pts',(6.6,-1.54677461255909,4.13685029011493));
#7590=CARTESIAN_POINT('Ctrl Pts',(6.6,-1.55578462243918,4.0866809055628));
#7591=CARTESIAN_POINT('Ctrl Pts',(6.6,-1.5624447079276,4.03617640078013));
#7592=CARTESIAN_POINT('Ctrl Pts',(6.6,-1.56482594198486,4.01811911802562));
#7593=CARTESIAN_POINT('Ctrl Pts',(6.6,-1.56690656930183,4.0000190527265));
#7594=CARTESIAN_POINT('Ctrl Pts',(6.6,-1.56868146275449,3.98188358890452));
#7595=CARTESIAN_POINT('Ctrl Pts',(6.6,-1.56996504110089,3.96876827281105));
#7596=CARTESIAN_POINT('Ctrl Pts',(6.6,-1.57108783614685,3.95564316697099));
#7597=CARTESIAN_POINT('Ctrl Pts',(6.6,-1.57204829871556,3.94251393056363));
#7598=CARTESIAN_POINT('Ctrl Pts',(6.6,-1.57651492193096,3.88145652546695));
#7599=CARTESIAN_POINT('Ctrl Pts',(6.6,-1.57747688601606,3.8202878692938));
#7600=CARTESIAN_POINT('Ctrl Pts',(6.6,-1.57477701172204,3.75928439565726));
#7601=CARTESIAN_POINT('Ctrl Pts',(6.6,-1.57207713742801,3.69828092202073));
#7602=CARTESIAN_POINT('Ctrl Pts',(6.6,-1.56571553600282,3.63744172304545));
#7603=CARTESIAN_POINT('Ctrl Pts',(6.6,-1.55548296577373,3.57706412386904));
#7604=CARTESIAN_POINT('Ctrl Pts',(6.6,-1.55476975631725,3.57285580926891));
#7605=CARTESIAN_POINT('Ctrl Pts',(6.6,-1.55403772001803,3.56864974883175));
#7606=CARTESIAN_POINT('Ctrl Pts',(6.6,-1.55328677638795,3.5644460487792));
#7607=CARTESIAN_POINT('Ctrl Pts',(2.5,-0.90555138132905,2.37953274318763));
#7608=CARTESIAN_POINT('Ctrl Pts',(2.5,-0.93880750735117,2.39730741392822));
#7609=CARTESIAN_POINT('Ctrl Pts',(2.5,-0.971294169096419,2.41632950410138));
#7610=CARTESIAN_POINT('Ctrl Pts',(2.5,-1.00293325234873,2.43657864884141));
#7611=CARTESIAN_POINT('Ctrl Pts',(2.5,-1.05381727266378,2.46914463326318));
#7612=CARTESIAN_POINT('Ctrl Pts',(2.5,-1.10251035681737,2.504881140639));
#7613=CARTESIAN_POINT('Ctrl Pts',(2.5,-1.14893834404752,2.54343425063693));
#7614=CARTESIAN_POINT('Ctrl Pts',(2.5,-1.19536633127767,2.58198736063487));
#7615=CARTESIAN_POINT('Ctrl Pts',(2.5,-1.23952977771182,2.62335775774592));
#7616=CARTESIAN_POINT('Ctrl Pts',(2.5,-1.28133554406986,2.66724270313463));
#7617=CARTESIAN_POINT('Ctrl Pts',(2.5,-1.30007944324187,2.68691881634089));
#7618=CARTESIAN_POINT('Ctrl Pts',(2.5,-1.31834908791515,2.70710103623637));
#7619=CARTESIAN_POINT('Ctrl Pts',(2.5,-1.33613438528023,2.72776484851289));
#7620=CARTESIAN_POINT('Ctrl Pts',(2.5,-1.34511395963603,2.73819774907128));
#7621=CARTESIAN_POINT('Ctrl Pts',(2.5,-1.3539700498305,2.7487534378352));
#7622=CARTESIAN_POINT('Ctrl Pts',(2.5,-1.36270123656446,2.75942890284035));
#7623=CARTESIAN_POINT('Ctrl Pts',(2.5,-1.37087012055391,2.76941685039178));
#7624=CARTESIAN_POINT('Ctrl Pts',(2.5,-1.37893068792576,2.77951115670231));
#7625=CARTESIAN_POINT('Ctrl Pts',(2.5,-1.3868685316678,2.78969190448424));
#7626=CARTESIAN_POINT('Ctrl Pts',(2.5,-1.42575294050728,2.83956342777312));
#7627=CARTESIAN_POINT('Ctrl Pts',(2.5,-1.46176828378797,2.89159377977689));
#7628=CARTESIAN_POINT('Ctrl Pts',(2.5,-1.49483280838799,2.94542719134683));
#7629=CARTESIAN_POINT('Ctrl Pts',(2.5,-1.52879779255553,3.00072666998067));
#7630=CARTESIAN_POINT('Ctrl Pts',(2.5,-1.55964980038297,3.0579294097504));
#7631=CARTESIAN_POINT('Ctrl Pts',(2.5,-1.5872713657029,3.1166972983774));
#7632=CARTESIAN_POINT('Ctrl Pts',(2.5,-1.61427745983938,3.17415570502743));
#7633=CARTESIAN_POINT('Ctrl Pts',(2.5,-1.63819595312948,3.23311127180302));
#7634=CARTESIAN_POINT('Ctrl Pts',(2.5,-1.65888103082398,3.29327996689751));
#7635=CARTESIAN_POINT('Ctrl Pts',(2.5,-1.66330526486958,3.30614916629079));
#7636=CARTESIAN_POINT('Ctrl Pts',(2.5,-1.66758143129416,3.31907395081593));
#7637=CARTESIAN_POINT('Ctrl Pts',(2.5,-1.67170785006544,3.33205167100484));
#7638=CARTESIAN_POINT('Ctrl Pts',(2.5,-1.67470502409831,3.34147788005242));
#7639=CARTESIAN_POINT('Ctrl Pts',(2.5,-1.67762270873155,3.35093067258331));
#7640=CARTESIAN_POINT('Ctrl Pts',(2.5,-1.68045765020628,3.36039960232082));
#7641=CARTESIAN_POINT('Ctrl Pts',(2.5,-1.69969107444953,3.42464076722468));
#7642=CARTESIAN_POINT('Ctrl Pts',(2.5,-1.71515655757218,3.48973852410454));
#7643=CARTESIAN_POINT('Ctrl Pts',(2.5,-1.72674329036456,3.55533433283122));
#7644=CARTESIAN_POINT('Ctrl Pts',(2.5,-1.73830533428164,3.62079037077252));
#7645=CARTESIAN_POINT('Ctrl Pts',(2.5,-1.74600577016652,3.68674333672573));
#7646=CARTESIAN_POINT('Ctrl Pts',(2.5,-1.74969313315652,3.75286685210673));
#7647=CARTESIAN_POINT('Ctrl Pts',(2.5,-1.75158782641292,3.78684337652853));
#7648=CARTESIAN_POINT('Ctrl Pts',(2.5,-1.75242223721534,3.82086532262759));
#7649=CARTESIAN_POINT('Ctrl Pts',(2.5,-1.75217071705448,3.85489016933049));
#7650=CARTESIAN_POINT('Ctrl Pts',(2.5,-1.75188640575889,3.89335089635671));
#7651=CARTESIAN_POINT('Ctrl Pts',(2.5,-1.75021469129045,3.93181536987594));
#7652=CARTESIAN_POINT('Ctrl Pts',(2.5,-1.74719268051567,3.97023541010561));
#7653=CARTESIAN_POINT('Ctrl Pts',(2.5,-1.74626233628244,3.98206325108041));
#7654=CARTESIAN_POINT('Ctrl Pts',(2.5,-1.74520379368855,3.99388863700969));
#7655=CARTESIAN_POINT('Ctrl Pts',(2.5,-1.74401857389237,4.00570464324205));
#7656=CARTESIAN_POINT('Ctrl Pts',(2.5,-1.73746351572078,4.07105506048821));
#7657=CARTESIAN_POINT('Ctrl Pts',(2.5,-1.72706359835322,4.13587276899823));
#7658=CARTESIAN_POINT('Ctrl Pts',(2.5,-1.71308067358899,4.19991291679085));
#7659=CARTESIAN_POINT('Ctrl Pts',(2.5,-1.69878949243908,4.26536484250758));
#7660=CARTESIAN_POINT('Ctrl Pts',(2.5,-1.68075547676008,4.33000530229676));
#7661=CARTESIAN_POINT('Ctrl Pts',(2.5,-1.65920408579077,4.39358324301916));
#7662=CARTESIAN_POINT('Ctrl Pts',(2.5,-1.63719262963768,4.45851840458285));
#7663=CARTESIAN_POINT('Ctrl Pts',(2.5,-1.6115118634901,4.52234611045107));
#7664=CARTESIAN_POINT('Ctrl Pts',(2.5,-1.58234824099336,4.58479677198594));
#7665=CARTESIAN_POINT('Ctrl Pts',(2.5,-1.57482933895901,4.6008976663832));
#7666=CARTESIAN_POINT('Ctrl Pts',(2.5,-1.56707866594256,4.61690697691865));
#7667=CARTESIAN_POINT('Ctrl Pts',(2.5,-1.55909887661223,4.63281994276844));
#7668=CARTESIAN_POINT('Ctrl Pts',(2.5,-1.55322527454176,4.64453283709354));
#7669=CARTESIAN_POINT('Ctrl Pts',(2.5,-1.54722753641133,4.65619353199876));
#7670=CARTESIAN_POINT('Ctrl Pts',(2.5,-1.5411066480093,4.66780009870029));
#7671=CARTESIAN_POINT('Ctrl Pts',(2.5,-1.53534542546513,4.67872465888653));
#7672=CARTESIAN_POINT('Ctrl Pts',(2.5,-1.52947966958375,4.68959258357274));
#7673=CARTESIAN_POINT('Ctrl Pts',(2.5,-1.52351124623624,4.70040147771323));
#7674=CARTESIAN_POINT('Ctrl Pts',(2.5,-1.48912287726794,4.76267927173023));
#7675=CARTESIAN_POINT('Ctrl Pts',(2.5,-1.4513252131105,4.82300799807137));
#7676=CARTESIAN_POINT('Ctrl Pts',(2.5,-1.41034991340656,4.88110430172282));
#7677=CARTESIAN_POINT('Ctrl Pts',(2.5,-1.37394992444786,4.93271355965951));
#7678=CARTESIAN_POINT('Ctrl Pts',(2.5,-1.33504133706495,4.982561572211));
#7679=CARTESIAN_POINT('Ctrl Pts',(2.5,-1.29375331926984,5.03044054309444));
#7680=CARTESIAN_POINT('Ctrl Pts',(2.5,-1.28165188881147,5.04447376792591));
#7681=CARTESIAN_POINT('Ctrl Pts',(2.5,-1.26934585898454,5.05833775135132));
#7682=CARTESIAN_POINT('Ctrl Pts',(2.5,-1.25683802017703,5.07202700942535));
#7683=CARTESIAN_POINT('Ctrl Pts',(2.5,-1.2467077044287,5.0831141771435));
#7684=CARTESIAN_POINT('Ctrl Pts',(2.5,-1.23645016461734,5.09408100911092));
#7685=CARTESIAN_POINT('Ctrl Pts',(2.5,-1.22607160176172,5.10492048819118));
#7686=CARTESIAN_POINT('Ctrl Pts',(2.5,-1.17589217237818,5.15732840657345));
#7687=CARTESIAN_POINT('Ctrl Pts',(2.5,-1.12285728917657,5.20679395228197));
#7688=CARTESIAN_POINT('Ctrl Pts',(2.5,-1.0671763087449,5.25302071945437));
#7689=CARTESIAN_POINT('Ctrl Pts',(2.5,-1.01196398502003,5.29885840431713));
#7690=CARTESIAN_POINT('Ctrl Pts',(2.5,-0.954149411695466,5.3415125564613));
#7691=CARTESIAN_POINT('Ctrl Pts',(2.5,-0.893894163872906,5.38066677881512));
#7692=CARTESIAN_POINT('Ctrl Pts',(2.5,-0.883181709014017,5.38762779639712));
#7693=CARTESIAN_POINT('Ctrl Pts',(2.5,-0.872392012796053,5.39447809860179));
#7694=CARTESIAN_POINT('Ctrl Pts',(2.5,-0.861525859670531,5.40121577991141));
#7695=CARTESIAN_POINT('Ctrl Pts',(2.2684956023837,1.13599383904839,2.05457297837212));
#7696=CARTESIAN_POINT('Ctrl Pts',(2.30551665559472,1.66530114882627,2.43205274651924));
#7697=CARTESIAN_POINT('Ctrl Pts',(2.37954688899609,2.30874613777931,3.74944295559739));
#7698=CARTESIAN_POINT('Ctrl Pts',(2.49058630258783,1.16608200062918,5.64507475471972));
#7699=CARTESIAN_POINT('Ctrl Pts',(2.60161384315891,-1.04293058450782,5.7096573157296));
#7700=CARTESIAN_POINT('Ctrl Pts',(2.71264138372999,-2.2985040575111,3.89288000979708));
#7701=CARTESIAN_POINT('Ctrl Pts',(2.82366892430106,-1.45435102275404,1.85036189287024));
#7702=CARTESIAN_POINT('Ctrl Pts',(2.93469646487215,0.718720235097674,1.4504525726535));
#7703=CARTESIAN_POINT('Ctrl Pts',(3.04572400544322,2.23505443062616,3.05738160024003));
#7704=CARTESIAN_POINT('Ctrl Pts',(3.15675154601431,1.70937833319429,5.20357835530822));
#7705=CARTESIAN_POINT('Ctrl Pts',(3.26777908658538,-0.378088709672632,5.92786550335696));
#7706=CARTESIAN_POINT('Ctrl Pts',(3.37880662715646,-2.12010467341404,4.56866108547329));
#7707=CARTESIAN_POINT('Ctrl Pts',(3.48983416772754,-1.92509810864168,2.36771502264023));
#7708=CARTESIAN_POINT('Ctrl Pts',(3.60086170829862,0.0287726246970394,1.3359598329503));
#7709=CARTESIAN_POINT('Ctrl Pts',(3.7118892488697,1.95635373610663,2.41603341962473));
#7710=CARTESIAN_POINT('Ctrl Pts',(3.82291678944078,2.0965179233959,4.62114101481739));
#7711=CARTESIAN_POINT('Ctrl Pts',(3.93394433001185,0.321203270128675,5.93658538901197));
#7712=CARTESIAN_POINT('Ctrl Pts',(4.04497187058293,-1.74757773142461,5.16051723839122));
#7713=CARTESIAN_POINT('Ctrl Pts',(4.15599941115401,-2.2196887832987,3.00198764182795));
#7714=CARTESIAN_POINT('Ctrl Pts',(4.26702695172509,-0.663786606567354,1.43313269957975));
#7715=CARTESIAN_POINT('Ctrl Pts',(4.37805449229617,1.49858251767498,1.88733236901576));
#7716=CARTESIAN_POINT('Ctrl Pts',(4.48908203286725,2.29177547185453,3.949608535076));
#7717=CARTESIAN_POINT('Ctrl Pts',(4.60010957343832,0.991093389100879,5.73576745544));
#7718=CARTESIAN_POINT('Ctrl Pts',(4.7111371140094,-1.21509863142361,5.61388972183788));
#7719=CARTESIAN_POINT('Ctrl Pts',(4.82216465458049,-2.3111189503039,3.69532819685544));
#7720=CARTESIAN_POINT('Ctrl Pts',(4.93319219515156,-1.29559086556015,1.73297264398223));
#7721=CARTESIAN_POINT('Ctrl Pts',(5.04421973572264,0.903650040337952,1.51972289010189));
#7722=CARTESIAN_POINT('Ctrl Pts',(5.15524727629372,2.27727441159882,3.25041685278073));
#7723=CARTESIAN_POINT('Ctrl Pts',(5.26627481686479,1.57027056200704,5.34380488426394));
#7724=CARTESIAN_POINT('Ctrl Pts',(5.37730235743588,-0.571403078011826,5.88727855768163));
#7725=CARTESIAN_POINT('Ctrl Pts',(5.48832989800695,-2.19102344350068,4.38427456450717));
#7726=CARTESIAN_POINT('Ctrl Pts',(5.59935743857804,-1.80880579267535,2.20804710973091));
#7727=CARTESIAN_POINT('Ctrl Pts',(5.71038497914911,0.225994198385467,1.34682732113855));
#7728=CARTESIAN_POINT('Ctrl Pts',(5.82141251972019,2.05437013573577,2.5876082456352));
#7729=CARTESIAN_POINT('Ctrl Pts',(5.93244006029126,2.00567014672563,4.79648094529437));
#7730=CARTESIAN_POINT('Ctrl Pts',(6.04346760086235,0.124697940094911,5.95583840267335));
#7731=CARTESIAN_POINT('Ctrl Pts',(6.15449514143342,-1.87059546628156,5.00542858236713));
#7732=CARTESIAN_POINT('Ctrl Pts',(6.2655226820045,-2.15606965103839,2.81553154933147));
#7733=CARTESIAN_POINT('Ctrl Pts',(6.37655022257558,-0.473125107460962,1.3831890024094));
#7734=CARTESIAN_POINT('Ctrl Pts',(6.48757776314666,1.64508549561477,2.02446699268324));
#7735=CARTESIAN_POINT('Ctrl Pts',(6.56159612352738,2.0503723003236,3.43311140089402));
#7736=CARTESIAN_POINT('Ctrl Pts',(6.59860530371774,1.91070454657702,4.06783526971427));
#7737=CARTESIAN_POINT('Ctrl Pts',(2.34618472182287,1.05786062916686,2.16412661457789));
#7738=CARTESIAN_POINT('Ctrl Pts',(2.38320577503389,1.55076239015994,2.51564347259569));
#7739=CARTESIAN_POINT('Ctrl Pts',(2.45723600843527,2.14995148560286,3.74242410073808));
#7740=CARTESIAN_POINT('Ctrl Pts',(2.56827542202699,1.08587933881672,5.50767508957099));
#7741=CARTESIAN_POINT('Ctrl Pts',(2.67930296259808,-0.971198228706072,5.56781568741114));
#7742=CARTESIAN_POINT('Ctrl Pts',(2.79033050316915,-2.14041385159106,3.87599561071092));
#7743=CARTESIAN_POINT('Ctrl Pts',(2.90135804374023,-1.35432133086994,1.97396108729576));
#7744=CARTESIAN_POINT('Ctrl Pts',(3.01238558431131,0.669286939735766,1.60155737298641));
#7745=CARTESIAN_POINT('Ctrl Pts',(3.12341312488239,2.08132826511188,3.09796245346921));
#7746=CARTESIAN_POINT('Ctrl Pts',(3.23444066545347,1.59180796310647,5.09654463903297));
#7747=CARTESIAN_POINT('Ctrl Pts',(3.34546820602455,-0.352083916784466,5.77101560163446));
#7748=CARTESIAN_POINT('Ctrl Pts',(3.45649574659563,-1.97428470703338,4.50529672953804));
#7749=CARTESIAN_POINT('Ctrl Pts',(3.5675232871667,-1.79269061716177,2.45573087208473));
#7750=CARTESIAN_POINT('Ctrl Pts',(3.67855082773778,0.0267936548760598,1.49493939893213));
#7751=CARTESIAN_POINT('Ctrl Pts',(3.78957836830886,1.82179649485102,2.50072594871047));
#7752=CARTESIAN_POINT('Ctrl Pts',(3.90060590887995,1.9523202444135,4.55416710996289));
#7753=CARTESIAN_POINT('Ctrl Pts',(4.01163344945101,0.299111035420234,5.77913573698043));
#7754=CARTESIAN_POINT('Ctrl Pts',(4.12266099002211,-1.62738002173627,5.05644524881745));
#7755=CARTESIAN_POINT('Ctrl Pts',(4.23368853059317,-2.06701946096996,3.04637846975065));
#7756=CARTESIAN_POINT('Ctrl Pts',(4.34471607116426,-0.618131624590583,1.58542875397713));
#7757=CARTESIAN_POINT('Ctrl Pts',(4.45574361173533,1.39551060095016,2.00838874861888));
#7758=CARTESIAN_POINT('Ctrl Pts',(4.56677115230641,2.13414805541207,3.92882237031159));
#7759=CARTESIAN_POINT('Ctrl Pts',(4.67779869287749,0.92292637523073,5.59212998197178));
#7760=CARTESIAN_POINT('Ctrl Pts',(4.78882623344857,-1.13152462500531,5.47863495099715));
#7761=CARTESIAN_POINT('Ctrl Pts',(4.89985377401965,-2.15216109701436,3.69203133383899));
#7762=CARTESIAN_POINT('Ctrl Pts',(5.01088131459073,-1.2064806349059,1.86464582482029));
#7763=CARTESIAN_POINT('Ctrl Pts',(5.1219088551618,0.841497345636436,1.66606330521921));
#7764=CARTESIAN_POINT('Ctrl Pts',(5.23293639573289,2.12064437238283,3.27772081718985));
#7765=CARTESIAN_POINT('Ctrl Pts',(5.34396393630396,1.46226796976159,5.22712644242662));
#7766=CARTESIAN_POINT('Ctrl Pts',(5.45499147687504,-0.532102198828669,5.73322021013476));
#7767=CARTESIAN_POINT('Ctrl Pts',(5.56601901744612,-2.04032571197971,4.33359224103263));
#7768=CARTESIAN_POINT('Ctrl Pts',(5.6770465580172,-1.68439684099265,2.30704485548668));
#7769=CARTESIAN_POINT('Ctrl Pts',(5.78807409858828,0.210450406220844,1.50505942555297));
#7770=CARTESIAN_POINT('Ctrl Pts',(5.89910163915935,1.91307136502743,2.66049992560517));
#7771=CARTESIAN_POINT('Ctrl Pts',(6.01012917973044,1.86772094212562,4.71744722891832));
#7772=CARTESIAN_POINT('Ctrl Pts',(6.1211567203015,0.116121264772982,5.79706453592731));
#7773=CARTESIAN_POINT('Ctrl Pts',(6.2321842608726,-1.74193664512735,4.9120235296154));
#7774=CARTESIAN_POINT('Ctrl Pts',(6.34321180144366,-2.00777602762851,2.87274675403155));
#7775=CARTESIAN_POINT('Ctrl Pts',(6.45423934201476,-0.440583748475745,1.53892016467367));
#7776=CARTESIAN_POINT('Ctrl Pts',(6.56526688258582,1.53193716163296,2.13609130675508));
#7777=CARTESIAN_POINT('Ctrl Pts',(6.63928524296654,1.90934849916403,3.44784970607045));
#7778=CARTESIAN_POINT('Ctrl Pts',(6.6762944231569,1.77928703864022,4.03891751659649));
#7779=CARTESIAN_POINT('Ctrl Pts',(2.42387384126203,0.979727419285334,2.27368025078364));
#7780=CARTESIAN_POINT('Ctrl Pts',(2.46089489447305,1.43622363149362,2.59923419867212));
#7781=CARTESIAN_POINT('Ctrl Pts',(2.53492512787443,1.99115683342641,3.73540524587877));
#7782=CARTESIAN_POINT('Ctrl Pts',(2.64596454146616,1.00567667700427,5.37027542442224));
#7783=CARTESIAN_POINT('Ctrl Pts',(2.75699208203724,-0.899465872904321,5.42597405909269));
#7784=CARTESIAN_POINT('Ctrl Pts',(2.86801962260832,-1.98232364567101,3.85911121162473));
#7785=CARTESIAN_POINT('Ctrl Pts',(2.9790471631794,-1.25429163898582,2.09756028172128));
#7786=CARTESIAN_POINT('Ctrl Pts',(3.09007470375048,0.619853644373857,1.75266217331931));
#7787=CARTESIAN_POINT('Ctrl Pts',(3.20110224432155,1.9276020995976,3.13854330669838));
#7788=CARTESIAN_POINT('Ctrl Pts',(3.31212978489263,1.47423759301864,4.98951092275774));
#7789=CARTESIAN_POINT('Ctrl Pts',(3.42315732546371,-0.326079123896298,5.61416569991195));
#7790=CARTESIAN_POINT('Ctrl Pts',(3.53418486603479,-1.82846474065272,4.44193237360281));
#7791=CARTESIAN_POINT('Ctrl Pts',(3.64521240660587,-1.66028312568185,2.54374672152922));
#7792=CARTESIAN_POINT('Ctrl Pts',(3.75623994717695,0.0248146850550797,1.65391896491398));
#7793=CARTESIAN_POINT('Ctrl Pts',(3.86726748774802,1.6872392535954,2.58541847779621));
#7794=CARTESIAN_POINT('Ctrl Pts',(3.97829502831911,1.8081225654311,4.4871932051084));
#7795=CARTESIAN_POINT('Ctrl Pts',(4.08932256889018,0.277018800711796,5.6216860849489));
#7796=CARTESIAN_POINT('Ctrl Pts',(4.20035010946126,-1.50718231204793,4.95237325924367));
#7797=CARTESIAN_POINT('Ctrl Pts',(4.31137765003234,-1.9143501386412,3.09076929767336));
#7798=CARTESIAN_POINT('Ctrl Pts',(4.42240519060342,-0.572476642613814,1.73772480837452));
#7799=CARTESIAN_POINT('Ctrl Pts',(4.5334327311745,1.29243868422536,2.12944512822199));
#7800=CARTESIAN_POINT('Ctrl Pts',(4.64446027174558,1.97652063896961,3.90803620554717));
#7801=CARTESIAN_POINT('Ctrl Pts',(4.75548781231665,0.85475936136058,5.44849250850354));
#7802=CARTESIAN_POINT('Ctrl Pts',(4.86651535288773,-1.04795061858702,5.34338018015643));
#7803=CARTESIAN_POINT('Ctrl Pts',(4.97754289345882,-1.99320324372482,3.68873447082252));
#7804=CARTESIAN_POINT('Ctrl Pts',(5.08857043402989,-1.11737040425166,1.99631900565835));
#7805=CARTESIAN_POINT('Ctrl Pts',(5.19959797460097,0.779344650934923,1.81240372033652));
#7806=CARTESIAN_POINT('Ctrl Pts',(5.31062551517205,1.96401433316682,3.305024781599));
#7807=CARTESIAN_POINT('Ctrl Pts',(5.42165305574313,1.35426537751614,5.11044800058928));
#7808=CARTESIAN_POINT('Ctrl Pts',(5.53268059631421,-0.492801319645516,5.5791618625879));
#7809=CARTESIAN_POINT('Ctrl Pts',(5.64370813688528,-1.88962798045874,4.2829099175581));
#7810=CARTESIAN_POINT('Ctrl Pts',(5.75473567745637,-1.55998788930993,2.40604260124246));
#7811=CARTESIAN_POINT('Ctrl Pts',(5.86576321802744,0.194906614056222,1.66329152996741));
#7812=CARTESIAN_POINT('Ctrl Pts',(5.97679075859853,1.77177259431909,2.73339160557513));
#7813=CARTESIAN_POINT('Ctrl Pts',(6.08781829916959,1.72977173752561,4.63841351254227));
#7814=CARTESIAN_POINT('Ctrl Pts',(6.19884583974068,0.107544589451052,5.63829066918126));
#7815=CARTESIAN_POINT('Ctrl Pts',(6.30987338031176,-1.61327782397314,4.81861847686368));
#7816=CARTESIAN_POINT('Ctrl Pts',(6.42090092088283,-1.85948240421864,2.92996195873161));
#7817=CARTESIAN_POINT('Ctrl Pts',(6.53192846145392,-0.408042389490527,1.69465132693797));
#7818=CARTESIAN_POINT('Ctrl Pts',(6.642956002025,1.41878882765114,2.2477156208269));
#7819=CARTESIAN_POINT('Ctrl Pts',(6.71697436240571,1.76832469800446,3.46258801124687));
#7820=CARTESIAN_POINT('Ctrl Pts',(6.75398354259607,1.64786953070343,4.00999976347872));
#7821=CARTESIAN_POINT('Ctrl Pts',(2.5015629607012,0.901594209403805,2.38323388698939));
#7822=CARTESIAN_POINT('Ctrl Pts',(2.53858401391222,1.3216848728273,2.68282492474856));
#7823=CARTESIAN_POINT('Ctrl Pts',(2.6126142473136,1.83236218124995,3.72838639101944));
#7824=CARTESIAN_POINT('Ctrl Pts',(2.72365366090533,0.925474015191809,5.23287575927348));
#7825=CARTESIAN_POINT('Ctrl Pts',(2.83468120147641,-0.827733517102571,5.28413243077424));
#7826=CARTESIAN_POINT('Ctrl Pts',(2.94570874204748,-1.82423343975097,3.84222681253854));
#7827=CARTESIAN_POINT('Ctrl Pts',(3.05673628261856,-1.15426194710171,2.22115947614681));
#7828=CARTESIAN_POINT('Ctrl Pts',(3.16776382318964,0.570420349011948,1.9037669736522));
#7829=CARTESIAN_POINT('Ctrl Pts',(3.27879136376072,1.77387593408332,3.17912415992756));
#7830=CARTESIAN_POINT('Ctrl Pts',(3.3898189043318,1.35666722293081,4.88247720648249));
#7831=CARTESIAN_POINT('Ctrl Pts',(3.50084644490287,-0.300074331008131,5.45731579818944));
#7832=CARTESIAN_POINT('Ctrl Pts',(3.61187398547396,-1.68264477427207,4.37856801766755));
#7833=CARTESIAN_POINT('Ctrl Pts',(3.72290152604503,-1.52787563420194,2.6317625709737));
#7834=CARTESIAN_POINT('Ctrl Pts',(3.83392906661612,0.0228357152340999,1.81289853089582));
#7835=CARTESIAN_POINT('Ctrl Pts',(3.94495660718719,1.55268201233977,2.67011100688194));
#7836=CARTESIAN_POINT('Ctrl Pts',(4.05598414775828,1.66392488644871,4.42021930025391));
#7837=CARTESIAN_POINT('Ctrl Pts',(4.16701168832934,0.254926566003358,5.46423643291735));
#7838=CARTESIAN_POINT('Ctrl Pts',(4.27803922890044,-1.38698460235959,4.84830126966989));
#7839=CARTESIAN_POINT('Ctrl Pts',(4.3890667694715,-1.76168081631245,3.13516012559607));
#7840=CARTESIAN_POINT('Ctrl Pts',(4.50009431004259,-0.526821660637044,1.8900208627719));
#7841=CARTESIAN_POINT('Ctrl Pts',(4.61112185061366,1.18936676750055,2.25050150782511));
#7842=CARTESIAN_POINT('Ctrl Pts',(4.72214939118474,1.81889322252715,3.88725004078275));
#7843=CARTESIAN_POINT('Ctrl Pts',(4.83317693175582,0.78659234749043,5.30485503503531));
#7844=CARTESIAN_POINT('Ctrl Pts',(4.9442044723269,-0.964376612168717,5.2081254093157));
#7845=CARTESIAN_POINT('Ctrl Pts',(5.05523201289798,-1.83424539043528,3.68543760780607));
#7846=CARTESIAN_POINT('Ctrl Pts',(5.16625955346906,-1.02826017359741,2.12799218649641));
#7847=CARTESIAN_POINT('Ctrl Pts',(5.27728709404013,0.717191956233405,1.95874413545384));
#7848=CARTESIAN_POINT('Ctrl Pts',(5.38831463461122,1.80738429395082,3.33232874600814));
#7849=CARTESIAN_POINT('Ctrl Pts',(5.49934217518229,1.2462627852707,4.99376955875193));
#7850=CARTESIAN_POINT('Ctrl Pts',(5.61036971575337,-0.45350044046236,5.42510351504104));
#7851=CARTESIAN_POINT('Ctrl Pts',(5.72139725632445,-1.73893024893777,4.23222759408355));
#7852=CARTESIAN_POINT('Ctrl Pts',(5.83242479689554,-1.43557893762722,2.50504034699825));
#7853=CARTESIAN_POINT('Ctrl Pts',(5.94345233746659,0.179362821891601,1.82152363438183));
#7854=CARTESIAN_POINT('Ctrl Pts',(6.0544798780377,1.63047382361075,2.80628328554509));
#7855=CARTESIAN_POINT('Ctrl Pts',(6.16550741860875,1.59182253292561,4.55937979616623));
#7856=CARTESIAN_POINT('Ctrl Pts',(6.27653495917986,0.0989679141291208,5.47951680243522));
#7857=CARTESIAN_POINT('Ctrl Pts',(6.38756249975091,-1.48461900281893,4.72521342411197));
#7858=CARTESIAN_POINT('Ctrl Pts',(6.498590040322,-1.71118878080877,2.98717716343168));
#7859=CARTESIAN_POINT('Ctrl Pts',(6.60961758089308,-0.375501030505309,1.85038248920226));
#7860=CARTESIAN_POINT('Ctrl Pts',(6.72064512146415,1.30564049366934,2.35933993489874));
#7861=CARTESIAN_POINT('Ctrl Pts',(6.79466348184488,1.62730089684488,3.47732631642329));
#7862=CARTESIAN_POINT('Ctrl Pts',(6.83167266203525,1.51645202276663,3.98108201036094));
#7863=CARTESIAN_POINT('Ctrl Pts',(6.6,-0.426653165344755,2.14890699090199));
#7864=CARTESIAN_POINT('Ctrl Pts',(6.6,-0.392021497824994,2.13398863376564));
#7865=CARTESIAN_POINT('Ctrl Pts',(6.6,-0.356894299772028,2.12044962477061));
#7866=CARTESIAN_POINT('Ctrl Pts',(6.6,-0.32133619505273,2.10833833927896));
#7867=CARTESIAN_POINT('Ctrl Pts',(6.6,-0.265498001506515,2.08931954430338));
#7868=CARTESIAN_POINT('Ctrl Pts',(6.6,-0.208598730002439,2.07381868407842));
#7869=CARTESIAN_POINT('Ctrl Pts',(6.6,-0.150939387672386,2.06168379970761));
#7870=CARTESIAN_POINT('Ctrl Pts',(6.6,-0.0913824051006462,2.0491495412895));
#7871=CARTESIAN_POINT('Ctrl Pts',(6.6,-0.031013775489611,2.04020620059287));
#7872=CARTESIAN_POINT('Ctrl Pts',(6.6,0.0298636687991222,2.03473391298628));
#7873=CARTESIAN_POINT('Ctrl Pts',(6.6,0.0578342379090375,2.0322196320325));
#7874=CARTESIAN_POINT('Ctrl Pts',(6.6,0.0859125425023256,2.03043876497452));
#7875=CARTESIAN_POINT('Ctrl Pts',(6.6,0.114070466778614,2.02938311428739));
#7876=CARTESIAN_POINT('Ctrl Pts',(6.6,0.127825777648026,2.02886742274605));
#7877=CARTESIAN_POINT('Ctrl Pts',(6.6,0.141600097379563,2.02852482806017));
#7878=CARTESIAN_POINT('Ctrl Pts',(6.6,0.15539018623994,2.02835456195391));
#7879=CARTESIAN_POINT('Ctrl Pts',(6.6,0.16829253625044,2.02819525675146));
#7880=CARTESIAN_POINT('Ctrl Pts',(6.6,0.181210508110224,2.02818695541741));
#7881=CARTESIAN_POINT('Ctrl Pts',(6.6,0.194119545976811,2.02832850350873));
#7882=CARTESIAN_POINT('Ctrl Pts',(6.6,0.257354815079917,2.02902188064017));
#7883=CARTESIAN_POINT('Ctrl Pts',(6.6,0.320489102895611,2.03330438411646));
#7884=CARTESIAN_POINT('Ctrl Pts',(6.6,0.383193278384661,2.04101811063467));
#7885=CARTESIAN_POINT('Ctrl Pts',(6.6,0.447605187382698,2.04894191868496));
#7886=CARTESIAN_POINT('Ctrl Pts',(6.6,0.511564220195584,2.06048621348128));
#7887=CARTESIAN_POINT('Ctrl Pts',(6.6,0.574732782147204,2.07553202138906));
#7888=CARTESIAN_POINT('Ctrl Pts',(6.6,0.636493843821096,2.09024258375453));
#7889=CARTESIAN_POINT('Ctrl Pts',(6.6,0.697500338542476,2.10830059516598));
#7890=CARTESIAN_POINT('Ctrl Pts',(6.6,0.757439278502091,2.1296429645003));
#7891=CARTESIAN_POINT('Ctrl Pts',(6.6,0.77025897939523,2.1342076563584));
#7892=CARTESIAN_POINT('Ctrl Pts',(6.6,0.783029821878101,2.13892276046386));
#7893=CARTESIAN_POINT('Ctrl Pts',(6.6,0.795748687204425,2.14378793840273));
#7894=CARTESIAN_POINT('Ctrl Pts',(6.6,0.80498703879146,2.14732176183585));
#7895=CARTESIAN_POINT('Ctrl Pts',(6.6,0.814196614693253,2.15093430581471));
#7896=CARTESIAN_POINT('Ctrl Pts',(6.6,0.823367217856443,2.15462160067646));
#7897=CARTESIAN_POINT('Ctrl Pts',(6.6,0.885585028569377,2.17963799378264));
#7898=CARTESIAN_POINT('Ctrl Pts',(6.6,0.946123260308849,2.20813435132922));
#7899=CARTESIAN_POINT('Ctrl Pts',(6.6,1.00463249771459,2.23997375815824));
#7900=CARTESIAN_POINT('Ctrl Pts',(6.6,1.06301708518201,2.27174533330335));
#7901=CARTESIAN_POINT('Ctrl Pts',(6.6,1.11938248640286,2.30684585706902));
#7902=CARTESIAN_POINT('Ctrl Pts',(6.6,1.17337908236605,2.34519025244813));
#7903=CARTESIAN_POINT('Ctrl Pts',(6.6,1.20112489863409,2.36489328242844));
#7904=CARTESIAN_POINT('Ctrl Pts',(6.6,1.22824511880884,2.38545362366961));
#7905=CARTESIAN_POINT('Ctrl Pts',(6.6,1.25469050295843,2.40686481674482));
#7906=CARTESIAN_POINT('Ctrl Pts',(6.6,1.28458305880661,2.43106697169013));
#7907=CARTESIAN_POINT('Ctrl Pts',(6.6,1.31361349719728,2.45635617344964));
#7908=CARTESIAN_POINT('Ctrl Pts',(6.6,1.34176728722325,2.48267337167383));
#7909=CARTESIAN_POINT('Ctrl Pts',(6.6,1.35578764887621,2.49577912533809));
#7910=CARTESIAN_POINT('Ctrl Pts',(6.6,1.3695970620793,2.50914671196291));
#7911=CARTESIAN_POINT('Ctrl Pts',(6.6,1.38316141179628,2.52273642352609));
#7912=CARTESIAN_POINT('Ctrl Pts',(6.6,1.42965922152231,2.56932117220041));
#7913=CARTESIAN_POINT('Ctrl Pts',(6.6,1.47332647655611,2.6185511247577));
#7914=CARTESIAN_POINT('Ctrl Pts',(6.6,1.51413239558925,2.67007175656389));
#7915=CARTESIAN_POINT('Ctrl Pts',(6.6,1.55582152221007,2.72270750632383));
#7916=CARTESIAN_POINT('Ctrl Pts',(6.6,1.59452464031864,2.7777347408237));
#7917=CARTESIAN_POINT('Ctrl Pts',(6.6,1.63018231428798,2.83482333659135));
#7918=CARTESIAN_POINT('Ctrl Pts',(6.6,1.66654200783675,2.89303587869451));
#7919=CARTESIAN_POINT('Ctrl Pts',(6.6,1.69973577324958,2.95339246282403));
#7920=CARTESIAN_POINT('Ctrl Pts',(6.6,1.72966447542417,3.01558249180135));
#7921=CARTESIAN_POINT('Ctrl Pts',(6.6,1.73401928737242,3.02463152706096));
#7922=CARTESIAN_POINT('Ctrl Pts',(6.6,1.73830490042804,3.03371943563744));
#7923=CARTESIAN_POINT('Ctrl Pts',(6.6,1.74252093471433,3.04284531379462));
#7924=CARTESIAN_POINT('Ctrl Pts',(6.6,1.74801629838275,3.05474038291927));
#7925=CARTESIAN_POINT('Ctrl Pts',(6.6,1.75339345222138,3.06669996012485));
#7926=CARTESIAN_POINT('Ctrl Pts',(6.6,1.75865150293071,3.07872207211292));
#7927=CARTESIAN_POINT('Ctrl Pts',(6.6,1.76360055612823,3.09003768602855));
#7928=CARTESIAN_POINT('Ctrl Pts',(6.6,1.76844015485371,3.1013997152548));
#7929=CARTESIAN_POINT('Ctrl Pts',(6.6,1.77316959011757,3.11280520801871));
#7930=CARTESIAN_POINT('Ctrl Pts',(6.6,1.80041932406339,3.17852058966537));
#7931=CARTESIAN_POINT('Ctrl Pts',(6.6,1.82401955598892,3.24568623982158));
#7932=CARTESIAN_POINT('Ctrl Pts',(6.6,1.84389319791717,3.31394437453886));
#7933=CARTESIAN_POINT('Ctrl Pts',(6.6,1.86154775129936,3.37458081387317));
#7934=CARTESIAN_POINT('Ctrl Pts',(6.6,1.87626122908549,3.43608043797506));
#7935=CARTESIAN_POINT('Ctrl Pts',(6.6,1.88795171173133,3.49821270271176));
#7936=CARTESIAN_POINT('Ctrl Pts',(6.6,1.89137817487732,3.51642357746748));
#7937=CARTESIAN_POINT('Ctrl Pts',(6.6,1.89454475423252,3.5346888947779));
#7938=CARTESIAN_POINT('Ctrl Pts',(6.6,1.89744890221981,3.55300305386885));
#7939=CARTESIAN_POINT('Ctrl Pts',(6.6,1.89980101603368,3.5678359710534));
#7940=CARTESIAN_POINT('Ctrl Pts',(6.6,1.90197972572745,3.58269332812843));
#7941=CARTESIAN_POINT('Ctrl Pts',(6.6,1.9039834114727,3.59756590193512));
#7942=CARTESIAN_POINT('Ctrl Pts',(6.6,1.91367106629442,3.66947356594452));
#7943=CARTESIAN_POINT('Ctrl Pts',(6.6,1.91927795233095,3.74177918255773));
#7944=CARTESIAN_POINT('Ctrl Pts',(6.6,1.92070287200251,3.81413426669386));
#7945=CARTESIAN_POINT('Ctrl Pts',(6.6,1.92211579885107,3.8858803749454));
#7946=CARTESIAN_POINT('Ctrl Pts',(6.6,1.91941728760809,3.95767611431338));
#7947=CARTESIAN_POINT('Ctrl Pts',(6.6,1.91246071929237,4.02919789218586));
#7948=CARTESIAN_POINT('Ctrl Pts',(6.6,1.91122396329219,4.0419132115665));
#7949=CARTESIAN_POINT('Ctrl Pts',(6.6,1.9098524915949,4.05461989137718));
#7950=CARTESIAN_POINT('Ctrl Pts',(6.6,1.90834530359594,4.06731613031539));
#7951=CARTESIAN_POINT('Ctrl Pts',(2.5,0.863580915426621,5.40376507534352));
#7952=CARTESIAN_POINT('Ctrl Pts',(2.5,0.903481800679317,5.37926660921982));
#7953=CARTESIAN_POINT('Ctrl Pts',(2.5,0.942351921741602,5.35328747129858));
#7954=CARTESIAN_POINT('Ctrl Pts',(2.5,0.98009997800088,5.32582783981609));
#7955=CARTESIAN_POINT('Ctrl Pts',(2.5,1.03756562079836,5.28402475031965));
#7956=CARTESIAN_POINT('Ctrl Pts',(2.5,1.09243293237426,5.23879201435724));
#7957=CARTESIAN_POINT('Ctrl Pts',(2.5,1.14456529515591,5.19047296275182));
#7958=CARTESIAN_POINT('Ctrl Pts',(2.5,1.19725087194605,5.14164116292633));
#7959=CARTESIAN_POINT('Ctrl Pts',(2.5,1.2471436239525,5.08965615147515));
#7960=CARTESIAN_POINT('Ctrl Pts',(2.5,1.29405766001486,5.03484467912125));
#7961=CARTESIAN_POINT('Ctrl Pts',(2.5,1.32834049376268,4.99479072614897));
#7962=CARTESIAN_POINT('Ctrl Pts',(2.49999999999999,1.36103175781229,4.95322678141866));
#7963=CARTESIAN_POINT('Ctrl Pts',(2.5,1.39204180474702,4.91027607043137));
#7964=CARTESIAN_POINT('Ctrl Pts',(2.5,1.39932292818565,4.9001912927742));
#7965=CARTESIAN_POINT('Ctrl Pts',(2.5,1.40651184414629,4.89002911337057));
#7966=CARTESIAN_POINT('Ctrl Pts',(2.5,1.41359773403284,4.87980534663974));
#7967=CARTESIAN_POINT('Ctrl Pts',(2.5,1.4537289806095,4.82190259762929));
#7968=CARTESIAN_POINT('Ctrl Pts',(2.5,1.49063491990531,4.76192357977479));
#7969=CARTESIAN_POINT('Ctrl Pts',(2.5,1.5241744546024,4.70019324897602));
#7970=CARTESIAN_POINT('Ctrl Pts',(2.5,1.55724799453256,4.63932059289972));
#7971=CARTESIAN_POINT('Ctrl Pts',(2.5,1.58704824368533,4.57674389634121));
#7972=CARTESIAN_POINT('Ctrl Pts',(2.5,1.61339223682867,4.51276105655928));
#7973=CARTESIAN_POINT('Ctrl Pts',(2.5,1.63919258494756,4.45009859187415));
#7974=CARTESIAN_POINT('Ctrl Pts',(2.5,1.66167798030882,4.38608652278053));
#7975=CARTESIAN_POINT('Ctrl Pts',(2.5,1.68062808017528,4.32100573103691));
#7976=CARTESIAN_POINT('Ctrl Pts',(2.5,1.68520397395649,4.30529062703671));
#7977=CARTESIAN_POINT('Ctrl Pts',(2.5,1.68957350060244,4.28951324697453));
#7978=CARTESIAN_POINT('Ctrl Pts',(2.5,1.69373310938903,4.27367764327361));
#7979=CARTESIAN_POINT('Ctrl Pts',(2.5,1.69762827690034,4.25884876579445));
#7980=CARTESIAN_POINT('Ctrl Pts',(2.5,1.70134027318467,4.24396443866154));
#7981=CARTESIAN_POINT('Ctrl Pts',(2.5,1.70485982262735,4.22905603382341));
#7982=CARTESIAN_POINT('Ctrl Pts',(2.5,1.72026850374741,4.16378664070909));
#7983=CARTESIAN_POINT('Ctrl Pts',(2.5,1.73201964293855,4.09796147516516));
#7984=CARTESIAN_POINT('Ctrl Pts',(2.5,1.73995104778607,4.03185909017483));
#7985=CARTESIAN_POINT('Ctrl Pts',(2.5,1.74764478811446,3.96773746292473));
#7986=CARTESIAN_POINT('Ctrl Pts',(2.5,1.75174426392432,3.90335417483549));
#7987=CARTESIAN_POINT('Ctrl Pts',(2.5,1.75205333162734,3.83896894622148));
#7988=CARTESIAN_POINT('Ctrl Pts',(2.5,1.75223292383878,3.80155615453449));
#7989=CARTESIAN_POINT('Ctrl Pts',(2.5,1.75113178109454,3.76414287274798));
#7990=CARTESIAN_POINT('Ctrl Pts',(2.5,1.7487036258443,3.72678250885966));
#7991=CARTESIAN_POINT('Ctrl Pts',(2.5,1.74647840079726,3.69254449319611));
#7992=CARTESIAN_POINT('Ctrl Pts',(2.5,1.74313852381005,3.65835091190104));
#7993=CARTESIAN_POINT('Ctrl Pts',(2.5,1.73870317030216,3.62424537115788));
#7994=CARTESIAN_POINT('Ctrl Pts',(2.5,1.73685252518352,3.61001488143867));
#7995=CARTESIAN_POINT('Ctrl Pts',(2.5,1.73481112807425,3.59579974532583));
#7996=CARTESIAN_POINT('Ctrl Pts',(2.5,1.73258023476543,3.58160325113988));
#7997=CARTESIAN_POINT('Ctrl Pts',(2.5,1.73102147713734,3.57168395400586));
#7998=CARTESIAN_POINT('Ctrl Pts',(2.5,1.7293705537313,3.56177631081533));
#7999=CARTESIAN_POINT('Ctrl Pts',(2.5,1.72762964038082,3.55188979175844));
#8000=CARTESIAN_POINT('Ctrl Pts',(2.5,1.71639361008828,3.48808120095145));
#8001=CARTESIAN_POINT('Ctrl Pts',(2.5,1.7013973068787,3.42504861484961));
#8002=CARTESIAN_POINT('Ctrl Pts',(2.5,1.68284183603963,3.36305994407503));
#8003=CARTESIAN_POINT('Ctrl Pts',(2.5,1.663527963892,3.29853766531827));
#8004=CARTESIAN_POINT('Ctrl Pts',(2.5,1.64035754708482,3.23514519508613));
#8005=CARTESIAN_POINT('Ctrl Pts',(2.5,1.61350667224645,3.17321353421575));
#8006=CARTESIAN_POINT('Ctrl Pts',(2.5,1.59336851611767,3.12676478856296));
#8007=CARTESIAN_POINT('Ctrl Pts',(2.5,1.57115896484118,3.08113825840607));
#8008=CARTESIAN_POINT('Ctrl Pts',(2.5,1.54693754647141,3.03648971833169));
#8009=CARTESIAN_POINT('Ctrl Pts',(2.5,1.53615118929738,3.01660669194615));
#8010=CARTESIAN_POINT('Ctrl Pts',(2.5,1.52496597272822,2.99691826608897));
#8011=CARTESIAN_POINT('Ctrl Pts',(2.5,1.51338567219742,2.97743787138593));
#8012=CARTESIAN_POINT('Ctrl Pts',(2.5,1.50517306502384,2.96362261427262));
#8013=CARTESIAN_POINT('Ctrl Pts',(2.5,1.49676293575689,2.94991442666182));
#8014=CARTESIAN_POINT('Ctrl Pts',(2.5,1.48816920216178,2.93633689673824));
#8015=CARTESIAN_POINT('Ctrl Pts',(2.5,1.45429941367692,2.88282487410349));
#8016=CARTESIAN_POINT('Ctrl Pts',(2.5,1.41753605926436,2.83126366672452));
#8017=CARTESIAN_POINT('Ctrl Pts',(2.5,1.37802108941853,2.7819436771186));
#8018=CARTESIAN_POINT('Ctrl Pts',(2.5,1.3464603183726,2.7425515959399));
#8019=CARTESIAN_POINT('Ctrl Pts',(2.5,1.31314338874534,2.70458976729865));
#8020=CARTESIAN_POINT('Ctrl Pts',(2.5,1.27813049929784,2.66822683678827));
#8021=CARTESIAN_POINT('Ctrl Pts',(2.5,1.26549763847306,2.65510687303871));
#8022=CARTESIAN_POINT('Ctrl Pts',(2.5,1.25264391284352,2.64219524937818));
#8023=CARTESIAN_POINT('Ctrl Pts',(2.5,1.23957189874079,2.62950057750473));
#8024=CARTESIAN_POINT('Ctrl Pts',(2.5,1.23011804990051,2.62031962742118));
#8025=CARTESIAN_POINT('Ctrl Pts',(2.5,1.22055629636979,2.61125828180273));
#8026=CARTESIAN_POINT('Ctrl Pts',(2.5,1.21089009782921,2.6023212812504));
#8027=CARTESIAN_POINT('Ctrl Pts',(2.5,1.16593824479605,2.56076050286386));
#8028=CARTESIAN_POINT('Ctrl Pts',(2.5,1.11871429572554,2.5218704031965));
#8029=CARTESIAN_POINT('Ctrl Pts',(2.5,1.06933638089496,2.48594621693982));
#8030=CARTESIAN_POINT('Ctrl Pts',(2.5,1.01995846606438,2.45002203068315));
#8031=CARTESIAN_POINT('Ctrl Pts',(2.5,0.968425945013954,2.41706310482043));
#8032=CARTESIAN_POINT('Ctrl Pts',(2.5,0.914840821524557,2.3874184035349));
#8033=CARTESIAN_POINT('Ctrl Pts',(2.5,0.911106104645141,2.38535225981689));
#8034=CARTESIAN_POINT('Ctrl Pts',(2.5,0.907361412733174,2.38330223944661));
#8035=CARTESIAN_POINT('Ctrl Pts',(2.5,0.903606778650209,2.38126847156104));
#8036=CARTESIAN_POINT('Origin',(6.6,0.,3.64739446828387));
#8037=CARTESIAN_POINT('',(6.6,-1.15470053837925,3.64739446828387));
#8038=CARTESIAN_POINT('',(6.6,-0.577350269189626,4.64739446828387));
#8039=CARTESIAN_POINT('',(6.6,-1.01036297108184,3.89739446828387));
#8040=CARTESIAN_POINT('',(6.6,0.577350269189627,4.64739446828387));
#8041=CARTESIAN_POINT('',(6.6,-0.288675134594813,4.64739446828387));
#8042=CARTESIAN_POINT('',(6.6,1.15470053837925,3.64739446828387));
#8043=CARTESIAN_POINT('',(6.6,0.721687836487033,4.39739446828387));
#8044=CARTESIAN_POINT('',(6.6,0.577350269189625,2.64739446828387));
#8045=CARTESIAN_POINT('',(6.6,1.01036297108184,3.39739446828387));
#8046=CARTESIAN_POINT('',(6.6,-0.577350269189626,2.64739446828387));
#8047=CARTESIAN_POINT('',(6.6,0.288675134594812,2.64739446828387));
#8048=CARTESIAN_POINT('',(6.6,-0.721687836487032,2.89739446828387));
#8049=CARTESIAN_POINT('Origin',(6.6,-1.15470053837925,3.64739446828387));
#8050=CARTESIAN_POINT('',(6.1,-1.15470053837925,3.64739446828387));
#8051=CARTESIAN_POINT('',(6.6,-1.15470053837925,3.64739446828387));
#8052=CARTESIAN_POINT('',(6.1,-0.577350269189626,4.64739446828387));
#8053=CARTESIAN_POINT('',(6.1,-0.577350269189626,4.64739446828387));
#8054=CARTESIAN_POINT('',(6.6,-0.577350269189626,4.64739446828387));
#8055=CARTESIAN_POINT('Origin',(6.6,-0.577350269189626,2.64739446828387));
#8056=CARTESIAN_POINT('',(6.1,-0.577350269189626,2.64739446828387));
#8057=CARTESIAN_POINT('',(6.6,-0.577350269189626,2.64739446828387));
#8058=CARTESIAN_POINT('',(6.1,-1.15470053837925,3.64739446828387));
#8059=CARTESIAN_POINT('Origin',(6.6,0.577350269189625,2.64739446828387));
#8060=CARTESIAN_POINT('',(6.1,0.577350269189625,2.64739446828387));
#8061=CARTESIAN_POINT('',(6.6,0.577350269189625,2.64739446828387));
#8062=CARTESIAN_POINT('',(6.1,-0.577350269189626,2.64739446828387));
#8063=CARTESIAN_POINT('Origin',(6.6,1.15470053837925,3.64739446828387));
#8064=CARTESIAN_POINT('',(6.1,1.15470053837925,3.64739446828387));
#8065=CARTESIAN_POINT('',(6.6,1.15470053837925,3.64739446828387));
#8066=CARTESIAN_POINT('',(6.1,0.577350269189625,2.64739446828387));
#8067=CARTESIAN_POINT('Origin',(6.6,0.577350269189627,4.64739446828387));
#8068=CARTESIAN_POINT('',(6.1,0.577350269189627,4.64739446828387));
#8069=CARTESIAN_POINT('',(6.6,0.577350269189627,4.64739446828387));
#8070=CARTESIAN_POINT('',(6.1,1.15470053837925,3.64739446828387));
#8071=CARTESIAN_POINT('Origin',(6.6,-0.577350269189626,4.64739446828387));
#8072=CARTESIAN_POINT('',(6.1,0.577350269189627,4.64739446828387));
#8073=CARTESIAN_POINT('Origin',(6.1,0.,3.64739446828387));
#8074=CARTESIAN_POINT('Origin',(2.5,0.,3.64739446828387));
#12111=UNCERTAINTY_MEASURE_WITH_UNIT(LENGTH_MEASURE(0.01),#12119,
'DISTANCE_ACCURACY_VALUE',
'Maximum model space distance between geometric entities at asserted c
onnectivities');
#12113=UNCERTAINTY_MEASURE_WITH_UNIT(LENGTH_MEASURE(0.01),#12119,
'DISTANCE_ACCURACY_VALUE',
'Maximum model space distance between geometric entities at asserted c
onnectivities');
#12116=(
GEOMETRIC_REPRESENTATION_CONTEXT(3)
GLOBAL_UNCERTAINTY_ASSIGNED_CONTEXT((#12111))
GLOBAL_UNIT_ASSIGNED_CONTEXT((#12119,#12121,#12122))
REPRESENTATION_CONTEXT('','3D')
);
#12118=(
GEOMETRIC_REPRESENTATION_CONTEXT(3)
GLOBAL_UNCERTAINTY_ASSIGNED_CONTEXT((#12113))
GLOBAL_UNIT_ASSIGNED_CONTEXT((#12119,#12121,#12122))
REPRESENTATION_CONTEXT('','3D')
);
#12119=(
LENGTH_UNIT()
NAMED_UNIT(*)
SI_UNIT(.MILLI.,.METRE.)
);
#12121=(
NAMED_UNIT(*)
PLANE_ANGLE_UNIT()
SI_UNIT($,.RADIAN.)
);
#12122=(
NAMED_UNIT(*)
SI_UNIT($,.STERADIAN.)
SOLID_ANGLE_UNIT()
);
#12125=SHAPE_DEFINITION_REPRESENTATION(#12129,#12136);
#12129=PRODUCT_DEFINITION_SHAPE('',$,#12141);
#12136=SHAPE_REPRESENTATION('',(#2667),#12116);
#12138=PRODUCT_DEFINITION_CONTEXT('part definition',#12152,'design');
#12141=PRODUCT_DEFINITION('Screw_01','Screw_01',#12145,#12138);
#12145=PRODUCT_DEFINITION_FORMATION('',$,#12156);
#12152=APPLICATION_CONTEXT(
'Core Data for Automotive Mechanical Design Process');
#12153=PRODUCT_CONTEXT('part definition',#12152,'mechanical');
#12156=PRODUCT('Screw_01','Screw_01',$,(#12153));
#12159=PRESENTATION_STYLE_ASSIGNMENT((#12161));
#12161=SURFACE_STYLE_USAGE(.BOTH.,#12163);
#12163=SURFACE_SIDE_STYLE('',(#12165));
#12165=SURFACE_STYLE_FILL_AREA(#12167);
#12167=FILL_AREA_STYLE('Opaque(160,160,160)',(#12169));
#12169=FILL_AREA_STYLE_COLOUR('Opaque(160,160,160)',#12171);
#12171=COLOUR_RGB('Opaque(160,160,160)', 0.09019608, 0.27058824, 0.51372549);
ENDSEC;
END-ISO-10303-21;
